ISO-10303-21;
HEADER;
FILE_DESCRIPTION (('STEP AP214'),
    '1' );
FILE_NAME ('Locking Pawl Compression Spring.step',
    '2026-10-09T14:10:49',
    ( '' ),
    ( '' ),
    'SwSTEP 2.0',
    'SolidWorks 2026',
    '' );
FILE_SCHEMA (( 'AUTOMOTIVE_DESIGN' ));
ENDSEC;

DATA;
#2=CARTESIAN_POINT ( 'NONE',  ( 12.17369753589567871, 10.51393144722840134, 2.800165564711390775 ) ) ;
#4=CARTESIAN_POINT ( 'NONE',  ( 11.85962738539019945, 21.73984789707424170, 3.515838200515787548 ) ) ;
#6=CARTESIAN_POINT ( 'NONE',  ( 8.350682983910802548, 10.74290543192399028, 2.522985661756687037 ) ) ;
#7=CARTESIAN_POINT ( 'NONE',  ( 2.865713946637347131, 12.03281576442448042, 5.073952485450168304 ) ) ;
#11=CARTESIAN_POINT ( 'NONE',  ( 11.51539948528376733, 12.31998346384714083, 5.480917910381482017 ) ) ;
#14=CARTESIAN_POINT ( 'NONE',  ( 3.657427262928014677, 14.72322116853433194, 9.063302901626695274 ) ) ;
#17=CARTESIAN_POINT ( 'NONE',  ( 2.809774020526558225, 19.21875272216368202, 7.448689460942592433 ) ) ;
#25=CARTESIAN_POINT ( 'NONE',  ( 10.71174415246057698, 20.20840087037584709, 6.087647022013951137 ) ) ;
#28=CARTESIAN_POINT ( 'NONE',  ( 12.58269666770059381, 11.55388254762453215, 3.248295542190139606 ) ) ;
#31=CARTESIAN_POINT ( 'NONE',  ( 6.789087559929837923, 18.21544151669790068, 7.520383359049297667 ) ) ;
#42=CARTESIAN_POINT ( 'NONE',  ( 9.280550395262261887, 14.88029421051436429, 7.112226467325535317 ) ) ;
#43=CARTESIAN_POINT ( 'NONE',  ( 11.94459739279681543, 20.94853845629116051, 3.647987758710024675 ) ) ;
#44=CARTESIAN_POINT ( 'NONE',  ( 3.622293142213341088, 12.24591714145684129, 6.558976304062217544 ) ) ;
#45=CARTESIAN_POINT ( 'NONE',  ( 6.749462305694075681, 11.05277248166000170, 4.479057920628951805 ) ) ;
#50=CARTESIAN_POINT ( 'NONE',  ( 10.56693948759176571, 19.61111237035978050, 5.589555579635868021 ) ) ;
#51=CARTESIAN_POINT ( 'NONE',  ( 8.239716553926831111, 21.32987559984598391, 5.052740338774581730 ) ) ;
#59=CARTESIAN_POINT ( 'NONE',  ( 11.16210623263107848, 18.34813493204594081, -4.029110776031238572 ) ) ;
#60=CARTESIAN_POINT ( 'NONE',  ( 2.165347194003833575, 20.74767509450332170, 6.678208812454825782 ) ) ;
#63=CARTESIAN_POINT ( 'NONE',  ( 6.018011364848629974, 21.34202296141599930, 4.812272833256288074 ) ) ;
#75=CARTESIAN_POINT ( 'NONE',  ( 2.895144775783714763, 20.91827869092655945, 2.067392077668602113 ) ) ;
#90=CARTESIAN_POINT ( 'NONE',  ( 9.174791387338732562, 15.41930233576164433, -2.840203025228832612 ) ) ;
#91=CARTESIAN_POINT ( 'NONE',  ( 2.493085962414791190, 11.21420404894608147, 3.435105624136618907 ) ) ;
#98=CARTESIAN_POINT ( 'NONE',  ( 9.266976129945037499, 14.72489524569131092, 6.957161557103688665 ) ) ;
#100=CARTESIAN_POINT ( 'NONE',  ( 3.378324179703998453, 14.02502511948407715, 7.785346146968057823 ) ) ;
#105=CARTESIAN_POINT ( 'NONE',  ( 0.7283536316373762087, 20.30898886747102594, 1.952961586103617142 ) ) ;
#108=CARTESIAN_POINT ( 'NONE',  ( 6.774501940737490457, 19.51815128457440451, 6.453198523737214920 ) ) ;
#115=CARTESIAN_POINT ( 'NONE',  ( 13.04354795994631111, 16.76121402582646880, 7.282986886760092204 ) ) ;
#118=CARTESIAN_POINT ( 'NONE',  ( 13.35587560995692868, 16.38622677847037679, 7.171674097283092131 ) ) ;
#121=CARTESIAN_POINT ( 'NONE',  ( 8.292815045765784987, 10.74474575179219116, 2.280097550029496656 ) ) ;
#122=CARTESIAN_POINT ( 'NONE',  ( 0.8394066731220519717, 19.67029402086490109, 2.252889122871652106 ) ) ;
#124=CARTESIAN_POINT ( 'NONE',  ( 1.780815508985763129, 20.40739888885963182, 4.751999544564226241 ) ) ;
#126=CARTESIAN_POINT ( 'NONE',  ( 14.41880979295608078, 20.66289627653780059, 3.789204515037973398 ) ) ;
#127=CARTESIAN_POINT ( 'NONE',  ( 5.346755153171518948, 14.26008107018554760, 7.537986371638543126 ) ) ;
#129=CARTESIAN_POINT ( 'NONE',  ( 0.1976838887606784945, 19.02276410538376084, 0.6665157320697154830 ) ) ;
#132=CARTESIAN_POINT ( 'NONE',  ( -0.8299773975634847645, 19.84689652320655995, 3.579766241068111476 ) ) ;
#140=CARTESIAN_POINT ( 'NONE',  ( 9.883496637816898911, 21.64168280960603141, 3.868047802342164498 ) ) ;
#143=CARTESIAN_POINT ( 'NONE',  ( 12.42291455053379856, 11.33033927736581248, 2.552232267275179822 ) ) ;
#145=CARTESIAN_POINT ( 'NONE',  ( -0.7347962684923032839, 20.04712316396406280, 3.997874094937027944 ) ) ;
#151=CARTESIAN_POINT ( 'NONE',  ( 4.296253888929676634, 19.19961258863813214, 0.3083300652943509745 ) ) ;
#152=CARTESIAN_POINT ( 'NONE',  ( 6.396056618077795797, 11.71523274630726164, 2.847703469759983008 ) ) ;
#155=CARTESIAN_POINT ( 'NONE',  ( 8.179867684019033192, 11.48837196139402295, 1.858590186261403598 ) ) ;
#156=CARTESIAN_POINT ( 'NONE',  ( 3.477066233666421979, 20.55600749251701842, 3.648995514013453789 ) ) ;
#158=CARTESIAN_POINT ( 'NONE',  ( 13.15265190013183449, 16.70050942663215210, 6.498420246545746792 ) ) ;
#159=CARTESIAN_POINT ( 'NONE',  ( 3.286495487773421598, 20.56225727104456169, 1.886831981940775949 ) ) ;
#160=CARTESIAN_POINT ( 'NONE',  ( 7.189655306835470938, 16.38024503317697622, -2.993817834679030288 ) ) ;
#168=CARTESIAN_POINT ( 'NONE',  ( 11.06414373101206117, 17.47476261052015190, 6.688118229093674039 ) ) ;
#169=CARTESIAN_POINT ( 'NONE',  ( 7.463855498632248953, 18.37204556237463393, -2.667043638653753490 ) ) ;
#174=CARTESIAN_POINT ( 'NONE',  ( 3.353433880231968534, 14.74976095948969679, 9.067427483657878540 ) ) ;
#177=CARTESIAN_POINT ( 'NONE',  ( 7.475884085846502103, 16.82090011607979463, 8.373859609186036224 ) ) ;
#181=CARTESIAN_POINT ( 'NONE',  ( 1.895584402099029120, 14.60931841795548536, 0.4380894700145442355 ) ) ;
#187=CARTESIAN_POINT ( 'NONE',  ( 5.129543141202642431, 19.14094820344656256, 7.993442615763653336 ) ) ;
#199=CARTESIAN_POINT ( 'NONE',  ( 12.51949563173172741, 11.87357545845056173, 4.349419763020000218 ) ) ;
#200=CARTESIAN_POINT ( 'NONE',  ( 6.311431466362975584, 21.18174881316136293, 5.533192182388949831 ) ) ;
#207=CARTESIAN_POINT ( 'NONE',  ( 7.493187710091532061, 16.56948303458045402, -2.124950967123346857 ) ) ;
#217=CARTESIAN_POINT ( 'NONE',  ( -0.001022716578500358631, 17.78166323453216791, 0.2331896389956350235 ) ) ;
#219=CARTESIAN_POINT ( 'NONE',  ( 7.380557675095882786, 16.58762552368920851, 7.687920665816121435 ) ) ;
#224=CARTESIAN_POINT ( 'NONE',  ( 13.93482735099323833, 21.64660035503122160, 3.717575555280015376 ) ) ;
#226=CARTESIAN_POINT ( 'NONE',  ( 13.26836735398159028, 17.42901524731493268, 7.078061169219369120 ) ) ;
#230=CARTESIAN_POINT ( 'NONE',  ( 9.479476315004470521, 15.99709907451843094, 7.980467261906161625 ) ) ;
#231=CARTESIAN_POINT ( 'NONE',  ( 0.4810215415031842134, 12.38241104890028232, 3.423352113816969577 ) ) ;
#233=CARTESIAN_POINT ( 'NONE',  ( 5.697655638014817114, 17.11702998724009461, -1.340185189716478931 ) ) ;
#234=CARTESIAN_POINT ( 'NONE',  ( 7.228545246289955095, 16.94088807395186791, 7.597636453550198787 ) ) ;
#235=CARTESIAN_POINT ( 'NONE',  ( 1.159471316600563018, 20.10462493015178964, 3.144633053345586404 ) ) ;
#240=CARTESIAN_POINT ( 'NONE',  ( 7.753680531148133603, 16.37218494104095967, -2.740645328831583960 ) ) ;
#241=CARTESIAN_POINT ( 'NONE',  ( 5.362875270629205104, 14.52669407825994696, 7.666357001590486497 ) ) ;
#242=CARTESIAN_POINT ( 'NONE',  ( 1.227981727922097921, 21.11436061630988092, 3.317903474119387575 ) ) ;
#245=CARTESIAN_POINT ( 'NONE',  ( 1.820039393668895888, 20.48353144049298180, 4.932753874264384386 ) ) ;
#249=CARTESIAN_POINT ( 'NONE',  ( 9.544203190417185567, 21.84156436469462292, 2.933652179873399213 ) ) ;
#252=CARTESIAN_POINT ( 'NONE',  ( 11.27018246201781260, 13.25626094221269646, -2.577908581355527140 ) ) ;
#260=CARTESIAN_POINT ( 'NONE',  ( 6.053719233771420960, 11.12068933878565247, 2.906810406936975344 ) ) ;
#264=CARTESIAN_POINT ( 'NONE',  ( 9.225191506351318793, 16.57983669178404895, 7.321902877288878564 ) ) ;
#265=CARTESIAN_POINT ( 'NONE',  ( 6.962953135734946564, 20.81446147317312168, 1.610669861356619936 ) ) ;
#266=CARTESIAN_POINT ( 'NONE',  ( 5.021296906522759507, 20.20829226350481989, 6.496222906105421302 ) ) ;
#267=CARTESIAN_POINT ( 'NONE',  ( 9.106845709993205418, 13.32481467742428016, -2.904340219645574983 ) ) ;
#274=CARTESIAN_POINT ( 'NONE',  ( 11.18299850411455232, 14.10173808182719135, 6.301220783482575527 ) ) ;
#275=CARTESIAN_POINT ( 'NONE',  ( 9.073444559871269632, 11.49988781216720213, 5.501919269197937723 ) ) ;
#279=CARTESIAN_POINT ( 'NONE',  ( 3.327436967205598339, 17.33544538521946876, -1.277308115045836523 ) ) ;
#282=CARTESIAN_POINT ( 'NONE',  ( 6.938136749357236788, 11.33047045554270227, 5.170081444403209048 ) ) ;
#294=CARTESIAN_POINT ( 'NONE',  ( 4.339045286082956032, 20.93870084934459186, 5.966996860266638336 ) ) ;
#306=CARTESIAN_POINT ( 'NONE',  ( 11.70396778136748850, 11.04557676861940152, 0.8370681489755618099 ) ) ;
#307=CARTESIAN_POINT ( 'NONE',  ( 3.459298138910898768, 21.44911200421750053, 3.505279687176134473 ) ) ;
#310=CARTESIAN_POINT ( 'NONE',  ( 5.577942838035520268, 14.33718092923608189, 8.413711891740923932 ) ) ;
#315=CARTESIAN_POINT ( 'NONE',  ( 7.680790805331456639, 18.03565907245706157, -1.845473237927973909 ) ) ;
#320=CARTESIAN_POINT ( 'NONE',  ( 3.353557634575417445, 13.78425396933717550, 7.627037753281808108 ) ) ;
#324=CARTESIAN_POINT ( 'NONE',  ( 1.894691563267759227, 21.17677690942452173, 5.065541174868540608 ) ) ;
#327=CARTESIAN_POINT ( 'NONE',  ( 3.920009176498074233, 17.18772947144893948, -0.7115550442440029544 ) ) ;
#332=CARTESIAN_POINT ( 'NONE',  ( 11.14915617881719889, 15.67423727725497606, 7.664175941428390537 ) ) ;
#333=CARTESIAN_POINT ( 'NONE',  ( 6.380166963026771221, 10.92343582149830183, 2.794643371853744007 ) ) ;
#334=CARTESIAN_POINT ( 'NONE',  ( 13.12613710073441986, 18.43276909965920396, 6.801715849308650697 ) ) ;
#340=CARTESIAN_POINT ( 'NONE',  ( 9.473890731828024769, 14.30658367118552654, 7.614261666668934225 ) ) ;
#341=CARTESIAN_POINT ( 'NONE',  ( 1.873443166787216674, 20.48353144049298180, 4.916761300496329312 ) ) ;
#344=CARTESIAN_POINT ( 'NONE',  ( 5.621998597895612626, 14.20914477843347257, -0.8778548432169819282 ) ) ;
#347=CARTESIAN_POINT ( 'NONE',  ( 12.61840913414979148, 21.24843477279145887, -1.488277761717505143 ) ) ;
#349=CARTESIAN_POINT ( 'NONE',  ( 0.2609373283441706048, 20.95713891276306029, 6.401234835325384509 ) ) ;
#350=CARTESIAN_POINT ( 'NONE',  ( 0.04756687825572484402, 20.98775885821133969, 5.773728306871808158 ) ) ;
#359=CARTESIAN_POINT ( 'NONE',  ( 10.92996571811956308, 19.50708099122125816, 6.637236655515030392 ) ) ;
#363=CARTESIAN_POINT ( 'NONE',  ( 11.51451690588786292, 12.10267245616517684, -1.401170015314361583 ) ) ;
#365=CARTESIAN_POINT ( 'NONE',  ( -0.3966899150635756488, 20.30256849354482185, 4.863884106276985086 ) ) ;
#370=CARTESIAN_POINT ( 'NONE',  ( 4.663792239772604376, 20.04349882488605417, 1.216183641137849936 ) ) ;
#375=CARTESIAN_POINT ( 'NONE',  ( 9.387588499473343617, 14.88153510792360024, 7.075887779341390349 ) ) ;
#376=CARTESIAN_POINT ( 'NONE',  ( 4.517629800827023701, 19.79998728558659238, 6.347442110243458835 ) ) ;
#378=CARTESIAN_POINT ( 'NONE',  ( 9.134405411020685150, 21.15227197021270200, 1.760129399948058282 ) ) ;
#379=CARTESIAN_POINT ( 'NONE',  ( 1.869769858248796046, 17.31795573271877942, 9.441083779479226834 ) ) ;
#380=CARTESIAN_POINT ( 'NONE',  ( 5.428607670497170190, 17.41093948017483939, -2.167354582218313563 ) ) ;
#386=CARTESIAN_POINT ( 'NONE',  ( 11.18374392228187908, 14.11224683893468068, 6.306351795193365639 ) ) ;
#387=CARTESIAN_POINT ( 'NONE',  ( 10.92933365986669259, 16.27139426067511607, -4.476694603249527837 ) ) ;
#390=CARTESIAN_POINT ( 'NONE',  ( 10.37510084784339703, 11.39042657884375309, 2.489853968234712500 ) ) ;
#393=CARTESIAN_POINT ( 'NONE',  ( 3.768687125443949348, 21.23176840745776062, 5.325114473994855935 ) ) ;
#396=CARTESIAN_POINT ( 'NONE',  ( 7.546623658496745435, 15.46605242080309850, 8.328871668325708910 ) ) ;
#402=CARTESIAN_POINT ( 'NONE',  ( 0.05840936790434386044, 16.18753194106394488, 0.7989642439863056111 ) ) ;
#421=CARTESIAN_POINT ( 'NONE',  ( 12.79548546626584127, 18.46234326053249220, 6.094044533436631994 ) ) ;
#423=CARTESIAN_POINT ( 'NONE',  ( 5.508019599735664684, 17.51021144529294560, 8.768403766408770394 ) ) ;
#426=CARTESIAN_POINT ( 'NONE',  ( 4.517480175593667546, 11.08280834804601156, 3.521422171990641559 ) ) ;
#429=CARTESIAN_POINT ( 'NONE',  ( 7.502072049523423658, 16.67234806097842892, -2.119060137569175772 ) ) ;
#433=CARTESIAN_POINT ( 'NONE',  ( 3.419769351041428873, 15.73143490412445900, 8.402936401063445970 ) ) ;
#441=CARTESIAN_POINT ( 'NONE',  ( 1.954711710866990693, 21.15578882893498047, 5.227293067434886531 ) ) ;
#444=CARTESIAN_POINT ( 'NONE',  ( 2.034109762226206541, 15.64505045901557345, 9.146289368853217638 ) ) ;
#452=CARTESIAN_POINT ( 'NONE',  ( 8.728086753073649007, 15.35048014666334559, -3.127714312744253711 ) ) ;
#456=CARTESIAN_POINT ( 'NONE',  ( 13.18577270084679576, 12.49465483329842286, 5.809243337312416600 ) ) ;
#461=CARTESIAN_POINT ( 'NONE',  ( 9.262764579346530525, 18.14018762746578517, 7.695032825047638525 ) ) ;
#463=CARTESIAN_POINT ( 'NONE',  ( 0.2422206219147293726, 20.17819236544972128, 6.176747626244641687 ) ) ;
#465=CARTESIAN_POINT ( 'NONE',  ( 5.857566774899138906, 18.14988412973438159, -1.063936251482671569 ) ) ;
#467=CARTESIAN_POINT ( 'NONE',  ( 8.463232041149611362, 10.77439257666578243, 1.655928866917091069 ) ) ;
#469=CARTESIAN_POINT ( 'NONE',  ( 1.877249823927544359, 13.01816804744978207, 0.3577989692409621059 ) ) ;
#470=CARTESIAN_POINT ( 'NONE',  ( 1.260594148623912059, 18.90536103616748775, 8.891112515372604719 ) ) ;
#473=CARTESIAN_POINT ( 'NONE',  ( 7.221254323107455519, 13.47081914689558069, 6.792995896567122216 ) ) ;
#479=CARTESIAN_POINT ( 'NONE',  ( 10.83806774996162403, 19.83502426011275688, 6.410176537624181492 ) ) ;
#483=CARTESIAN_POINT ( 'NONE',  ( 11.29923878586181196, 13.07119654552437638, -2.429333208372020270 ) ) ;
#491=CARTESIAN_POINT ( 'NONE',  ( 9.758652622545607613, 18.90452467200534414, -2.337483130687342925 ) ) ;
#494=CARTESIAN_POINT ( 'NONE',  ( 12.27885220188135484, 20.89247853322200044, -1.186209537071461151 ) ) ;
#495=CARTESIAN_POINT ( 'NONE',  ( 1.550445315360883258, 21.03017768341116067, 3.245805655982831439 ) ) ;
#497=CARTESIAN_POINT ( 'NONE',  ( 11.09799212544334246, 12.31865010030356089, -2.962437906143603250 ) ) ;
#502=CARTESIAN_POINT ( 'NONE',  ( 6.897255242458841806, 21.59165172380602371, 1.391285824881070221 ) ) ;
#506=CARTESIAN_POINT ( 'NONE',  ( 10.05115496733982638, 11.45101544124467097, 1.083611332447474540 ) ) ;
#509=CARTESIAN_POINT ( 'NONE',  ( 2.579550200575633223, 11.32322398379630179, 5.299602097076567375 ) ) ;
#532=CARTESIAN_POINT ( 'NONE',  ( 12.33551329399142915, 11.22339177084746176, 2.585388245275515917 ) ) ;
#533=CARTESIAN_POINT ( 'NONE',  ( 2.840321306701502291, 20.92456416987101875, 1.832874750768024086 ) ) ;
#536=CARTESIAN_POINT ( 'NONE',  ( 4.164513427734910067, 11.38116224488952177, 2.006366593415208399 ) ) ;
#540=CARTESIAN_POINT ( 'NONE',  ( 7.555449444248006685, 13.41026002100023184, -1.138537544275743274 ) ) ;
#543=CARTESIAN_POINT ( 'NONE',  ( 3.211736503681509980, 12.96355677795110140, 6.856356644963555347 ) ) ;
#548=CARTESIAN_POINT ( 'NONE',  ( 1.864588651777728590, 21.18383126686373430, 4.984355216872713434 ) ) ;
#550=CARTESIAN_POINT ( 'NONE',  ( 5.577949907072537350, 17.33943586079730181, 8.015011952332226741 ) ) ;
#559=CARTESIAN_POINT ( 'NONE',  ( 8.185500201082774652, 11.14036371107460255, 3.740216416401582755 ) ) ;
#562=CARTESIAN_POINT ( 'NONE',  ( 11.75539605838384638, 10.66431821468159136, -0.2581068381348511354 ) ) ;
#566=CARTESIAN_POINT ( 'NONE',  ( 7.725504655093541118, 11.48266921152324116, -0.1321688645820411623 ) ) ;
#567=CARTESIAN_POINT ( 'NONE',  ( 4.559726464520669431, 19.87799086262558035, 6.390853160755138873 ) ) ;
#569=CARTESIAN_POINT ( 'NONE',  ( 5.638166626312271390, 14.02190832120166775, -0.7723171704840984253 ) ) ;
#571=CARTESIAN_POINT ( 'NONE',  ( 0.9615939815707198468, 19.83869222877949667, 2.643595094647703370 ) ) ;
#574=CARTESIAN_POINT ( 'NONE',  ( 14.39495272017181016, 21.28532635717934340, 3.392014037587451458 ) ) ;
#576=CARTESIAN_POINT ( 'NONE',  ( 4.913515329053552705, 12.19104956382561689, 5.302203639509063038 ) ) ;
#577=CARTESIAN_POINT ( 'NONE',  ( 3.777435572934427110, 12.19982130767714246, 0.3897271289892410562 ) ) ;
#580=CARTESIAN_POINT ( 'NONE',  ( 4.502328515861612424, 19.89758433537658178, 0.8700102451280966598 ) ) ;
#585=CARTESIAN_POINT ( 'NONE',  ( 9.969205024995844155, 10.71176808653972223, 0.7780162768078369151 ) ) ;
#588=CARTESIAN_POINT ( 'NONE',  ( 11.20238673225087211, 13.86092089083514800, -2.958941917828961543 ) ) ;
#596=CARTESIAN_POINT ( 'NONE',  ( 9.466445536643458780, 17.21895884409014599, -2.918710521388331092 ) ) ;
#598=CARTESIAN_POINT ( 'NONE',  ( 4.551873131176118470, 19.73415439451352427, 6.433038573175717367 ) ) ;
#599=CARTESIAN_POINT ( 'NONE',  ( 8.554937540587033595, 20.63193666139594029, 0.1873199234380305001 ) ) ;
#600=CARTESIAN_POINT ( 'NONE',  ( 3.820173452861999053, 13.16763011922862070, 8.063327502814468417 ) ) ;
#606=CARTESIAN_POINT ( 'NONE',  ( 11.21453129928410597, 15.64639171652562588, 6.772637486115957728 ) ) ;
#607=CARTESIAN_POINT ( 'NONE',  ( 9.432974783129361995, 11.74680749646248223, -1.582753286535103499 ) ) ;
#610=CARTESIAN_POINT ( 'NONE',  ( 9.349647467888569707, 16.65363258022448179, -2.856910848570457961 ) ) ;
#613=CARTESIAN_POINT ( 'NONE',  ( 7.115219445481534066, 13.03499949018002191, 7.425824234857630657 ) ) ;
#616=CARTESIAN_POINT ( 'NONE',  ( 6.832388641462657120, 11.15782348525851120, 4.714514794290550981 ) ) ;
#634=CARTESIAN_POINT ( 'NONE',  ( 0.2965678313766248464, 20.95713891276306029, 6.390564738160584568 ) ) ;
#637=CARTESIAN_POINT ( 'NONE',  ( 5.548917213503941070, 13.89478552866151695, 8.213063205195311411 ) ) ;
#643=CARTESIAN_POINT ( 'NONE',  ( 1.460844719705742367, 14.43398395740774554, 8.397187112944255460 ) ) ;
#644=ORIENTED_EDGE ( 'NONE', *, *, #3564, .T. ) ;
#650=CARTESIAN_POINT ( 'NONE',  ( 3.604055471673875743, 16.46645633495994687, 9.203776892202039761 ) ) ;
#652=( GEOMETRIC_REPRESENTATION_CONTEXT ( 3 ) GLOBAL_UNCERTAINTY_ASSIGNED_CONTEXT ( ( #15443 ) ) GLOBAL_UNIT_ASSIGNED_CONTEXT ( ( #4485, #7792, #7584 ) ) REPRESENTATION_CONTEXT ( 'NONE', 'WORKASPACE' ) );
#653=CARTESIAN_POINT ( 'NONE',  ( 7.000609123144855062, 19.58301787754098200, 6.453108639060604723 ) ) ;
#659=CARTESIAN_POINT ( 'NONE',  ( 7.358775753619412718, 11.69576222774042229, 0.1904761656118920121 ) ) ;
#662=CARTESIAN_POINT ( 'NONE',  ( 11.28216995687987279, 11.80526944224940777, -2.285198803090960240 ) ) ;
#668=CARTESIAN_POINT ( 'NONE',  ( 7.246288661058416736, 14.17700572773325618, -2.455816413159584766 ) ) ;
#669=CARTESIAN_POINT ( 'NONE',  ( 3.783282799006013164, 14.05198016149147122, -0.1472696480691887966 ) ) ;
#671=CARTESIAN_POINT ( 'NONE',  ( 6.022052921700177919, 18.85282495273109760, -0.7063640773682651197 ) ) ;
#675=CARTESIAN_POINT ( 'NONE',  ( 7.067964712802636384, 11.13551934581288094, 4.361396337857177841 ) ) ;
#676=CARTESIAN_POINT ( 'NONE',  ( 4.643852685068835306, 11.88709150950850280, 4.078001338485435667 ) ) ;
#678=CARTESIAN_POINT ( 'NONE',  ( 2.864312977351492595, 11.23735775897588240, 5.231261027419050968 ) ) ;
#682=CARTESIAN_POINT ( 'NONE',  ( 6.162093721932920154, 20.44527992609954126, 5.228833816242916654 ) ) ;
#688=CARTESIAN_POINT ( 'NONE',  ( 9.637199341109212725, 11.24896747874181280, -0.6285487678327054129 ) ) ;
#692=CARTESIAN_POINT ( 'NONE',  ( 11.17252035512641406, 14.29393921748002505, -3.161770295153791821 ) ) ;
#693=CARTESIAN_POINT ( 'NONE',  ( 5.366064009540067126, 15.47516136557390176, -2.081252157664847502 ) ) ;
#700=CARTESIAN_POINT ( 'NONE',  ( 13.16576134418140676, 13.22236995718078134, 5.489006338729662815 ) ) ;
#702=CARTESIAN_POINT ( 'NONE',  ( 7.448594639129619388, 14.64975276093931100, -1.928932895048531826 ) ) ;
#706=CARTESIAN_POINT ( 'NONE',  ( 4.078297738883024159, 21.19975011080603977, 5.266598747592275309 ) ) ;
#711=CARTESIAN_POINT ( 'NONE',  ( 11.21068335584656950, 15.75969117811444953, 6.785562080493880543 ) ) ;
#712=CARTESIAN_POINT ( 'NONE',  ( 8.439759197263338564, 21.35170238401046205, -0.1649572212692822781 ) ) ;
#716=CARTESIAN_POINT ( 'NONE',  ( 9.461280943800495891, 13.02742443158000185, -1.607818659218023027 ) ) ;
#721=CARTESIAN_POINT ( 'NONE',  ( 5.979923096379600622, 10.94213887786034078, 2.451138684234262843 ) ) ;
#724=CARTESIAN_POINT ( 'NONE',  ( 7.260258248780015577, 12.25695181527388478, 6.604289441735033073 ) ) ;
#744=CARTESIAN_POINT ( 'NONE',  ( 4.406439411525544081, 20.54241105020114233, 0.3878223501788354843 ) ) ;
#748=CARTESIAN_POINT ( 'NONE',  ( 5.161554602150648208, 11.81472031015017166, 6.306168054739473838 ) ) ;
#752=CARTESIAN_POINT ( 'NONE',  ( 1.284022825976741000, 13.11577469953204655, 7.340846339184095903 ) ) ;
#761=CARTESIAN_POINT ( 'NONE',  ( 1.635490509552675942, 21.19865827025175520, 4.366209288297318025 ) ) ;
#766=CARTESIAN_POINT ( 'NONE',  ( 1.821934098042296446, 12.85015660565266060, 7.648703090803636861 ) ) ;
#773=CARTESIAN_POINT ( 'NONE',  ( 12.82931649728759282, 16.73453105516203721, 7.016643571353146314 ) ) ;
#776=CARTESIAN_POINT ( 'NONE',  ( 12.88484886689720810, 11.29734215691586208, 4.459301396266069695 ) ) ;
#783=CARTESIAN_POINT ( 'NONE',  ( 7.240898627860822501, 16.21294576777124519, -2.887031719764514115 ) ) ;
#786=CARTESIAN_POINT ( 'NONE',  ( 8.850476390893977197, 18.78072660019471840, 6.559035762646428402 ) ) ;
#787=CARTESIAN_POINT ( 'NONE',  ( 7.228733647532628481, 13.55792429055235715, 6.729328822189224013 ) ) ;
#792=CARTESIAN_POINT ( 'NONE',  ( 9.070861399739685638, 20.13899192311416186, 6.446725801674014100 ) ) ;
#795=CARTESIAN_POINT ( 'NONE',  ( 1.651338490073621879, 16.44735884859098718, -0.7918851340569855735 ) ) ;
#799=CARTESIAN_POINT ( 'NONE',  ( 2.084092584291341588, 17.94179249953145217, 0.2586688736977448833 ) ) ;
#807=CARTESIAN_POINT ( 'NONE',  ( 11.12436898423977638, 12.00734156490978677, 5.678099997755476025 ) ) ;
#810=CARTESIAN_POINT ( 'NONE',  ( 11.59421558736491598, 19.10596872916567435, -2.836117574684339449 ) ) ;
#811=CARTESIAN_POINT ( 'NONE',  ( 5.370882954727737690, 14.76353563683550263, -1.916208718001963796 ) ) ;
#813=CARTESIAN_POINT ( 'NONE',  ( 1.770729414466086782, 14.88544593074506928, 0.2654498043701122301 ) ) ;
#816=CARTESIAN_POINT ( 'NONE',  ( -0.1849527129589544072, 21.03045532914853055, 5.150944214860931680 ) ) ;
#820=CARTESIAN_POINT ( 'NONE',  ( 6.917893308609325942, 12.02983150285682079, 4.746903262785427735 ) ) ;
#821=CARTESIAN_POINT ( 'NONE',  ( 9.401342779853303355, 17.21989818313373988, -2.904324505523894651 ) ) ;
#822=CARTESIAN_POINT ( 'NONE',  ( 10.88895342146457601, 14.15760627606356081, -4.055013420937678248 ) ) ;
#829=CARTESIAN_POINT ( 'NONE',  ( 5.317747445270939011, 13.58815257356176076, -1.516694713297795261 ) ) ;
#832=CARTESIAN_POINT ( 'NONE',  ( 11.63049744206901792, 21.11709313486170103, 2.852222637699519669 ) ) ;
#835=CARTESIAN_POINT ( 'NONE',  ( 0.9037643508957434735, 18.98659669545878259, 7.881339249872772790 ) ) ;
#836=CARTESIAN_POINT ( 'NONE',  ( 5.211679344434179129, 21.23839086782724195, 3.885610057435962439 ) ) ;
#849=CARTESIAN_POINT ( 'NONE',  ( 12.06368358668478891, 10.32531656698114020, 0.6252471565032120537 ) ) ;
#861=CARTESIAN_POINT ( 'NONE',  ( 2.098362976749927888, 11.83352507831272149, 1.754813491889370747 ) ) ;
#864=CARTESIAN_POINT ( 'NONE',  ( 3.589437315726493605, 16.93684646903384206, -1.402224914170865810 ) ) ;
#869=CARTESIAN_POINT ( 'NONE',  ( 1.435649018927920739, 14.09384548075437138, 8.206564140987731903 ) ) ;
#876=CARTESIAN_POINT ( 'NONE',  ( 2.788940323695707768, 11.28012997864750311, 4.828948434681314517 ) ) ;
#878=CARTESIAN_POINT ( 'NONE',  ( 7.672689199289790984, 14.92411314052326965, 7.513769365600475147 ) ) ;
#880=CARTESIAN_POINT ( 'NONE',  ( 13.28857892897944382, 22.14715058108314594, 1.978915458932410720 ) ) ;
#883=EDGE_LOOP ( 'NONE', ( #644, #21861, #15270, #2551 ) ) ;
#885=CARTESIAN_POINT ( 'NONE',  ( 5.451387325446391152, 19.02104356353402181, -1.049876524968703428 ) ) ;
#888=CARTESIAN_POINT ( 'NONE',  ( 12.66657608565324544, 10.81635483712285151, 3.529341624401947541 ) ) ;
#893=CARTESIAN_POINT ( 'NONE',  ( 7.233312877372291894, 16.04677007903879726, -2.879531353839789087 ) ) ;
#897=CARTESIAN_POINT ( 'NONE',  ( 8.104304450262016957, 20.50171273394048299, 4.697722215350715658 ) ) ;
#901=CARTESIAN_POINT ( 'NONE',  ( 7.526225150842845046, 18.37388711802374530, -2.690556271596364901 ) ) ;
#904=CARTESIAN_POINT ( 'NONE',  ( 0.7365175131326759939, 11.31684784372412089, 4.865384749232847916 ) ) ;
#905=CARTESIAN_POINT ( 'NONE',  ( 0.5885023020491949586, 11.47569386093249300, 4.096986995605308657 ) ) ;
#907=CARTESIAN_POINT ( 'NONE',  ( 5.237852948251049412, 17.31877066267591658, 8.028226905314944872 ) ) ;
#913=CARTESIAN_POINT ( 'NONE',  ( 9.454490738039723396, 11.77944925497319595, -1.426592419569617354 ) ) ;
#916=CARTESIAN_POINT ( 'NONE',  ( 5.487919320111488197, 17.38806467533618516, -2.066457398598804396 ) ) ;
#918=CARTESIAN_POINT ( 'NONE',  ( 0.3644238609685282460, 12.38707500932596162, 3.460104896903041016 ) ) ;
#921=CARTESIAN_POINT ( 'NONE',  ( 5.850959131300735194, 20.65587636292193352, 4.328574444934527143 ) ) ;
#925=CARTESIAN_POINT ( 'NONE',  ( 9.411590077691956324, 21.23906099414256232, 1.666482855468156332 ) ) ;
#926=CARTESIAN_POINT ( 'NONE',  ( 9.754543803393604051, 21.05370774754728203, 3.404076865865295343 ) ) ;
#927=CARTESIAN_POINT ( 'NONE',  ( 3.676745431939328235, 18.24815116393151015, 8.767987032105414968 ) ) ;
#928=CARTESIAN_POINT ( 'NONE',  ( 13.54273369681055428, 22.20171528482708112, 2.439503800205132134 ) ) ;
#931=CARTESIAN_POINT ( 'NONE',  ( 3.128535511035963612, 21.16459892206533056, 2.693085165987005869 ) ) ;
#936=CARTESIAN_POINT ( 'NONE',  ( 10.90457161609252168, 21.16733262328514442, 0.8920809610247827370 ) ) ;
#938=CARTESIAN_POINT ( 'NONE',  ( 0.2293556595113930840, 20.07828324242409579, 6.214976256840158975 ) ) ;
#939=CARTESIAN_POINT ( 'NONE',  ( 2.064884689569050469, 11.61267145053902006, 3.635488099080468327 ) ) ;
#949=CARTESIAN_POINT ( 'NONE',  ( 12.44452585099119624, 19.94285714604490067, 5.084842939140666651 ) ) ;
#959=CARTESIAN_POINT ( 'NONE',  ( -0.07327418442642195939, 17.37668286801814688, 0.02659433903688191228 ) ) ;
#962=CARTESIAN_POINT ( 'NONE',  ( 3.826978250008152838, 18.56559772987111856, -0.9675601391790299433 ) ) ;
#973=CARTESIAN_POINT ( 'NONE',  ( 3.099914158177832224, 11.64373280860985105, 6.183033039608584858 ) ) ;
#982=CARTESIAN_POINT ( 'NONE',  ( 10.60640877659219861, 16.27109148020024421, -3.957100436307429359 ) ) ;
#985=CARTESIAN_POINT ( 'NONE',  ( 11.62203808576201958, 20.29981520329449296, -2.921068254133583508 ) ) ;
#990=CARTESIAN_POINT ( 'NONE',  ( 7.469192301192234318, 18.32891399945091848, -2.552061295666830265 ) ) ;
#993=CARTESIAN_POINT ( 'NONE',  ( 8.898720949407623593, 18.59683926628043338, 6.668590119552477269 ) ) ;
#995=CARTESIAN_POINT ( 'NONE',  ( 2.290308818630598431, 20.10037469023196621, 6.068923932348192274 ) ) ;
#998=CARTESIAN_POINT ( 'NONE',  ( 11.50899041575192783, 13.68104675248728164, 7.058214869108054401 ) ) ;
#1002=CARTESIAN_POINT ( 'NONE',  ( 4.141897743895355255, 11.26628406262684301, 2.001306006738907683 ) ) ;
#1003=CARTESIAN_POINT ( 'NONE',  ( 0.8150964148941177712, 11.42577256918107054, 5.083379029272794725 ) ) ;
#1005=CARTESIAN_POINT ( 'NONE',  ( 5.353244178343441462, 14.21749487271361190, 7.624480077791540467 ) ) ;
#1010=VERTEX_POINT ( 'NONE', #12138 ) ;
#1014=CARTESIAN_POINT ( 'NONE',  ( 11.44223642946347042, 15.42323504901881748, 7.509133475055971729 ) ) ;
#1017=CARTESIAN_POINT ( 'NONE',  ( 11.75036113457564113, 19.64364350978045692, -2.459295084851638613 ) ) ;
#1018=CARTESIAN_POINT ( 'NONE',  ( 5.438185394540740347, 13.64782653932916112, -1.443462502430749694 ) ) ;
#1020=CARTESIAN_POINT ( 'NONE',  ( 5.534656983323768209, 20.82992769506763864, 3.759961556826081353 ) ) ;
#1023=CARTESIAN_POINT ( 'NONE',  ( 5.724697889559749342, 20.71246359673639148, 3.995336445546636472 ) ) ;
#1026=CARTESIAN_POINT ( 'NONE',  ( 5.955902939063514090, 17.26127046106770635, -1.587797145480220440 ) ) ;
#1032=DIRECTION ( 'NONE',  ( 0.000000000000000000, 1.000000000000000000, -0.000000000000000000 ) ) ;
#1041=CARTESIAN_POINT ( 'NONE',  ( 12.03222557419000083, 20.69458624090882992, 3.924755836542371146 ) ) ;
#1043=CARTESIAN_POINT ( 'NONE',  ( 1.475850426351400291, 15.62743466753882871, 8.791782170180653111 ) ) ;
#1045=CARTESIAN_POINT ( 'NONE',  ( 5.581558841844106666, 11.65935603284404287, 0.7263510631195396750 ) ) ;
#1053=CARTESIAN_POINT ( 'NONE',  ( 0.2174850097829113538, 17.55712011575143450, 0.9574576086920399964 ) ) ;
#1055=CARTESIAN_POINT ( 'NONE',  ( 13.10833390419068323, 16.70056792996117068, 6.512416574496136867 ) ) ;
#1056=CARTESIAN_POINT ( 'NONE',  ( 2.655202054194977457, 19.64359183480943472, 1.537090893787881996 ) ) ;
#1057=CARTESIAN_POINT ( 'NONE',  ( 13.66015131967467156, 22.20657701893900082, 2.405489038835227689 ) ) ;
#1070=CARTESIAN_POINT ( 'NONE',  ( 1.263612230954551441, 21.11436061630988092, 3.307233376954588078 ) ) ;
#1073=CARTESIAN_POINT ( 'NONE',  ( 3.760528279849136180, 12.52252298731752767, 0.1935317675302483942 ) ) ;
#1085=CARTESIAN_POINT ( 'NONE',  ( 3.358315432832535308, 12.36100630735107586, 7.353239250121181847 ) ) ;
#1097=CARTESIAN_POINT ( 'NONE',  ( 9.024438055949596915, 14.85500521735966295, 7.276239533518110036 ) ) ;
#1100=CARTESIAN_POINT ( 'NONE',  ( 10.95655038952506821, 16.44103435568498028, -4.352389034132393419 ) ) ;
#1105=CARTESIAN_POINT ( 'NONE',  ( 8.298824244370219816, 21.01560961795355453, -0.4802659323016266191 ) ) ;
#1106=CARTESIAN_POINT ( 'NONE',  ( 6.566377038699175550, 20.23523262331454475, 0.6328596530739121206 ) ) ;
#1110=CARTESIAN_POINT ( 'NONE',  ( 13.60230603414709094, 21.45952595875148106, 1.784047991531949817 ) ) ;
#1113=CARTESIAN_POINT ( 'NONE',  ( 2.053946910387165037, 11.83412605131448103, 1.768482334681878765 ) ) ;
#1114=CARTESIAN_POINT ( 'NONE',  ( 0.5391250270183256532, 11.52139035671227063, 3.880880414641454390 ) ) ;
#1118=CARTESIAN_POINT ( 'NONE',  ( 3.546748655274437390, 20.63951482243974311, 3.565519225599600439 ) ) ;
#1125=CARTESIAN_POINT ( 'NONE',  ( 9.071028239221552880, 14.95428965682947364, -3.447124252751109896 ) ) ;
#1129=CARTESIAN_POINT ( 'NONE',  ( 12.78393319624934676, 21.33321389937485080, 0.2603733278526269568 ) ) ;
#1130=CARTESIAN_POINT ( 'NONE',  ( 6.221313271974531212, 20.46396301300350373, -0.3603416905545633320 ) ) ;
#1133=CARTESIAN_POINT ( 'NONE',  ( 0.02879538837996780537, 15.70524387060945948, 0.7619693622286592971 ) ) ;
#1141=CARTESIAN_POINT ( 'NONE',  ( 9.620285707524375951, 14.85500521735966295, 7.097803873153455179 ) ) ;
#1143=CARTESIAN_POINT ( 'NONE',  ( 3.493358086098580895, 18.28455830479323652, 8.910730656749969114 ) ) ;
#1151=FACE_OUTER_BOUND ( 'NONE', #18739, .T. ) ;
#1158=CARTESIAN_POINT ( 'NONE',  ( 12.44961998140978920, 19.86344286058260877, 5.004692419167065864 ) ) ;
#1159=CARTESIAN_POINT ( 'NONE',  ( 0.6401730578246815906, 19.56094186154469128, 7.247650664160103062 ) ) ;
#1167=CARTESIAN_POINT ( 'NONE',  ( 0.1329439002683138471, 16.97859826092474123, 0.8348816815925818036 ) ) ;
#1172=CARTESIAN_POINT ( 'NONE',  ( 11.27301368098517109, 12.84969026437554085, -2.377990926030757901 ) ) ;
#1173=CARTESIAN_POINT ( 'NONE',  ( 2.780407218318890816, 19.89006846276929252, 1.848699377103335983 ) ) ;
#1176=CARTESIAN_POINT ( 'NONE',  ( 13.07922436883402639, 18.81117101484460363, 6.777410824046630644 ) ) ;
#1185=CARTESIAN_POINT ( 'NONE',  ( 3.462698832070913113, 13.65298187125114282, -0.7916853570755781888 ) ) ;
#1188=CARTESIAN_POINT ( 'NONE',  ( 4.384153316260242406, 20.40071751837500713, 0.3961553867452964339 ) ) ;
#1192=CARTESIAN_POINT ( 'NONE',  ( 0.7351087584799428365, 12.21554749956470154, 4.727313382918564955 ) ) ;
#1201=CARTESIAN_POINT ( 'NONE',  ( 3.191654872741395810, 11.85014480429067518, 6.591825004443473190 ) ) ;
#1210=CARTESIAN_POINT ( 'NONE',  ( 10.37976351492118177, 21.20110815220486344, 0.3605273278593796316 ) ) ;
#1211=CARTESIAN_POINT ( 'NONE',  ( 1.317196433845851278, 18.94197024501346505, 8.977327884498558674 ) ) ;
#1214=CARTESIAN_POINT ( 'NONE',  ( 11.08703814780444574, 12.78412554608461704, -3.188527895529572831 ) ) ;
#1218=CARTESIAN_POINT ( 'NONE',  ( 8.120560827974646401, 20.48090210490235918, 4.740215234001606603 ) ) ;
#1219=CARTESIAN_POINT ( 'NONE',  ( 6.866807723763238336, 12.09672977032890628, 4.952112561794938195 ) ) ;
#1222=CARTESIAN_POINT ( 'NONE',  ( 13.47389875389390390, 21.39272917331400947, 1.812698284662595860 ) ) ;
#1224=CARTESIAN_POINT ( 'NONE',  ( 3.574308380569269694, 17.35305612800781816, -1.439843021498107278 ) ) ;
#1225=CARTESIAN_POINT ( 'NONE',  ( 1.555646991996000983, 13.12134795819716615, 8.453438023037161742 ) ) ;
#1228=CARTESIAN_POINT ( 'NONE',  ( 2.929146897677799011, 12.03771362664550182, 5.053990511100109551 ) ) ;
#1236=CARTESIAN_POINT ( 'NONE',  ( 7.111278525918518056, 14.37945976953069227, -2.629222021087245675 ) ) ;
#1237=CARTESIAN_POINT ( 'NONE',  ( 9.795690773676662744, 20.30269022822975344, -2.134972486994283436 ) ) ;
#1240=CARTESIAN_POINT ( 'NONE',  ( 7.909502645964201051, 21.52839833913197154, 4.227392646788147523 ) ) ;
#1242=CARTESIAN_POINT ( 'NONE',  ( 0.4274521096678008947, 18.57721708583670761, 1.304126942807774192 ) ) ;
#1248=CARTESIAN_POINT ( 'NONE',  ( 6.091961158834851453, 12.63305981940006184, 0.05014679470045566023 ) ) ;
#1250=CARTESIAN_POINT ( 'NONE',  ( 4.364534777017994749, 21.23176840745776062, 5.146678813630421345 ) ) ;
#1253=CARTESIAN_POINT ( 'NONE',  ( 6.502656462190326003, 11.69884544686561156, 2.814585947965546175 ) ) ;
#1262=CARTESIAN_POINT ( 'NONE',  ( 12.08903476211492567, 20.60414639161901107, 4.074121722111526900 ) ) ;
#1269=CARTESIAN_POINT ( 'NONE',  ( 3.855576660607481276, 17.17015518278662611, -0.5977695734878597511 ) ) ;
#1275=CARTESIAN_POINT ( 'NONE',  ( 6.918379510864386184, 20.81512969834162163, 1.623812571277526873 ) ) ;
#1276=CARTESIAN_POINT ( 'NONE',  ( 2.230131626902869701, 18.39186932040918521, 0.5436086090886416144 ) ) ;
#1279=CARTESIAN_POINT ( 'NONE',  ( 5.437298796767638720, 17.41108386104152572, -2.170668680170849463 ) ) ;
#1292=CARTESIAN_POINT ( 'NONE',  ( 7.043391965848642577, 11.65531656196440125, 6.036309832577432033 ) ) ;
#1294=CARTESIAN_POINT ( 'NONE',  ( 3.920931115142209045, 11.91735779063842671, 0.9340496824192962011 ) ) ;
#1303=CARTESIAN_POINT ( 'NONE',  ( 2.509320924895964477, 11.29223014825765148, 3.623872359968939083 ) ) ;
#1313=CARTESIAN_POINT ( 'NONE',  ( 10.73407978594872247, 12.55266643930576187, 5.489046158664341313 ) ) ;
#1316=CARTESIAN_POINT ( 'NONE',  ( 11.16079976075009306, 18.33999801989851264, -4.031859812358146833 ) ) ;
#1320=CARTESIAN_POINT ( 'NONE',  ( 8.614852540573018302, 11.67329553713541301, 3.681175664236859824 ) ) ;
#1321=CARTESIAN_POINT ( 'NONE',  ( 6.979112806929661517, 12.38239436642183655, 5.473019091119168955 ) ) ;
#1326=CARTESIAN_POINT ( 'NONE',  ( 7.248826198693623546, 18.51489551114278953, 8.068672937415568569 ) ) ;
#1327=CARTESIAN_POINT ( 'NONE',  ( 1.693473566456777268, 15.76551524387820358, 9.579563128626743307 ) ) ;
#1330=CARTESIAN_POINT ( 'NONE',  ( 1.185359635733331807, 18.49730447209151762, 8.305304426369882975 ) ) ;
#1337=CARTESIAN_POINT ( 'NONE',  ( 10.22080760973594060, 10.44972119249194087, 2.230886230584283147 ) ) ;
#1338=CARTESIAN_POINT ( 'NONE',  ( 9.252248000141340967, 12.72407294680628809, -2.360866086177806356 ) ) ;
#1341=CARTESIAN_POINT ( 'NONE',  ( 6.443349162879769665, 20.91163864500137137, 0.2251968743725665245 ) ) ;
#1343=CARTESIAN_POINT ( 'NONE',  ( 2.856790208578295687, 12.03350028468612010, 5.076489826180115905 ) ) ;
#1345=CARTESIAN_POINT ( 'NONE',  ( 11.00242668500211707, 11.56703545653052068, 3.822456357127572257 ) ) ;
#1347=CARTESIAN_POINT ( 'NONE',  ( 4.466030190238354791, 11.34862606615942227, 1.934780985301236322 ) ) ;
#1351=CARTESIAN_POINT ( 'NONE',  ( 6.703689575097724784, 11.54993908224053278, 2.743509046784338601 ) ) ;
#1361=CARTESIAN_POINT ( 'NONE',  ( 13.15469369770092989, 14.51428635076888796, 6.086221178321558511 ) ) ;
#1365=CARTESIAN_POINT ( 'NONE',  ( 7.040796410886670742, 14.83344068326428022, 8.020876762884475042 ) ) ;
#1374=CARTESIAN_POINT ( 'NONE',  ( 0.1597621683595935593, 17.17245058820156700, 0.8711918762187601528 ) ) ;
#1376=CARTESIAN_POINT ( 'NONE',  ( 6.453281463188345946, 11.60683490608310109, 3.227001759829918548 ) ) ;
#1380=CARTESIAN_POINT ( 'NONE',  ( 13.24595452700000919, 12.74059347184058133, 6.150563788764593198 ) ) ;
#1387=CARTESIAN_POINT ( 'NONE',  ( 8.066674694811821311, 19.54961979818703099, -0.9699248743207408152 ) ) ;
#1388=CARTESIAN_POINT ( 'NONE',  ( 5.686630817712229558, 12.08264022589296260, -0.3164579326137271775 ) ) ;
#1393=CARTESIAN_POINT ( 'NONE',  ( 1.592392888938656714, 13.91834099111223111, 9.138786557039964009 ) ) ;
#1396=CARTESIAN_POINT ( 'NONE',  ( 4.775750319492399143, 21.07304345130302181, 1.432334575049791781 ) ) ;
#1403=CARTESIAN_POINT ( 'NONE',  ( 2.254736932229037816, 12.49607832033696297, 2.404643631543990967 ) ) ;
#1405=CARTESIAN_POINT ( 'NONE',  ( 9.504781684163363664, 11.74348662527086162, -1.607088501048118845 ) ) ;
#1412=CARTESIAN_POINT ( 'NONE',  ( 2.113164745155809321, 19.10603123094681521, 0.07079837725019544337 ) ) ;
#1422=CARTESIAN_POINT ( 'NONE',  ( 12.86189321301863409, 16.70784808449734982, 6.676389785412363054 ) ) ;
#1429=CARTESIAN_POINT ( 'NONE',  ( 9.146367685053196084, 13.29999752303458749, 6.171800590334175496 ) ) ;
#1437=CARTESIAN_POINT ( 'NONE',  ( 0.02739341652945818245, 12.76637012722054187, 1.557401313085817529 ) ) ;
#1440=CARTESIAN_POINT ( 'NONE',  ( 1.937017454913535719, 20.47856574081302128, 4.897271291058011400 ) ) ;
#1446=CARTESIAN_POINT ( 'NONE',  ( 5.568602949700707683, 12.07884102837326168, -0.2844809541441045697 ) ) ;
#1448=CARTESIAN_POINT ( 'NONE',  ( 9.069221020798989841, 15.12857177743934933, -3.487417871451969464 ) ) ;
#1452=CARTESIAN_POINT ( 'NONE',  ( 9.127199320685813078, 18.85452980171875126, 7.399920140601325080 ) ) ;
#1454=CARTESIAN_POINT ( 'NONE',  ( 0.05507860973824520862, 14.29202264928412092, 1.244272104700797410 ) ) ;
#1457=CARTESIAN_POINT ( 'NONE',  ( 7.008079519739982111, 18.28595648477671887, 7.207522408034829020 ) ) ;
#1461=CARTESIAN_POINT ( 'NONE',  ( 11.77775824504519520, 15.70746112734460986, 7.146079882600543165 ) ) ;
#1462=CARTESIAN_POINT ( 'NONE',  ( 2.596796854730198056, 19.75183458472020348, 0.4273034937204048256 ) ) ;
#1474=CARTESIAN_POINT ( 'NONE',  ( 11.08076314313121991, 13.15907583843444684, 5.707371360959808015 ) ) ;
#1477=CARTESIAN_POINT ( 'NONE',  ( 12.76988556689188137, 18.82436523581427323, 5.780649009981873476 ) ) ;
#1492=CARTESIAN_POINT ( 'NONE',  ( 5.544963268879691043, 15.56575848494070868, -1.416610689648610810 ) ) ;
#1493=CARTESIAN_POINT ( 'NONE',  ( 3.121107721641948274, 20.34465986264832793, 2.720177380617953222 ) ) ;
#1495=CARTESIAN_POINT ( 'NONE',  ( 8.143579141861840398, 10.68807868122940263, 1.737412375843639056 ) ) ;
#1500=CARTESIAN_POINT ( 'NONE',  ( 8.362500416128090919, 20.24457714144503129, -0.2252561178185202018 ) ) ;
#1501=CARTESIAN_POINT ( 'NONE',  ( 12.04632062715783825, 21.69057506433588145, 3.955334450274141211 ) ) ;
#1507=CARTESIAN_POINT ( 'NONE',  ( 3.452510760150116376, 13.11091270743887982, 8.248611567737054173 ) ) ;
#1510=CARTESIAN_POINT ( 'NONE',  ( 7.499653097299838755, 16.51387688058736813, 8.389459965282956233 ) ) ;
#1518=CARTESIAN_POINT ( 'NONE',  ( 2.167641574481099731, 12.74517228915138212, 1.985490079943990516 ) ) ;
#1519=CARTESIAN_POINT ( 'NONE',  ( 10.28844099665304412, 20.83333359141052199, -1.718030307083335595 ) ) ;
#1524=CARTESIAN_POINT ( 'NONE',  ( 2.096007501654802319, 11.92778348172325309, 1.811772831717551213 ) ) ;
#1533=CARTESIAN_POINT ( 'NONE',  ( 12.92240294059410211, 14.85126536588636981, 6.483913497415390914 ) ) ;
#1542=CARTESIAN_POINT ( 'NONE',  ( 8.651812068854638937, 11.71838207857883241, 3.844930327028207806 ) ) ;
#1548=CARTESIAN_POINT ( 'NONE',  ( 0.2490388986165102403, 18.99610975872131391, 0.7649840613554721447 ) ) ;
#1551=CARTESIAN_POINT ( 'NONE',  ( 3.152307289661677725, 19.27890597942106155, 7.411273792436298358 ) ) ;
#1557=CARTESIAN_POINT ( 'NONE',  ( 9.883904741205039812, 20.90551644660764197, -1.655877603440282675 ) ) ;
#1559=CARTESIAN_POINT ( 'NONE',  ( 9.165814705648051230, 13.36932551753513820, -2.800491248554054291 ) ) ;
#1565=CARTESIAN_POINT ( 'NONE',  ( 7.531365603956712285, 21.70037184525196139, 3.190346535578575615 ) ) ;
#1568=CARTESIAN_POINT ( 'NONE',  ( 6.939857573655906720, 18.57054895600834143, 7.059575150324737258 ) ) ;
#1573=CARTESIAN_POINT ( 'NONE',  ( 11.73484804242726298, 13.86399106732309328, 6.608254899136346339 ) ) ;
#1575=CARTESIAN_POINT ( 'NONE',  ( -0.2353009082112856032, 21.11857065418899992, 4.744919637712884608 ) ) ;
#1578=CARTESIAN_POINT ( 'NONE',  ( 2.479339246688891052, 12.01113885212942201, 3.583524443125778891 ) ) ;
#1584=CARTESIAN_POINT ( 'NONE',  ( 10.98060958781924690, 12.63125357519729164, 5.207718750913196359 ) ) ;
#1588=CARTESIAN_POINT ( 'NONE',  ( 12.92686589858350565, 12.55799597913518184, 4.809958993587978959 ) ) ;
#1590=CARTESIAN_POINT ( 'NONE',  ( 6.380166963026771221, 10.92343582149830183, 2.794643371853744007 ) ) ;
#1592=CARTESIAN_POINT ( 'NONE',  ( 1.550976474600018085, 20.56989294761467946, 5.021185002739427361 ) ) ;
#1597=CARTESIAN_POINT ( 'NONE',  ( 6.112021107885185600, 11.58565454437474251, 2.923295850109377536 ) ) ;
#1599=CARTESIAN_POINT ( 'NONE',  ( 11.90896688976436302, 20.94853845629116051, 3.658657855874824172 ) ) ;
#1600=CARTESIAN_POINT ( 'NONE',  ( 12.90481261863918938, 18.46417960692862437, 6.065349631274771447 ) ) ;
#1602=CARTESIAN_POINT ( 'NONE',  ( 8.186312780807948997, 21.32987559984598391, 5.068732912542537328 ) ) ;
#1607=CARTESIAN_POINT ( 'NONE',  ( 9.675305929993816889, 20.98082586346679435, 3.267053697050358085 ) ) ;
#1608=CARTESIAN_POINT ( 'NONE',  ( 10.98487345271878901, 19.57756785145604184, 6.723427973997481821 ) ) ;
#1609=B_SPLINE_CURVE_WITH_KNOTS ( 'NONE', 3,
 ( #21823, #20148, #3475, #10325, #18716, #15209, #18393, #11777, #17073, #10211, #10106, #20257, #15434, #1805, #260, #10003, #18609, #16854, #1695, #16757, #4913, #20472, #5023, #6577, #12104, #20041, #18505, #7002, #16955, #11660, #6677, #1597, #13770, #8552, #5339, #20362, #18830, #15108, #8434, #15328, #3699, #10441, #152 ),
 .UNSPECIFIED., .F., .F.,
 ( 4, 3, 3, 3, 3, 3, 3, 3, 3, 3, 3, 3, 3, 3, 4 ),
 ( 0.000000000000000000, 0.09090909086959420016, 0.1818181817392079958, 0.2500562842553700205, 0.2727272726088130206, 0.3636363634784169907, 0.4545454543480210163, 0.5000905312070750286, 0.5454545452175250109, 0.6363636360871299802, 0.7272727269567340613, 0.7500720420152089396, 0.8181818178263380315, 0.9090909086959420016, 0.9999999995655460827 ),
 .UNSPECIFIED. ) ;
#1615=CARTESIAN_POINT ( 'NONE',  ( 3.704058153803886366, 12.19654146317258103, 0.4088179348593441453 ) ) ;
#1618=CARTESIAN_POINT ( 'NONE',  ( 7.229408460074554732, 18.55040875409351031, 7.925878126512573729 ) ) ;
#1625=CARTESIAN_POINT ( 'NONE',  ( 2.065058272705286413, 12.01021496580790782, 1.672441337454303900 ) ) ;
#1635=CARTESIAN_POINT ( 'NONE',  ( 11.00015320311062439, 17.51254433608867700, 6.806021621348003592 ) ) ;
#1642=CARTESIAN_POINT ( 'NONE',  ( 8.545873062880019688, 11.61005284472577159, 3.376861938372578198 ) ) ;
#1643=CARTESIAN_POINT ( 'NONE',  ( 3.430718016658220293, 15.33128678211075702, 8.333009793459709158 ) ) ;
#1647=CARTESIAN_POINT ( 'NONE',  ( -0.1672139265598213131, 16.21125157041092635, 0.03678197978728087181 ) ) ;
#1651=CARTESIAN_POINT ( 'NONE',  ( 1.377977696595360291, 12.31440956997844083, 6.220707012221055265 ) ) ;
#1658=CARTESIAN_POINT ( 'NONE',  ( 7.867384389574832326, 10.77439257666578243, 1.834364527281745483 ) ) ;
#1661=CARTESIAN_POINT ( 'NONE',  ( 11.68885165013066185, 21.89103689682439224, 3.044870294398752453 ) ) ;
#1663=CARTESIAN_POINT ( 'NONE',  ( 8.590151053309458717, 10.83020630611641266, 3.529432304467389425 ) ) ;
#1664=CARTESIAN_POINT ( 'NONE',  ( 3.480677399789653848, 14.96908372069038684, 8.311097829955567562 ) ) ;
#1669=CARTESIAN_POINT ( 'NONE',  ( 8.600866579439452764, 11.08822532131044092, 1.666493167020851818 ) ) ;
#1671=CARTESIAN_POINT ( 'NONE',  ( 2.903384396171142967, 20.92902966678202148, 1.811677702956517866 ) ) ;
#1674=CARTESIAN_POINT ( 'NONE',  ( -0.01591978660616180652, 15.70515029433102860, 0.7746393958769953736 ) ) ;
#1682=CARTESIAN_POINT ( 'NONE',  ( 10.20773825118543421, 21.26060903501195298, 4.752181056839726025 ) ) ;
#1685=CARTESIAN_POINT ( 'NONE',  ( 12.74520702676420392, 11.91691794096125534, 3.970093380836815289 ) ) ;
#1688=CARTESIAN_POINT ( 'NONE',  ( 6.007628987977455814, 11.57021355890683978, 2.543656572248523595 ) ) ;
#1693=CARTESIAN_POINT ( 'NONE',  ( 3.738535879684092400, 15.59511426254074173, -0.5956637481122312172 ) ) ;
#1695=CARTESIAN_POINT ( 'NONE',  ( 6.010820999879410209, 11.26290339936039153, 2.930039796312023270 ) ) ;
#1699=CARTESIAN_POINT ( 'NONE',  ( 5.792450260185113109, 12.69966494906990206, 0.1988901986138334466 ) ) ;
#1700=CARTESIAN_POINT ( 'NONE',  ( 4.007488201923330884, 20.44159178862518189, 5.038468532300615088 ) ) ;
#1702=CARTESIAN_POINT ( 'NONE',  ( 8.546142373387299429, 20.63131727706956298, 0.1902865990017700848 ) ) ;
#1703=CARTESIAN_POINT ( 'NONE',  ( 2.000976789916291132, 15.60105019847626551, 9.484685655146686045 ) ) ;
#1705=CARTESIAN_POINT ( 'NONE',  ( 11.53313857698689837, 20.24893436370382105, -3.119838056082069766 ) ) ;
#1710=CARTESIAN_POINT ( 'NONE',  ( 9.829229519957147332, 20.86878119585347235, 3.677952529984052532 ) ) ;
#1711=CARTESIAN_POINT ( 'NONE',  ( 9.396859391623667790, 12.85930032217342145, 6.944093101771448673 ) ) ;
#1718=CARTESIAN_POINT ( 'NONE',  ( 10.98588874387031211, 13.67752812875329838, -3.721421232128317769 ) ) ;
#1719=CARTESIAN_POINT ( 'NONE',  ( 5.043785943435923791, 12.41500460647656112, 7.215820400045201310 ) ) ;
#1722=CARTESIAN_POINT ( 'NONE',  ( 5.768991567460251879, 21.49153886321743201, 4.134389838676610474 ) ) ;
#1733=CARTESIAN_POINT ( 'NONE',  ( 2.827832784706104441, 20.82732273834332304, 1.888333759270794499 ) ) ;
#1744=CARTESIAN_POINT ( 'NONE',  ( 7.472981172757774182, 13.15088303497838140, -1.026857982812649395 ) ) ;
#1745=CARTESIAN_POINT ( 'NONE',  ( 3.287836056772957427, 11.90013693509636106, 6.878074374375073852 ) ) ;
#1750=CARTESIAN_POINT ( 'NONE',  ( 9.154392979045368861, 13.35535808052676110, 6.215094776725202053 ) ) ;
#1755=CARTESIAN_POINT ( 'NONE',  ( 0.3034835435385529467, 19.20128088117248311, 0.8914707698310011530 ) ) ;
#1758=CARTESIAN_POINT ( 'NONE',  ( 5.344873306944882607, 17.31775664876643006, 7.991828959977699043 ) ) ;
#1763=CARTESIAN_POINT ( 'NONE',  ( 8.327167164761551277, 10.82907781979698214, 3.764246136999646275 ) ) ;
#1765=CARTESIAN_POINT ( 'NONE',  ( 13.08108576808625045, 18.67096353113900520, 6.700927112183967971 ) ) ;
#1769=CARTESIAN_POINT ( 'NONE',  ( 9.343037286256407725, 12.92999292743880702, 6.861527116923473280 ) ) ;
#1770=CARTESIAN_POINT ( 'NONE',  ( 1.122858828880666460, 18.50002798056422293, 8.328379096489866740 ) ) ;
#1775=CARTESIAN_POINT ( 'NONE',  ( 1.852730722019251930, 20.39130814012998982, 4.938901323796075715 ) ) ;
#1778=CARTESIAN_POINT ( 'NONE',  ( 9.570742583039159257, 15.35048014666334559, -3.380060443643036816 ) ) ;
#1781=CARTESIAN_POINT ( 'NONE',  ( 3.570643486829286228, 15.44796252803982206, -1.483651343954088597 ) ) ;
#1784=CARTESIAN_POINT ( 'NONE',  ( 5.344534969970771598, 14.21717427261922673, 7.627733794437622450 ) ) ;
#1792=CARTESIAN_POINT ( 'NONE',  ( 11.10692670746270316, 13.33981709075777644, 5.846286987766022847 ) ) ;
#1794=CARTESIAN_POINT ( 'NONE',  ( 10.44282649712041433, 20.84799543583206116, 5.382918864209185195 ) ) ;
#1797=CARTESIAN_POINT ( 'NONE',  ( 13.07577240337103319, 13.46997794477539578, 5.567646671893168531 ) ) ;
#1799=CARTESIAN_POINT ( 'NONE',  ( 1.650854728546951256, 13.47654819534602133, 1.014815903823355736 ) ) ;
#1805=CARTESIAN_POINT ( 'NONE',  ( 6.072633846711956274, 11.08857437794745060, 2.898804142493843106 ) ) ;
#1810=CARTESIAN_POINT ( 'NONE',  ( 7.518022070815600699, 21.00575954651474220, 3.199318596789233027 ) ) ;
#1812=CARTESIAN_POINT ( 'NONE',  ( 9.745609355272696561, 21.05303134726939973, 3.406578442638684034 ) ) ;
#1813=CARTESIAN_POINT ( 'NONE',  ( 5.930740481208400361, 15.68947463651248420, 8.349508172414736862 ) ) ;
#1814=CARTESIAN_POINT ( 'NONE',  ( 6.883721427746540833, 11.28756208157694019, 5.058899341199012412 ) ) ;
#1820=CARTESIAN_POINT ( 'NONE',  ( 10.62526409008942530, 19.44399953203486930, 5.732770084512769593 ) ) ;
#1821=CARTESIAN_POINT ( 'NONE',  ( 8.188127480685322368, 10.68876677029517985, 1.724185228589610430 ) ) ;
#1829=CARTESIAN_POINT ( 'NONE',  ( 4.288727190992245752, 11.05839472165502180, 3.905392380839078914 ) ) ;
#1832=CARTESIAN_POINT ( 'NONE',  ( 7.411476586714386805, 17.43287269264193995, 8.287351011025366532 ) ) ;
#1841=CARTESIAN_POINT ( 'NONE',  ( 1.904339175427839370, 14.42031344806993509, 0.5205678229890007280 ) ) ;
#1845=CARTESIAN_POINT ( 'NONE',  ( 1.804151634728472509, 13.13951335195213233, 0.4288176399958442686 ) ) ;
#1857=CARTESIAN_POINT ( 'NONE',  ( 9.094193234406278137, 13.35316387417510242, 6.359510078786708931 ) ) ;
#1858=CARTESIAN_POINT ( 'NONE',  ( 6.019117752002316912, 11.27437957348430153, 1.137765012461108727 ) ) ;
#1866=CARTESIAN_POINT ( 'NONE',  ( 7.485261295460871267, 16.46636833195797323, -2.127643011693920894 ) ) ;
#1870=CARTESIAN_POINT ( 'NONE',  ( -0.08963606460140813303, 17.11798323789379239, 0.09094961474301116455 ) ) ;
#1872=CARTESIAN_POINT ( 'NONE',  ( 2.799714621286362171, 11.92572550326888070, 3.472117233931273805 ) ) ;
#1877=CARTESIAN_POINT ( 'NONE',  ( 8.904586033696963554, 18.52979832374122182, 7.665090501505551934 ) ) ;
#1880=CARTESIAN_POINT ( 'NONE',  ( 12.56049810209382578, 20.55707369507660687, 5.409390963554637111 ) ) ;
#1885=CARTESIAN_POINT ( 'NONE',  ( 8.906453209518582881, 11.27159611284453078, 4.875366572814009203 ) ) ;
#1886=CARTESIAN_POINT ( 'NONE',  ( 5.411841742863021665, 15.73786965665290793, 8.085039117809539988 ) ) ;
#1888=CARTESIAN_POINT ( 'NONE',  ( 6.124911956022416781, 11.96954057703546148, 1.636852048146504313 ) ) ;
#1892=CARTESIAN_POINT ( 'NONE',  ( 7.966291526427072611, 18.22263143684711650, -2.425212026461652126 ) ) ;
#1894=CARTESIAN_POINT ( 'NONE',  ( 2.456256303170528899, 20.82653447492750232, 6.630392102736424320 ) ) ;
#1897=CARTESIAN_POINT ( 'NONE',  ( 1.044675250455524562, 12.39565097329668042, 6.288947036086600662 ) ) ;
#1902=CARTESIAN_POINT ( 'NONE',  ( 11.29248933744070094, 17.61190850482638126, 7.438500274146146118 ) ) ;
#1906=CARTESIAN_POINT ( 'NONE',  ( 11.37084557258393680, 12.66814131563982748, -2.073203632157150977 ) ) ;
#1909=CARTESIAN_POINT ( 'NONE',  ( 5.901153730144788057, 20.52421269917602231, 5.344389719742077105 ) ) ;
#1918=CARTESIAN_POINT ( 'NONE',  ( 8.565727124014848926, 11.53726303284714128, 3.541620658823112944 ) ) ;
#1919=CARTESIAN_POINT ( 'NONE',  ( 3.468174865916350047, 20.55352757937665231, 3.625693982640088020 ) ) ;
#1920=CARTESIAN_POINT ( 'NONE',  ( 13.94037765912086968, 20.92783617524978013, 3.342340119663654630 ) ) ;
#1921=CARTESIAN_POINT ( 'NONE',  ( -0.4116026285172821320, 20.72700438578640458, 3.664095157482434306 ) ) ;
#1922=CARTESIAN_POINT ( 'NONE',  ( 10.89765286091802210, 14.15736234249478720, -4.058299758797063284 ) ) ;
#1929=CARTESIAN_POINT ( 'NONE',  ( 11.19880827645247479, 14.32817945148129191, 6.410845832078652329 ) ) ;
#1930=CARTESIAN_POINT ( 'NONE',  ( 7.454783155005726414, 18.37230293632699230, -2.665002534372324039 ) ) ;
#1936=CARTESIAN_POINT ( 'NONE',  ( 6.183449657823808288, 10.85153064243760213, 2.375645654555686104 ) ) ;
#1939=CARTESIAN_POINT ( 'NONE',  ( 7.545109171398233450, 14.90330900736333142, 8.204851733050276152 ) ) ;
#1943=CARTESIAN_POINT ( 'NONE',  ( 1.885017549903653888, 14.91461614480940945, 0.3181462793239871467 ) ) ;
#1945=CARTESIAN_POINT ( 'NONE',  ( 3.766360634439569033, 14.28061422378609002, -0.1577300086709537419 ) ) ;
#1950=CARTESIAN_POINT ( 'NONE',  ( 4.620631840053190942, 20.50352216405097749, 6.712139773280671129 ) ) ;
#1963=CARTESIAN_POINT ( 'NONE',  ( 9.285644904300696112, 17.21895884409014599, -2.864567016515628062 ) ) ;
#1964=CARTESIAN_POINT ( 'NONE',  ( 3.701753992781950053, 14.72343274211524644, 9.049335738697640963 ) ) ;
#1967=CARTESIAN_POINT ( 'NONE',  ( 5.516318909232666101, 16.92504161144799468, 8.771371271385028479 ) ) ;
#1971=CARTESIAN_POINT ( 'NONE',  ( 7.521333489489228086, 16.89536166212861090, -2.106288691737336016 ) ) ;
#1974=CARTESIAN_POINT ( 'NONE',  ( 3.426769813837023282, 14.84877425439436571, 8.187781101960947439 ) ) ;
#1978=CARTESIAN_POINT ( 'NONE',  ( 3.190248314799053464, 19.04062286170201546, 8.431111234986099490 ) ) ;
#1982=CARTESIAN_POINT ( 'NONE',  ( 3.721838304568709344, 16.48662853297856401, 8.524029460627765786 ) ) ;
#1987=CARTESIAN_POINT ( 'NONE',  ( 5.982655683593218754, 20.62467454825192092, -0.1193919904210567484 ) ) ;
#1989=CARTESIAN_POINT ( 'NONE',  ( 11.95762566148904327, 21.63633082368178151, 3.785239628339895912 ) ) ;
#1993=CARTESIAN_POINT ( 'NONE',  ( 9.441105179033391082, 16.62352861847284657, 7.978075225639419621 ) ) ;
#1994=CARTESIAN_POINT ( 'NONE',  ( 1.524583137339517780, 15.70105570582070520, 8.880780227086491507 ) ) ;
#1995=CARTESIAN_POINT ( 'NONE',  ( 6.138121642458962413, 19.25141403178904298, -0.4363714260734747330 ) ) ;
#1996=CARTESIAN_POINT ( 'NONE',  ( 7.048998319408883440, 18.08802919812652021, 7.290918307196334602 ) ) ;
#1999=CARTESIAN_POINT ( 'NONE',  ( 7.539145179894531701, 16.37851731477712391, -3.008003415082166399 ) ) ;
#2000=CARTESIAN_POINT ( 'NONE',  ( -0.7351689855894368852, 20.80871142581116118, 3.732510512736133546 ) ) ;
#2001=CARTESIAN_POINT ( 'NONE',  ( 0.6418754216142991131, 20.43628740585238646, 7.348520308371068843 ) ) ;
#2004=CARTESIAN_POINT ( 'NONE',  ( 1.450916895402551532, 14.30666394527731633, 8.434575071336105623 ) ) ;
#2009=CARTESIAN_POINT ( 'NONE',  ( 11.39633395548191785, 16.56875889582252270, 7.579279425343053767 ) ) ;
#2011=CARTESIAN_POINT ( 'NONE',  ( 11.36068676796085875, 17.98270986927288106, -3.346212262616973021 ) ) ;
#2013=CARTESIAN_POINT ( 'NONE',  ( 3.722424747480308493, 20.61711312421807918, 5.170631176151997188 ) ) ;
#2017=CARTESIAN_POINT ( 'NONE',  ( 4.241210656867956175, 19.03653144147999754, 0.1777686537783049470 ) ) ;
#2021=CARTESIAN_POINT ( 'NONE',  ( 11.10449564925248467, 12.61980174807018251, 5.312955716968204456 ) ) ;
#2022=CARTESIAN_POINT ( 'NONE',  ( 9.316180898295447932, 14.88029421051436429, 7.101556370160515996 ) ) ;
#2023=CARTESIAN_POINT ( 'NONE',  ( 7.188422006453914825, 19.80783775455006435, 6.631232769852104525 ) ) ;
#2024=CARTESIAN_POINT ( 'NONE',  ( 10.75667203142358019, 10.89927089225536250, 4.183043474010283980 ) ) ;
#2031=CARTESIAN_POINT ( 'NONE',  ( 11.51558075932182845, 10.98646219477360297, -1.335441368411448115 ) ) ;
#2033=CARTESIAN_POINT ( 'NONE',  ( 9.643416883055870414, 12.23232111864449756, -0.7319516263326404371 ) ) ;
#2035=CARTESIAN_POINT ( 'NONE',  ( 13.30756833192837973, 22.19916104524133971, 1.697755270691982732 ) ) ;
#2036=CARTESIAN_POINT ( 'NONE',  ( 1.396283581706163179, 16.44430802189885199, -0.6243410038125684069 ) ) ;
#2039=CARTESIAN_POINT ( 'NONE',  ( 7.397026236728797777, 12.98560518583070156, 7.265883842775997081 ) ) ;
#2044=CARTESIAN_POINT ( 'NONE',  ( 0.04798837220721437896, 15.99000724392452355, 0.8174092256989702321 ) ) ;
#2048=CARTESIAN_POINT ( 'NONE',  ( 3.931607425614295881, 13.02331082334462664, 0.7891442226006756266 ) ) ;
#2054=CARTESIAN_POINT ( 'NONE',  ( 5.075214630907313840, 19.34300442968084965, 7.864654554335390735 ) ) ;
#2065=CARTESIAN_POINT ( 'NONE',  ( 11.63657489771697762, 19.71324643990528358, -2.510315654606890767 ) ) ;
#2066=CARTESIAN_POINT ( 'NONE',  ( 1.666480301802111708, 14.62668795976242642, -0.5087735202898915343 ) ) ;
#2069=CARTESIAN_POINT ( 'NONE',  ( 4.428162769058000769, 11.10825873668719233, 3.140058628108473027 ) ) ;
#2074=CARTESIAN_POINT ( 'NONE',  ( 7.974225380408622499, 19.27095890255583654, -1.194036445722556294 ) ) ;
#2086=CARTESIAN_POINT ( 'NONE',  ( 2.034095840400902411, 21.12497993269252206, 5.441157602331140097 ) ) ;
#2093=CARTESIAN_POINT ( 'NONE',  ( 11.71175349776414798, 21.61111399576532222, 4.019351335416992299 ) ) ;
#2095=CARTESIAN_POINT ( 'NONE',  ( 11.07300705963626086, 22.03001829576734139, 1.335942992242750815 ) ) ;
#2098=CARTESIAN_POINT ( 'NONE',  ( 13.19949732976186674, 21.42485117465795241, 1.390320667582642278 ) ) ;
#2099=CARTESIAN_POINT ( 'NONE',  ( 9.353409075422060681, 13.00170194491951747, 6.914035789133324172 ) ) ;
#2100=CARTESIAN_POINT ( 'NONE',  ( 3.774570344757517404, 14.05232170482083198, -0.1440267703289939694 ) ) ;
#2105=CARTESIAN_POINT ( 'NONE',  ( 5.828491125658624483, 12.77629345597859611, 0.2544156256959317353 ) ) ;
#2106=CARTESIAN_POINT ( 'NONE',  ( 7.278394972475737745, 16.40995809457478316, 7.634184181800698354 ) ) ;
#2111=CARTESIAN_POINT ( 'NONE',  ( 12.05982911834764160, 19.98250042233096124, -2.959000471914774888 ) ) ;
#2114=CARTESIAN_POINT ( 'NONE',  ( 6.375721097596529496, 21.18628736811522373, 5.516090907968282053 ) ) ;
#2115=CARTESIAN_POINT ( 'NONE',  ( -0.02957876527916961790, 21.01733645358232039, 5.567338713754919510 ) ) ;
#2118=CARTESIAN_POINT ( 'NONE',  ( 3.381061492508358413, 16.48226916726223479, 8.534974189403024880 ) ) ;
#2123=SURFACE_STYLE_FILL_AREA ( #17054 ) ;
#2124=CARTESIAN_POINT ( 'NONE',  ( 10.91865587142655158, 19.54907707356796109, 6.609524152570670275 ) ) ;
#2126=CARTESIAN_POINT ( 'NONE',  ( 11.15127959100651722, 15.67546746552279302, -3.541987318106106120 ) ) ;
#2132=CARTESIAN_POINT ( 'NONE',  ( 4.996268568956748091, 20.49501342957312744, 2.074042226353195684 ) ) ;
#2138=CARTESIAN_POINT ( 'NONE',  ( 9.274993866748067362, 13.35316387417510242, 6.305366573914296779 ) ) ;
#2140=CARTESIAN_POINT ( 'NONE',  ( 7.475049925495288683, 16.36412484890493957, -2.235126692085353639 ) ) ;
#2141=CARTESIAN_POINT ( 'NONE',  ( 0.5343612684300755866, 18.97471059823722328, 0.6418818272746593667 ) ) ;
#2148=CARTESIAN_POINT ( 'NONE',  ( 6.283322441762637212, 20.69450185495974281, -0.2642756491526417895 ) ) ;
#2149=MECHANICAL_DESIGN_GEOMETRIC_PRESENTATION_REPRESENTATION('',(#11690),#18747);
#2152=CARTESIAN_POINT ( 'NONE',  ( 9.291847323842565842, 15.23045113553444097, -2.731355305102841413 ) ) ;
#2155=CARTESIAN_POINT ( 'NONE',  ( 0.9545976637875654980, 21.03017768341116067, 3.424241316347047981 ) ) ;
#2158=CARTESIAN_POINT ( 'NONE',  ( 7.541834703702306797, 14.74947482163050161, 8.160879108828842377 ) ) ;
#2185=CARTESIAN_POINT ( 'NONE',  ( 12.78095741915561945, 21.47881914407666315, 0.5220334371899034709 ) ) ;
#2187=CARTESIAN_POINT ( 'NONE',  ( 5.179235369666963074, 19.21458830873230283, 8.065034840720384679 ) ) ;
#2190=CARTESIAN_POINT ( 'NONE',  ( 5.543297571818101233, 13.82534514388550129, 8.177650472684211636 ) ) ;
#2196=CARTESIAN_POINT ( 'NONE',  ( 7.609271008339460352, 13.06901655821814145, -0.8557159515761880719 ) ) ;
#2203=CARTESIAN_POINT ( 'NONE',  ( 0.7633619320212706727, 20.37518500713720471, 2.043613188576509199 ) ) ;
#2205=CARTESIAN_POINT ( 'NONE',  ( 3.936278269025204501, 16.50247895544803711, 8.791069023109434610 ) ) ;
#2207=CARTESIAN_POINT ( 'NONE',  ( 13.24246334734214336, 22.12989337480687269, 1.990192772094774076 ) ) ;
#2213=CARTESIAN_POINT ( 'NONE',  ( 7.516414041016176384, 19.83100852729402064, -1.255802337575999905 ) ) ;
#2215=CARTESIAN_POINT ( 'NONE',  ( 12.12180015326468485, 10.40596899240396311, 1.263324329328538109 ) ) ;
#2220=CARTESIAN_POINT ( 'NONE',  ( 8.113089735847959005, 10.84140768076111172, 1.524413057128902294 ) ) ;
#2222=CARTESIAN_POINT ( 'NONE',  ( 5.651855977748085458, 20.83490078207852392, 3.725216732626875693 ) ) ;
#2224=ADVANCED_FACE ( 'NONE', ( #6153 ), #15861, .T. ) ;
#2225=CARTESIAN_POINT ( 'NONE',  ( 5.917177850220659785, 12.44752302178212133, 0.6815623641613539618 ) ) ;
#2229=CARTESIAN_POINT ( 'NONE',  ( 10.07533004185552272, 21.75488213915048163, 3.488364678943705943 ) ) ;
#2231=CARTESIAN_POINT ( 'NONE',  ( 1.840183766054111159, 21.28931287393832150, 5.000021689193579810 ) ) ;
#2232=CARTESIAN_POINT ( 'NONE',  ( 0.8789596239274352074, 19.99575406279286582, 7.958759135206050495 ) ) ;
#2234=AXIS2_PLACEMENT_3D ( 'NONE', #14022, #2275, #17644 ) ;
#2235=CARTESIAN_POINT ( 'NONE',  ( 6.650780717571844747, 11.71035962591412272, 4.098950421500386909 ) ) ;
#2241=CARTESIAN_POINT ( 'NONE',  ( 6.396056618077795797, 11.71523274630726164, 2.847703469759983008 ) ) ;
#2242=CARTESIAN_POINT ( 'NONE',  ( 10.84114159136082556, 11.15340055693774346, 4.434419607208564429 ) ) ;
#2246=CARTESIAN_POINT ( 'NONE',  ( 11.17813456493683688, 16.31200234120390391, -3.589686200531655658 ) ) ;
#2255=CARTESIAN_POINT ( 'NONE',  ( 12.23442992331478330, 20.89186537925146325, -1.172561438593525462 ) ) ;
#2256=CARTESIAN_POINT ( 'NONE',  ( 4.218669509945208951, 20.25152453169299349, 5.586594807314953393 ) ) ;
#2258=CARTESIAN_POINT ( 'NONE',  ( 5.589282794631477813, 15.56565457311297251, -1.430601909125969406 ) ) ;
#2265=CARTESIAN_POINT ( 'NONE',  ( 6.056291209943008624, 11.11068921130002174, 1.344815542909726380 ) ) ;
#2269=CARTESIAN_POINT ( 'NONE',  ( 9.524025606199806759, 12.69250285052379645, -1.295200290336259608 ) ) ;
#2272=CARTESIAN_POINT ( 'NONE',  ( 0.7719978298209800860, 18.72099911278871787, 8.787022842826415214 ) ) ;
#2275=DIRECTION ( 'NONE',  ( 0.000000000000000000, 0.000000000000000000, 1.000000000000000000 ) ) ;
#2283=CARTESIAN_POINT ( 'NONE',  ( 2.092738645373398043, 17.72593790894276822, 0.2727642672195841334 ) ) ;
#2285=CARTESIAN_POINT ( 'NONE',  ( 9.124037948774077478, 15.28165795756530265, -3.667571731158457471 ) ) ;
#2297=CARTESIAN_POINT ( 'NONE',  ( 3.021518493146395201, 19.78048590522542227, 7.993777974749627369 ) ) ;
#2299=CARTESIAN_POINT ( 'NONE',  ( 5.205980611946986691, 11.94362822924763634, 6.505740943259474385 ) ) ;
#2304=CARTESIAN_POINT ( 'NONE',  ( 1.345719439226387371, 13.41272998646361714, 7.668264603079712138 ) ) ;
#2311=CARTESIAN_POINT ( 'NONE',  ( 3.025083360574306379, 19.58333031856296103, 8.033243523162543198 ) ) ;
#2315=CARTESIAN_POINT ( 'NONE',  ( 4.226748096773134122, 12.75273057655540043, 0.7412141520461309474 ) ) ;
#2317=CARTESIAN_POINT ( 'NONE',  ( 13.37542130762736647, 22.16307796594318802, 1.955246718568947273 ) ) ;
#2323=CARTESIAN_POINT ( 'NONE',  ( 8.698080803895434698, 18.39925938975357056, 7.424547285105621341 ) ) ;
#2326=CARTESIAN_POINT ( 'NONE',  ( 12.02571325582669282, 10.42810541502117161, 0.8657527866613862200 ) ) ;
#2330=CARTESIAN_POINT ( 'NONE',  ( 7.711757841094235566, 11.51867810285771121, -0.1922238782181159011 ) ) ;
#2333=CARTESIAN_POINT ( 'NONE',  ( 5.786084785701969935, 17.74437171614160391, -1.199539018687937331 ) ) ;
#2334=CARTESIAN_POINT ( 'NONE',  ( 7.130351268715567237, 12.94937010301612723, 6.204865410933570580 ) ) ;
#2337=CARTESIAN_POINT ( 'NONE',  ( 6.344892231242216241, 11.19290776549860134, 1.289291468351646763 ) ) ;
#2338=CARTESIAN_POINT ( 'NONE',  ( 4.898461982228181633, 12.16261474950084498, 5.232768426419909247 ) ) ;
#2341=CARTESIAN_POINT ( 'NONE',  ( 6.266996954026719635, 21.18238311700324417, 5.546799428808435017 ) ) ;
#2342=CARTESIAN_POINT ( 'NONE',  ( 1.266019147034259884, 18.88490084365312782, 8.903593704730354830 ) ) ;
#2347=CARTESIAN_POINT ( 'NONE',  ( 1.828908678823709666, 20.48283743933590273, 4.930034699729209713 ) ) ;
#2352=CARTESIAN_POINT ( 'NONE',  ( 9.688677822838410947, 11.12736925383730124, -0.4069968778330486092 ) ) ;
#2355=CARTESIAN_POINT ( 'NONE',  ( 11.47251706867474041, 12.23848474711970802, -1.592967478809933723 ) ) ;
#2356=CARTESIAN_POINT ( 'NONE',  ( 5.656534285913039639, 12.27047075047317115, -0.3509529794051957086 ) ) ;
#2358=CARTESIAN_POINT ( 'NONE',  ( 0.3202639567549845911, 18.57485916386803382, 1.339964575302207805 ) ) ;
#2362=CARTESIAN_POINT ( 'NONE',  ( 6.060393788137320215, 20.48930581516298233, 4.878321978022181149 ) ) ;
#2368=CARTESIAN_POINT ( 'NONE',  ( 6.496396028925151889, 20.04364414270774120, 0.1831189632268445389 ) ) ;
#2369=CARTESIAN_POINT ( 'NONE',  ( 7.588986978588807553, 13.14768317755540039, -1.065587204641165409 ) ) ;
#2371=CARTESIAN_POINT ( 'NONE',  ( 12.81298227213678942, 22.28511555871962102, 0.3971908496776146991 ) ) ;
#2378=CARTESIAN_POINT ( 'NONE',  ( 11.16649006228652041, 16.55586016349425194, 6.818406148130505606 ) ) ;
#2379=CARTESIAN_POINT ( 'NONE',  ( 6.794028650656957602, 11.05210752777782091, 4.465890901017215420 ) ) ;
#2382=CARTESIAN_POINT ( 'NONE',  ( 9.926485704785847020, 11.59865289762421270, 0.5377904742533208271 ) ) ;
#2384=CARTESIAN_POINT ( 'NONE',  ( 0.02376778487644688048, 20.19881069607145108, 5.688190597157388950 ) ) ;
#2385=CARTESIAN_POINT ( 'NONE',  ( 0.9792782680767874171, 12.85015660565266060, 7.901049221702420411 ) ) ;
#2388=CARTESIAN_POINT ( 'NONE',  ( 7.520682447844541763, 16.20627867842422631, 8.395911810959326260 ) ) ;
#2394=CARTESIAN_POINT ( 'NONE',  ( 0.02905096893341448799, 15.40301703741441663, 0.9139028180173993654 ) ) ;
#2401=CARTESIAN_POINT ( 'NONE',  ( 12.56778430086266063, 10.42448595387692301, 2.703119026783505685 ) ) ;
#2411=CARTESIAN_POINT ( 'NONE',  ( 1.699527425015976645, 13.92038700339129242, 9.102769882603862328 ) ) ;
#2414=CARTESIAN_POINT ( 'NONE',  ( 5.247544535690431111, 12.08598944411757792, 6.695756513832588297 ) ) ;
#2417=CARTESIAN_POINT ( 'NONE',  ( 1.327405647319859439, 13.31436210545662213, 7.568774271523563080 ) ) ;
#2420=CARTESIAN_POINT ( 'NONE',  ( 3.296278299113588606, 13.37815361419331062, 7.298396853533315465 ) ) ;
#2425=PRODUCT_DEFINITION_SHAPE ( 'NONE', 'NONE',  #3715 ) ;
#2427=CARTESIAN_POINT ( 'NONE',  ( 1.164373365471405464, 20.93742321894627167, 3.100345057572924556 ) ) ;
#2430=CARTESIAN_POINT ( 'NONE',  ( 6.264679519144333852, 12.20187417505221994, 0.8393449708032283407 ) ) ;
#2436=CARTESIAN_POINT ( 'NONE',  ( 8.937652522793825938, 16.60610825764645071, 7.830010146707459207 ) ) ;
#2439=CARTESIAN_POINT ( 'NONE',  ( 12.46883308523603695, 10.55182128074574166, 2.701636765429729969 ) ) ;
#2444=CARTESIAN_POINT ( 'NONE',  ( 7.810601781778314212, 11.28094437888862167, 0.2371453506886788687 ) ) ;
#2445=CARTESIAN_POINT ( 'NONE',  ( 2.224701653548029512, 12.53189561649392125, 2.144358178734434350 ) ) ;
#2447=CARTESIAN_POINT ( 'NONE',  ( 8.802231832380332577, 18.96461393410900342, 6.449481405740358220 ) ) ;
#2448=CARTESIAN_POINT ( 'NONE',  ( 7.323594443806002552, 14.97599272452439934, 7.432113103085323580 ) ) ;
#2449=EDGE_CURVE ( 'NONE', #1010, #10254, #2856, .T. ) ;
#2453=CARTESIAN_POINT ( 'NONE',  ( 5.655654580052440039, 15.45793682862229801, -2.195876644601166383 ) ) ;
#2454=CARTESIAN_POINT ( 'NONE',  ( 0.9710684863527534461, 19.78858245918292980, 8.191681233637670090 ) ) ;
#2457=CARTESIAN_POINT ( 'NONE',  ( 1.479868076741676086, 15.70115217790233508, 8.893450642701147046 ) ) ;
#2464=CARTESIAN_POINT ( 'NONE',  ( 10.32679327456467711, 10.57999906717443217, 2.270008812520685204 ) ) ;
#2468=CARTESIAN_POINT ( 'NONE',  ( 5.951137870369475280, 11.39017030426189159, 0.9629264744454320013 ) ) ;
#2477=CARTESIAN_POINT ( 'NONE',  ( 8.288275297767960126, 11.49260726995666104, 1.826824681916124016 ) ) ;
#2480=CARTESIAN_POINT ( 'NONE',  ( 11.17045701329781870, 16.27078922038444375, -3.703851085504920704 ) ) ;
#2482=CARTESIAN_POINT ( 'NONE',  ( 5.232332039340263030, 18.73163945740397196, 8.232832001541300571 ) ) ;
#2486=CARTESIAN_POINT ( 'NONE',  ( 13.00775088886534014, 18.81300736124048001, 6.802859426759906292 ) ) ;
#2490=CARTESIAN_POINT ( 'NONE',  ( 9.718623483178818745, 12.00923416725010107, -0.3876423491285933554 ) ) ;
#2492=CARTESIAN_POINT ( 'NONE',  ( 1.218747862079375022, 17.86133278564378557, 8.560453536580162393 ) ) ;
#2493=CARTESIAN_POINT ( 'NONE',  ( 3.023071641832506984, 21.04679274153226132, 3.678863645485955569 ) ) ;
#2505=CARTESIAN_POINT ( 'NONE',  ( 1.899735969233180333, 16.00403838164227110, 0.07924708280844300345 ) ) ;
#2506=CARTESIAN_POINT ( 'NONE',  ( 13.51152013350133352, 14.65422691944639766, 7.038129281359358558 ) ) ;
#2521=CARTESIAN_POINT ( 'NONE',  ( 4.604894575570973814, 10.97102203747262195, 3.812269742438572973 ) ) ;
#2525=CARTESIAN_POINT ( 'NONE',  ( 3.513538848007559778, 15.00484000090286152, -1.245897553462994800 ) ) ;
#2536=CARTESIAN_POINT ( 'NONE',  ( 3.227538363289882195, 11.94188570999173571, 6.753139928253237834 ) ) ;
#2538=CARTESIAN_POINT ( 'NONE',  ( 4.527065879313684427, 11.94740837896324237, 2.138596589892054034 ) ) ;
#2545=CARTESIAN_POINT ( 'NONE',  ( 10.84552853021218688, 12.37556557019096282, -2.818576892710451531 ) ) ;
#2548=CARTESIAN_POINT ( 'NONE',  ( 12.48372930177676920, 10.56671872245006050, 2.763668074036412570 ) ) ;
#2551=ORIENTED_EDGE ( 'NONE', *, *, #6778, .F. ) ;
#2554=CARTESIAN_POINT ( 'NONE',  ( 7.604625018144008486, 19.02913910763591687, -2.252239620500007256 ) ) ;
#2555=CARTESIAN_POINT ( 'NONE',  ( 4.609813405446039347, 11.78043576488526156, 3.796358869022819604 ) ) ;
#2557=CARTESIAN_POINT ( 'NONE',  ( 6.993363486292583531, 20.75028404412490701, 1.749401355466371433 ) ) ;
#2561=CARTESIAN_POINT ( 'NONE',  ( 10.52032305797299649, 21.01595720978967918, 5.334914312547826221 ) ) ;
#2565=CARTESIAN_POINT ( 'NONE',  ( 4.055157505679755303, 21.31629319454957994, 5.262475580173261669 ) ) ;
#2566=CARTESIAN_POINT ( 'NONE',  ( 1.087827283830285152, 11.64378971619068182, 6.276593309653182295 ) ) ;
#2568=CARTESIAN_POINT ( 'NONE',  ( 4.515094011053506939, 19.87742190051230295, 6.403799425183819061 ) ) ;
#2576=CARTESIAN_POINT ( 'NONE',  ( 10.32109744938338736, 10.57878439573850216, 2.246271997629611050 ) ) ;
#2579=CARTESIAN_POINT ( 'NONE',  ( 11.75421244062162707, 19.65546872379294641, -2.449785111124973547 ) ) ;
#2580=CARTESIAN_POINT ( 'NONE',  ( 5.668659900314127142, 12.22025655502366170, -0.2948841661913189638 ) ) ;
#2582=CARTESIAN_POINT ( 'NONE',  ( 1.218075570542494157, 20.32969464963275996, 3.548942957621183503 ) ) ;
#2589=CARTESIAN_POINT ( 'NONE',  ( 11.52990124875157285, 14.00597049205862277, 6.372915746226297529 ) ) ;
#2590=CARTESIAN_POINT ( 'NONE',  ( 12.45292882564249126, 11.21852838486178250, 2.551366500747729749 ) ) ;
#2595=CARTESIAN_POINT ( 'NONE',  ( 3.615788786696767954, 21.36951672728427098, 4.012832544778790478 ) ) ;
#2603=CARTESIAN_POINT ( 'NONE',  ( 10.02812634705811234, 19.92366122336811785, -1.416044127237466643 ) ) ;
#2606=CARTESIAN_POINT ( 'NONE',  ( 1.380668470443014995, 16.87825376251806020, 8.818428724692342513 ) ) ;
#2607=CARTESIAN_POINT ( 'NONE',  ( 1.061556958528351302, 17.24875406955469259, 9.359407947903699565 ) ) ;
#2619=CARTESIAN_POINT ( 'NONE',  ( 1.911717863348795454, 16.21068983458730273, 0.06601438884004878771 ) ) ;
#2621=CARTESIAN_POINT ( 'NONE',  ( 13.45807824676604625, 16.76891278191635593, 7.254207109304789292 ) ) ;
#2634=CARTESIAN_POINT ( 'NONE',  ( 1.905042971753606373, 18.25238594264126135, -0.4688794665317326804 ) ) ;
#2637=CARTESIAN_POINT ( 'NONE',  ( 3.518382746470379185, 15.72191495716070797, -1.383387655830451868 ) ) ;
#2649=CARTESIAN_POINT ( 'NONE',  ( 2.109114244753337086, 11.89287442835424713, 1.870778569916088152 ) ) ;
#2658=CARTESIAN_POINT ( 'NONE',  ( 7.895845287764687193, 11.40205806595764138, 1.929403598022860544 ) ) ;
#2661=CARTESIAN_POINT ( 'NONE',  ( 11.81437950571842421, 10.58622871606461224, -0.01149372372624126934 ) ) ;
#2666=CARTESIAN_POINT ( 'NONE',  ( 8.008853420312213700, 10.95545630081279143, 1.083615874370668752 ) ) ;
#2667=CARTESIAN_POINT ( 'NONE',  ( 8.666075731349446087, 19.39233966230795403, 6.124975956293988943 ) ) ;
#2668=CARTESIAN_POINT ( 'NONE',  ( 2.553282444597012368, 19.73155930485265586, 6.734093347788381756 ) ) ;
#2672=CARTESIAN_POINT ( 'NONE',  ( 7.473677272119537029, 12.62524416591024057, -1.682421981746856865 ) ) ;
#2675=CARTESIAN_POINT ( 'NONE',  ( 13.57150076887395151, 22.11904549731909952, 1.890065446233673452 ) ) ;
#2678=CARTESIAN_POINT ( 'NONE',  ( 3.582999334761938659, 17.35319764795464792, -1.443157694066694807 ) ) ;
#2679=CARTESIAN_POINT ( 'NONE',  ( 1.136769403771278775, 11.72606752483194192, 6.493935939501890076 ) ) ;
#2681=CARTESIAN_POINT ( 'NONE',  ( -0.2158892827208123977, 20.30256849354482185, 4.809740601404282501 ) ) ;
#2687=CARTESIAN_POINT ( 'NONE',  ( 9.742485288642992458, 11.02108255535072168, -0.1776678401114160366 ) ) ;
#2690=CARTESIAN_POINT ( 'NONE',  ( 12.54102569310331816, 21.14438424194486288, -0.3961202071941773983 ) ) ;
#2691=CARTESIAN_POINT ( 'NONE',  ( 5.644721527306630016, 12.32188619433131294, -0.4059770778182363316 ) ) ;
#2693=CARTESIAN_POINT ( 'NONE',  ( 5.111570728101542116, 12.95486688907394246, 6.687046794338158406 ) ) ;
#2697=CARTESIAN_POINT ( 'NONE',  ( 11.41393435462807737, 17.53555608635337393, 6.774740267079724987 ) ) ;
#2698=CARTESIAN_POINT ( 'NONE',  ( 5.005774954510405550, 18.45579612835071615, 7.507356342279577710 ) ) ;
#2709=CARTESIAN_POINT ( 'NONE',  ( 11.97400483195221277, 20.77626866726145138, 3.770676366985183936 ) ) ;
#2710=CARTESIAN_POINT ( 'NONE',  ( 1.140921941160975228, 18.20957084091965683, 8.407057880873713529 ) ) ;
#2712=CARTESIAN_POINT ( 'NONE',  ( 4.163765799268428047, 11.37607716600946084, 3.937147338019182374 ) ) ;
#2723=CARTESIAN_POINT ( 'NONE',  ( 8.556880530951183061, 11.53658052784436094, 3.544415608734076351 ) ) ;
#2724=CARTESIAN_POINT ( 'NONE',  ( 2.476689525297502747, 19.21360138094522796, 1.103912187563293790 ) ) ;
#2725=CARTESIAN_POINT ( 'NONE',  ( 9.457138866168421032, 16.63237982350910826, 8.096441382392347563 ) ) ;
#2734=CARTESIAN_POINT ( 'NONE',  ( 6.010155830883637584, 11.27374497607938331, 1.140174849044627070 ) ) ;
#2737=CARTESIAN_POINT ( 'NONE',  ( 3.536137602566534532, 16.20739087061626194, -1.426542626591323693 ) ) ;
#2750=CARTESIAN_POINT ( 'NONE',  ( 3.051292505765481611, 11.56282819984068233, 5.969449698946827532 ) ) ;
#2755=CARTESIAN_POINT ( 'NONE',  ( 13.21598617904356843, 21.40926851296702438, 1.892361481066431761 ) ) ;
#2759=CARTESIAN_POINT ( 'NONE',  ( 7.245293160062258764, 13.09203250846072208, -1.032046942138396428 ) ) ;
#2762=CARTESIAN_POINT ( 'NONE',  ( 10.92596818984666740, 15.71281552240790980, -4.318717355501334509 ) ) ;
#2767=CARTESIAN_POINT ( 'NONE',  ( 8.082574189534248887, 20.56981455947430248, -1.053435052150081708 ) ) ;
#2768=CARTESIAN_POINT ( 'NONE',  ( 8.985952281912938489, 18.19521758435699965, 6.854078172061496943 ) ) ;
#2771=CARTESIAN_POINT ( 'NONE',  ( 2.772268972823688227, 19.27421045831329138, 7.270480256298323951 ) ) ;
#2776=CARTESIAN_POINT ( 'NONE',  ( 3.515085772594902291, 13.11399658182230077, 8.225784691290757067 ) ) ;
#2777=CARTESIAN_POINT ( 'NONE',  ( 0.8915019007142239715, 11.45163104751902239, 5.416119751115242131 ) ) ;
#2779=CARTESIAN_POINT ( 'NONE',  ( 1.951530046808849228, 14.88544593074506928, 0.2113062994974087283 ) ) ;
#2786=CARTESIAN_POINT ( 'NONE',  ( 9.284756493703616442, 12.52235313574567144, -2.202660405334921023 ) ) ;
#2792=CARTESIAN_POINT ( 'NONE',  ( 5.766733102981766557, 11.86842019456400621, 0.1504060388216716393 ) ) ;
#2794=CARTESIAN_POINT ( 'NONE',  ( 7.156415711929009937, 13.47382733369860119, 6.808263970100831841 ) ) ;
#2798=CARTESIAN_POINT ( 'NONE',  ( 5.774898037902874037, 20.68996510477920836, 4.127828386637749425 ) ) ;
#2802=CARTESIAN_POINT ( 'NONE',  ( 14.01242225938494457, 20.92405235932746166, 3.318798650793908678 ) ) ;
#2803=CARTESIAN_POINT ( 'NONE',  ( 0.7655485048701912154, 20.32785531569650317, 1.774472875170517439 ) ) ;
#2806=CARTESIAN_POINT ( 'NONE',  ( 6.722594236988291172, 11.51780469952192298, 2.735504111625294943 ) ) ;
#2817=CARTESIAN_POINT ( 'NONE',  ( 11.47061170363800819, 21.20994850999973380, 2.421414491514969569 ) ) ;
#2818=CARTESIAN_POINT ( 'NONE',  ( 1.481718377196148406, 15.01894485712453076, 8.639932247213000238 ) ) ;
#2820=CARTESIAN_POINT ( 'NONE',  ( -0.1178366066227022335, 13.07040487695864250, 2.210290218837267506 ) ) ;
#2828=CARTESIAN_POINT ( 'NONE',  ( 0.5545849870865751097, 18.94100205338251186, 1.657181427631677417 ) ) ;
#2831=CARTESIAN_POINT ( 'NONE',  ( 5.943860589180493648, 18.80374057110937969, -0.8413134284775921623 ) ) ;
#2832=CARTESIAN_POINT ( 'NONE',  ( 2.480011849002778046, 19.22266723186190518, 1.111811738353578605 ) ) ;
#2833=CARTESIAN_POINT ( 'NONE',  ( 12.61503648570790048, 20.52417811251926238, 5.621890414035338956 ) ) ;
#2844=B_SPLINE_CURVE_WITH_KNOTS ( 'NONE', 3,
 ( #3264, #11656, #18502, #15325, #15432, #13336, #8337 ),
 .UNSPECIFIED., .F., .F.,
 ( 4, 1, 1, 1, 4 ),
 ( 0.000000000000000000, 0.2499992835874668695, 0.4999999879860682617, 0.7500006923846697093, 1.000000000000000000 ),
 .UNSPECIFIED. ) ;
#2845=CARTESIAN_POINT ( 'NONE',  ( 1.062432521211429393, 11.63297050342826289, 6.580026358220900207 ) ) ;
#2848=CARTESIAN_POINT ( 'NONE',  ( 3.856869842080445920, 12.13100849778645340, 0.6426578681662645787 ) ) ;
#2855=CARTESIAN_POINT ( 'NONE',  ( 4.073379047215689219, 12.50506245289733620, 1.480859224242744299 ) ) ;
#2856=B_SPLINE_CURVE_WITH_KNOTS ( 'NONE', 3,
 ( #20566, #5428, #12193, #10638, #1222, #11281, #18145, #19780, #1110, #4334, #19578, #4654, #18029, #11176, #6195, #16488, #9618, #9726, #17829, #19673, #17928, #2675, #12740, #6298, #9405, #16384 ),
 .UNSPECIFIED., .F., .F.,
 ( 4, 2, 2, 1, 2, 2, 2, 2, 1, 2, 2, 2, 2, 4 ),
 ( 0.000000000000000000, 0.06249999999999787670, 0.1249999999999957534, 0.1874999999999936162, 0.2187499999999944489, 0.2499999999999952816, 0.5000000000000145439, 0.6250000000000203171, 0.6875000000000225375, 0.7187500000000225375, 0.7500000000000225375, 0.8125000000000168754, 0.8750000000000112133, 1.000000000000000000 ),
 .UNSPECIFIED. ) ;
#2862=CARTESIAN_POINT ( 'NONE',  ( 3.270378689765827573, 12.06369702427301505, 6.947417772566477190 ) ) ;
#2873=CARTESIAN_POINT ( 'NONE',  ( 9.804971849761239255, 20.33297925226851888, -1.164330711434534038 ) ) ;
#2877=CARTESIAN_POINT ( 'NONE',  ( 11.19677005946078552, 12.16295462910996150, -2.669674531000855833 ) ) ;
#2882=CARTESIAN_POINT ( 'NONE',  ( 8.636160761027110055, 19.47637978834870154, 6.052143982077559770 ) ) ;
#2889=CARTESIAN_POINT ( 'NONE',  ( 6.698225881633547374, 10.91861244885538085, 4.257383380063560097 ) ) ;
#2890=CARTESIAN_POINT ( 'NONE',  ( 1.494793067313823220, 12.79616285387843178, 8.147785873054054662 ) ) ;
#2893=CARTESIAN_POINT ( 'NONE',  ( 4.219720171048965796, 12.02975038249582163, 2.261177325983976694 ) ) ;
#2900=CARTESIAN_POINT ( 'NONE',  ( 8.998936210029770066, 21.96122921384184323, 1.701528532610274702 ) ) ;
#2902=CARTESIAN_POINT ( 'NONE',  ( 10.07729208704005686, 20.97526076903321979, -1.393227384962903548 ) ) ;
#2906=CARTESIAN_POINT ( 'NONE',  ( 12.86658186011742799, 21.36847253319938034, 0.4848128236591797702 ) ) ;
#2907=CARTESIAN_POINT ( 'NONE',  ( 8.526560839306522865, 20.68998476507356798, 5.890721982252703270 ) ) ;
#2910=CARTESIAN_POINT ( 'NONE',  ( 6.593701308395895744, 19.51815128457440451, 6.507342028609568452 ) ) ;
#2913=CARTESIAN_POINT ( 'NONE',  ( 6.288807527935679431, 20.20918138442159773, 5.471213349970711626 ) ) ;
#2917=CARTESIAN_POINT ( 'NONE',  ( 11.43683134601739049, 18.10558555415017068, -3.440669360032733604 ) ) ;
#2918=CARTESIAN_POINT ( 'NONE',  ( 5.318399099313155354, 16.52349172687392098, 8.034301819513165910 ) ) ;
#2921=CARTESIAN_POINT ( 'NONE',  ( 7.017766547708233382, 11.00346980177178224, 4.143188840625095182 ) ) ;
#2928=CARTESIAN_POINT ( 'NONE',  ( 6.714528961867625156, 11.12069169983300299, 2.708914882803345137 ) ) ;
#2936=ORIENTED_EDGE ( 'NONE', *, *, #21877, .T. ) ;
#2937=CARTESIAN_POINT ( 'NONE',  ( 11.91464549116346561, 20.84857631512679177, 3.612794791681625650 ) ) ;
#2946=CARTESIAN_POINT ( 'NONE',  ( 0.8282372033119331789, 19.59804870509496055, 2.312752627255655113 ) ) ;
#2949=CARTESIAN_POINT ( 'NONE',  ( 9.701140030272853210, 21.05370774754728203, 3.420069439634078279 ) ) ;
#2954=CARTESIAN_POINT ( 'NONE',  ( 7.366404870011150408, 12.62799681450196054, -1.646865681378777646 ) ) ;
#2964=CARTESIAN_POINT ( 'NONE',  ( 0.5847478725274279920, 20.32785531569650317, 1.828616380043220691 ) ) ;
#2967=CARTESIAN_POINT ( 'NONE',  ( 3.632615605465845832, 17.33140468479308538, -1.342300317307963509 ) ) ;
#2972=CARTESIAN_POINT ( 'NONE',  ( 2.232581729494868217, 12.55203364629052665, 2.299247354297082602 ) ) ;
#2975=CARTESIAN_POINT ( 'NONE',  ( 4.582301617914484204, 11.87654007454232108, 3.801650534573477458 ) ) ;
#2981=CARTESIAN_POINT ( 'NONE',  ( 3.634673347361986551, 15.97827594584995481, 9.198068844196187754 ) ) ;
#2990=CARTESIAN_POINT ( 'NONE',  ( 10.81515204167621924, 18.24951553479433031, -3.654582590115240226 ) ) ;
#2993=CARTESIAN_POINT ( 'NONE',  ( 11.15957945745538815, 12.36081089520519605, -2.843515111212955748 ) ) ;
#2997=CARTESIAN_POINT ( 'NONE',  ( 8.885977996197350848, 12.18137409406300620, 4.901112392138662344 ) ) ;
#3002=CARTESIAN_POINT ( 'NONE',  ( 2.855389239292441150, 11.23804227924006227, 5.233798368148996794 ) ) ;
#3003=CARTESIAN_POINT ( 'NONE',  ( 0.7890252754738890095, 11.42114643257019146, 4.969940827006558592 ) ) ;
#3006=CARTESIAN_POINT ( 'NONE',  ( 3.448768254860767435, 13.61749910441900191, 7.578225799708883770 ) ) ;
#3014=CARTESIAN_POINT ( 'NONE',  ( 7.462231758176627316, 21.81816933872264030, 3.277137776123120183 ) ) ;
#3015=CARTESIAN_POINT ( 'NONE',  ( 9.166816848515864535, 13.36017816153255211, -2.795096715123733588 ) ) ;
#3017=CARTESIAN_POINT ( 'NONE',  ( 8.855399128654450891, 19.86079412954436663, 6.740554311246585328 ) ) ;
#3019=CARTESIAN_POINT ( 'NONE',  ( 3.416691995540810822, 16.48226916726223479, 8.524304092238224939 ) ) ;
#3022=CARTESIAN_POINT ( 'NONE',  ( 6.665396026729170309, 19.45118757208885896, 6.417806572678339094 ) ) ;
#3027=CARTESIAN_POINT ( 'NONE',  ( 12.09589873078120270, 11.13638386089868249, 0.7328227269680089861 ) ) ;
#3029=CARTESIAN_POINT ( 'NONE',  ( 3.094989319135907913, 19.78346126529704208, 7.974999081070190066 ) ) ;
#3040=CARTESIAN_POINT ( 'NONE',  ( 11.86489017329819085, 20.90669377702615250, 3.480282917028821199 ) ) ;
#3044=CARTESIAN_POINT ( 'NONE',  ( 6.279877271179575615, 11.31448603738602188, 4.296343679347063294 ) ) ;
#3050=CARTESIAN_POINT ( 'NONE',  ( 3.843255135554278556, 17.07327212836336372, -0.6144225183285193514 ) ) ;
#3054=CARTESIAN_POINT ( 'NONE',  ( 5.535879021512672082, 15.56565457311297251, -1.414609335357769559 ) ) ;
#3057=CARTESIAN_POINT ( 'NONE',  ( 5.391407144478529645, 13.59023913265000338, -1.534842905340066954 ) ) ;
#3061=CARTESIAN_POINT ( 'NONE',  ( 10.88042432497300638, 18.51148264076616101, 6.327082982554776081 ) ) ;
#3062=CARTESIAN_POINT ( 'NONE',  ( 7.229729504486647862, 14.38111527192631200, -2.659786112516965062 ) ) ;
#3067=CARTESIAN_POINT ( 'NONE',  ( 3.342050458355601883, 21.45407066062478307, 3.539861934473672811 ) ) ;
#3070=CARTESIAN_POINT ( 'NONE',  ( 5.639002058890934421, 21.52895174503652953, 3.779455238249453064 ) ) ;
#3076=CARTESIAN_POINT ( 'NONE',  ( 1.120844084417135011, 12.59384379629693207, 6.529727573272420038 ) ) ;
#3079=CARTESIAN_POINT ( 'NONE',  ( 2.525842802073233084, 12.09107524552456603, 3.660819305400447199 ) ) ;
#3080=CARTESIAN_POINT ( 'NONE',  ( 9.612433970843095921, 14.64457645186116252, 7.826711049808183773 ) ) ;
#3084=CARTESIAN_POINT ( 'NONE',  ( 2.013765651847553073, 18.70393287884557054, -0.1586800916523363469 ) ) ;
#3092=CARTESIAN_POINT ( 'NONE',  ( 11.63887962177664015, 21.02863807409008245, 3.776004642387295274 ) ) ;
#3099=CARTESIAN_POINT ( 'NONE',  ( 8.105578319609293203, 11.67745808062331214, 1.442659932574160253 ) ) ;
#3103=CARTESIAN_POINT ( 'NONE',  ( -0.1543974142126335047, 14.11522100541123592, 0.5695158722648775429 ) ) ;
#3106=CARTESIAN_POINT ( 'NONE',  ( 0.8541095398342212208, 12.13066582883064193, 4.831952372105788207 ) ) ;
#3112=CARTESIAN_POINT ( 'NONE',  ( 9.377360826946816275, 19.33115936737788232, -2.952836903115966471 ) ) ;
#3114=CARTESIAN_POINT ( 'NONE',  ( 9.199613818395116382, 17.51864436858641838, -3.513625226794980350 ) ) ;
#3118=CARTESIAN_POINT ( 'NONE',  ( 6.992329041007389279, 21.55996507129514939, 1.710843802307564721 ) ) ;
#3120=CARTESIAN_POINT ( 'NONE',  ( 3.471600356522836606, 14.96929529427155714, 8.313123240795297519 ) ) ;
#3126=CARTESIAN_POINT ( 'NONE',  ( 11.40763102503163218, 14.41047425500502754, -3.504232829823089368 ) ) ;
#3127=CARTESIAN_POINT ( 'NONE',  ( 3.352276079298180722, 11.89587513260652152, 6.861475299447377552 ) ) ;
#3130=CARTESIAN_POINT ( 'NONE',  ( 6.396056618077795797, 11.71523274630726164, 2.847703469759983008 ) ) ;
#3133=DIRECTION ( 'NONE',  ( 0.2868778675745011220, 0.000000000000000000, 0.9579671649362033747 ) ) ;
#3141=CARTESIAN_POINT ( 'NONE',  ( 12.85889632468635568, 18.41644950543497572, 5.976846945769059616 ) ) ;
#3145=CARTESIAN_POINT ( 'NONE',  ( 6.985997644112802440, 16.61588919119046182, 8.232423580698503329 ) ) ;
#3153=CARTESIAN_POINT ( 'NONE',  ( 9.216504298751090118, 16.57988186816537279, 7.325230060800960175 ) ) ;
#3155=CARTESIAN_POINT ( 'NONE',  ( 11.10672801841564628, 12.31819272753022254, -2.965602515288232155 ) ) ;
#3160=CARTESIAN_POINT ( 'NONE',  ( 9.140504733104041435, 21.05562268498557188, 1.832113029465568754 ) ) ;
#3161=CARTESIAN_POINT ( 'NONE',  ( 6.292329232406544293, 20.69394519596638204, -0.2665356535715593389 ) ) ;
#3167=CARTESIAN_POINT ( 'NONE',  ( 1.548022356803757216, 14.62510310756713672, -0.4782326917522521370 ) ) ;
#3170=CARTESIAN_POINT ( 'NONE',  ( 6.850747683931677656, 19.94702954872458989, 7.017284919865954151 ) ) ;
#3178=CARTESIAN_POINT ( 'NONE',  ( 6.355167927674128414, 20.69792818844234361, -0.2884820177363571769 ) ) ;
#3179=CARTESIAN_POINT ( 'NONE',  ( 3.964049121815345966, 12.88683406160677158, 0.9507199798804107926 ) ) ;
#3185=CARTESIAN_POINT ( 'NONE',  ( 1.864081481279129537, 12.78457889254149649, 0.7313840301176890435 ) ) ;
#3186=ADVANCED_FACE ( 'NONE', ( #6508 ), #13269, .T. ) ;
#3192=CARTESIAN_POINT ( 'NONE',  ( 13.15380310827069010, 21.44506156727471335, 1.916236206408076903 ) ) ;
#3196=CARTESIAN_POINT ( 'NONE',  ( 7.747576815138661921, 12.05201058041374118, 0.2846308798510710503 ) ) ;
#3204=CARTESIAN_POINT ( 'NONE',  ( 9.270728378017370375, 14.93585744516916236, 7.021239391598488311 ) ) ;
#3210=CARTESIAN_POINT ( 'NONE',  ( 3.454954327428137351, 15.44872671029758671, -1.443864749231975830 ) ) ;
#3211=CARTESIAN_POINT ( 'NONE',  ( -0.1786810500680980907, 15.98335145267441249, 0.04971173333621729806 ) ) ;
#3215=CARTESIAN_POINT ( 'NONE',  ( 0.4780110449530477479, 13.07040487695864250, 2.031854558472322658 ) ) ;
#3222=CARTESIAN_POINT ( 'NONE',  ( 6.788691988670617405, 21.59576476661624156, 1.422531602670973561 ) ) ;
#3224=B_SPLINE_CURVE_WITH_KNOTS ( 'NONE', 3,
 ( #1590, #13228, #8332, #6668, #11544, #17614, #14319, #14100, #20803, #5989, #5671, #2468, #21039, #14422, #5884, #2792, #7661, #12875, #19370, #2580, #2356, #2691, #4351, #7556, #10768, #4125, #11092, #17732, #9196, #4236, #1018, #16086, #16193, #9087, #10976, #15980, #811, #15864, #19158, #12760, #16296, #12430, #693, #4024, #10868, #9420, #9312, #17511, #14213, #7438, #21250, #916, #17845, #19481, #7765, #20927, #21135, #14532, #4460, #6103, #19594, #5787, #11192, #17944, #9528, #12546, #19270, #10076, #14974, #6640, #13404, #1130, #20114, #18361, #18050, #6211, #8199, #1341, #4987, #8305, #8083, #16723, #18475, #6434, #21689, #11743, #21460, #3118, #14858, #18166, #7983, #12982, #14754, #3344, #9638, #1565, #9965, #20010, #16404, #3229, #21354, #1240, #7871, #19913, #19691, #9742, #16612, #14648, #9842, #4560, #11303, #13090, #2907, #21573, #4784, #6317, #19800, #11514, #4675, #11418, #3017, #16505, #13201, #6547, #18257, #1452, #13308, #4880, #11626, #15077, #21790, #461, #8632, #12069, #11849, #17258, #15510, #13855, #1993, #18907, #13520, #5304, #5202, #230, #10512, #3665, #3778, #18580, #13740, #11952, #3551, #3443, #6755, #340, #3888, #12288, #16922, #6871, #18683, #2099, #10178, #20228, #1769, #5101, #8845, #18795, #20556, #7085, #15624, #8516, #10289, #10411, #13972, #7210, #5418, #17038, #1885, #15408, #20669, #20434, #5529, #16821, #8734, #19013, #1663, #8401, #15177, #12183, #15296, #6, #121, #6970, #13630, #20328, #17153, #6078, #2220, #14294, #2666, #9169, #11064, #12619, #2444, #5762, #17487, #566, #2330, #7742, #19130, #17820, #19451, #7635, #3998, #12727, #8961, #10946, #15738, #4210, #19342, #9395, #4326, #12519, #15952, #14502, #668, #7310, #21219, #9285, #14187, #12850, #16164, #14397, #893, #783, #9064, #15839, #21014, #5962, #21110, #10843, #14074, #20781, #19242, #19571, #17702, #20895, #990, #10626, #5860, #17379, #2554, #5643, #7413, #4104, #12404, #10741, #17591, #7531, #16061, #4439, #9503, #2767, #16274, #7849, #1105, #14624, #21333, #11169, #17920, #6193, #12960, #11870, #16841, #13758, #13991, #20690, #3684, #20246, #13881, #13648, #15423, #10532, #8421, #18595, #8650, #249, #3465, #15198, #17278, #5547, #20578, #20348, #140, #5120, #10094, #12202, #1682, #18925, #12306, #6989, #17169, #1794, #5329, #17056, #5217, #10199, #25, #16942, #479, #8536, #3796, #2124, #359, #15315, #5439, #6775, #10427, #13539, #18817, #12094, #8865, #15652, #11976, #1902, #7233, #6887, #18706, #3365, #2009, #3574, #10314, #20459, #8749, #15530, #7111, #1014, #9417, #9082, #7761, #10864, #15975, #7329, #7654, #16083, #17842, #7433, #4122, #19033, #3907, #17726, #10649, #14208, #17610, #4232, #14417, #20923, #9191, #807, #12425, #6100, #10971, #7552, #5666, #2242, #11087, #14527, #21132, #5782, #15858, #14094, #17401, #5984, #8980, #12754, #21245, #2464, #2576, #15758, #17507, #21032, #14315, #20799, #19476, #5881, #585, #4017, #12643, #19367, #19154, #4347, #10764, #2687, #2352, #688, #12540, #9308, #19266, #16185, #913, #7978, #4672, #21788, #14969, #19793, #2786, #1338, #4782, #16722, #3015, #1559, #6314, #7868, #11295, #13088, #16292, #13306, #4457, #8081, #1125, #1448, #9840, #6207, #9962, #21685, #14644, #11416, #14750, #14855, #19910, #12870, #9523, #6545, #16609, #3114, #18162, #19686, #18045, #21570, #8196, #20008, #9740, #4878, #21349, #16502, #8303, #13199, #1237, #11623, #19590, #6429, #15075, #11512, #11188, #2902, #9635, #18358, #3225, #17940, #12978, #4556, #16400, #18255, #8398, #10176, #10283, #13626, #5098, #18790, #2095, #12178, #18902, #15617, #15174, #20110, #17033, #17253, #8840, #6966, #1661, #3546, #4, #3774, #1989, #6750, #11740, #13732, #6867, #10509, #13848, #20324, #6637, #4983, #1880, #20551, #5195, #7080, #13517, #16919, #20226, #11847, #8730, #18575, #13401, #3441, #5414, #15506, #3660, #1765, #334, #18473, #20430, #3341, #226, #15404, #10071, #16819, #8511, #15291, #5300, #118, #11948, #18677, #12063, #8627, #10404, #17149, #15948, #9391, #9164, #4320, #12723, #12399, #11060, #14183, #19237, #13966, #5638, #10839, #5524, #15733, #19446, #456, #7206, #21008, #20665, #10737, #20888, #7527, #5758, #17816, #776, #5957, #12514, #17587, #17371, #888, #5855, #19338, #14290, #2548, #19008, #2439, #17482, #4100, #16057, #12615, #9281, #2215, #4205, #2326, #9060, #8957, #12284, #10942, #3884, #2661, #562, #19123, #15835, #7629, #7306, #10622, #14069, #20776, #14392, #17697, #21106, #3993, #662, #7409, #2877, #2993, #13570, #18527, #13459, #9608, #1214, #7956, #20274, #19767, #1718, #9497, #21434, #11897, #7737, #4642, #8455, #14727, #16871, #16270, #4531, #2762, #17916, #3392, #9717, #21215, #1100, #6287, #11388, #18626, #10126, #15228, #14498, #16481, #6073, #1316, #8059, #59, #6809, #5145, #11794, #14830, #3493, #16159, #18134, #12845, #21543, #6697, #985, #20169, #19567, #5044, #4434, #11165, #6188, #7843, #14620, #21328, #12956, #19664, #11270, #18018, #16375, #7357, #19062, #20378, #3717, #12124, #20610, #17306, #10228, #8780, #5698, #10561, #15785, #2035, #5468 ),
 .UNSPECIFIED., .F., .F.,
 ( 4, 3, 3, 3, 3, 3, 3, 3, 3, 3, 3, 3, 3, 3, 3, 3, 3, 3, 3, 3, 3, 3, 3, 3, 3, 3, 3, 3, 3, 3, 3, 3, 3, 3, 3, 3, 3, 3, 3, 3, 3, 3, 3, 3, 3, 3, 3, 3, 3, 3, 3, 3, 3, 3, 3, 3, 3, 3, 3, 3, 3, 3, 3, 3, 3, 3, 3, 3, 3, 3, 3, 3, 3, 3, 3, 3, 3, 3, 3, 3, 3, 3, 3, 3, 3, 3, 3, 3, 3, 3, 3, 3, 3, 3, 3, 3, 3, 3, 3, 3, 3, 3, 3, 3, 3, 3, 3, 3, 3, 3, 3, 3, 3, 3, 3, 3, 3, 3, 3, 3, 3, 3, 3, 3, 3, 3, 3, 3, 3, 3, 3, 3, 3, 3, 3, 3, 3, 3, 3, 3, 3, 3, 3, 3, 3, 3, 3, 3, 3, 3, 3, 3, 3, 3, 3, 3, 3, 3, 3, 3, 3, 3, 3, 3, 3, 3, 3, 3, 3, 3, 3, 3, 3, 3, 3, 3, 3, 3, 3, 3, 3, 3, 3, 3, 3, 3, 3, 3, 3, 3, 3, 3, 3, 3, 3, 3, 3, 3, 3, 3, 3, 3, 3, 3, 3, 3, 3, 3, 3, 3, 3, 3, 3, 3, 3, 3, 3, 3, 3, 3, 3, 3, 4 ),
 ( 3.925670666076010412E-10, 0.006134969684172960139, 0.01226993897578289999, 0.01250000110578649952, 0.01840490826738569799, 0.02453987755898860007, 0.02874999196542460042, 0.03067484685060149763, 0.03680981614220439624, 0.04294478543380729485, 0.04500001148800239492, 0.04907975472542019935, 0.05521472401702309796, 0.06124999979532610300, 0.06134969330862600351, 0.06748466260023890106, 0.07361963189184179968, 0.07749999361584829216, 0.07975460118344469829, 0.08588957047505760278, 0.09202453976666050139, 0.09375001134813680526, 0.09815950905826340001, 0.1042944783498659933, 0.1099999977686790115, 0.1104294476415189907, 0.1165644169330719987, 0.1226993862247249961, 0.1262499965223490006, 0.1288343555162780041, 0.1349693248079310015, 0.1411042940994839956, 0.1425000097258770082, 0.1472392633911369930, 0.1533742326826889879, 0.1587499949892519913, 0.1595092019743420131, 0.1656441712658950072, 0.1717791405575480046, 0.1750000001443519915, 0.1779141098491009987, 0.1840490791407540239, 0.1901840484324069935, 0.1912500069742819886, 0.1963190177239599876, 0.2024539870156130128, 0.2074999923037350036, 0.2085889563071649799, 0.2147239255988180051, 0.2208588948903709992, 0.2237500038726649987, 0.2269938641820239966, 0.2331288334735770185, 0.2392638027652299881, 0.2400000037079649817, 0.2453987720567829822, 0.2515337413484359796, 0.2562499904402019690, 0.2576687106399890292, 0.2638036799316419989, 0.2699386492231939938, 0.2725000070773460070, 0.2760736185148470190, 0.2822085878064999886, 0.2883435570980529827, 0.2887500007056810203, 0.2944785263897060079, 0.3006134956812590020, 0.3049999898827670530, 0.3067484649729119717, 0.3128834342644650213, 0.3190184035561179909, 0.3212500092129830231, 0.3251533728476699858, 0.3312883421393230110, 0.3374233114308760051, 0.3435582807225289748, 0.3496932500140820244, 0.3537499908145410044, 0.3558282193057349940, 0.3619631885972879881, 0.3680981578889409578, 0.3700000099152420119, 0.3742331271805939830, 0.3803680964721469770, 0.3862499973465969849, 0.3865030657637990030, 0.3926380350553519971, 0.3987730043470049668, 0.4024999931180490154, 0.4049079736385579609, 0.4110429429302110416, 0.4171779122217639801, 0.4187500090755189586, 0.4233128815134169498, 0.4294478508049699994, 0.4349999948622240153, 0.4355828200966229691, 0.4417177893881750195, 0.4478527586798280447, 0.4512499964198479763, 0.4539877279713809832, 0.4601226972630340084, 0.4662576665546870336, 0.4675000068816390075, 0.4723926358462400277, 0.4785276051378929973, 0.4837499920180829971, 0.4846625744294459914, 0.4907975437210990166, 0.4969325130126520107, 0.5000000001685559470, 0.5030674823043039812, 0.5092024515958569753, 0.5153374208875100004, 0.5162500038123820634, 0.5214723901790629945, 0.5276073594707160197, 0.5324999896260669274, 0.5337423287622690138, 0.5398772980539219279, 0.5460122673455750641, 0.5487500037328389979, 0.5521472366371280582, 0.5582822059287810834, 0.5644171752203329673, 0.5650000005741819820, 0.5705521445119859925, 0.5766871138035389865, 0.5812499883134720768, 0.5828220830951920117, 0.5889570523867450058, 0.5950920216783980310, 0.5975000065084529188, 0.6012269909699510251, 0.6073619602616039392, 0.6134969295531559341, 0.6137499979673349815, 0.6196318988448089593, 0.6257668681363620644, 0.6299999884298229658, 0.6319018374280149786, 0.6380368067196680038, 0.6441717760112209978, 0.6462500080219170107, 0.6503067453028739120, 0.6564417145944269061, 0.6625766838860800423, 0.6687116531776330364, 0.6748466224692860616, 0.6787499900177470513, 0.6809815917608379454, 0.6871165610524909706, 0.6932515303440439647, 0.6950000080182459072, 0.6993864996356971009, 0.7055214689272500950, 0.7112499946371489967, 0.7116564382189030091, 0.7177914075104560032, 0.7239263768021090284, 0.7274999928349140665, 0.7300613460937620536, 0.7361963153853140485, 0.7423312846769670736, 0.7437500065219889711, 0.7484662539685200677, 0.7546012232601729819, 0.7599999918748050476, 0.7607361925517259760, 0.7668711618433790012, 0.7730061311349319952, 0.7762499964153849463, 0.7791411004265850204, 0.7852760697181370153, 0.7914110390097899295, 0.7925000038579510520, 0.7975460083013429236, 0.8036809775929959487, 0.8087499891400269370, 0.8098159468845489428, 0.8159509161762020790, 0.8220858854678549932, 0.8250000001582830089, 0.8282208547594079873, 0.8343558240510610124, 0.8404907933426140065, 0.8412500006211290904, 0.8466257626342659215, 0.8527607319258190266, 0.8574999871756959768, 0.8588957012174720518, 0.8650306705090250459, 0.8711656398006779600, 0.8737500034313691044, 0.8773006090922309541, 0.8834355783838840903, 0.8895705476754370844, 0.8899999975822959764, 0.8957055169670899986, 0.9018404862586419934, 0.9062499864893789336, 0.9079754555502950186, 0.9141104248419479328, 0.9202453941335010379, 0.9225000056768799528, 0.9263803634251540631, 0.9325153327167070572, 0.9386503020083599713, 0.9387499955187870171, 0.9447852712999129654, 0.9509202405915659906, 0.9549999872948490287, 0.9570552098831189847, 0.9631901791747710107, 0.9693251484663240047, 0.9712500064484830276, 0.9754601177579770299, 0.9815950870495300240, 0.9874999942073410253, 0.9877300563411829382, 0.9938650256327359322, 0.9999999949243889574 ),
 .UNSPECIFIED. ) ;
#3225=CARTESIAN_POINT ( 'NONE',  ( 10.30870223385876372, 21.38393516060608945, -0.7694343885214717238 ) ) ;
#3229=CARTESIAN_POINT ( 'NONE',  ( 7.744129980428262172, 21.62877852693285874, 3.774467130889562316 ) ) ;
#3238=CARTESIAN_POINT ( 'NONE',  ( 9.910007369255215082, 12.06055924076114216, -1.458087275941579275 ) ) ;
#3239=CLOSED_SHELL ( 'NONE', ( #3186, #21303, #2224, #12793, #3616, #20570 ) ) ;
#3240=CARTESIAN_POINT ( 'NONE',  ( 2.565001838803366407, 20.83040400030756345, 6.599755016110631090 ) ) ;
#3253=CARTESIAN_POINT ( 'NONE',  ( 11.01422740109451937, 12.78785806401926095, 5.371526240743504488 ) ) ;
#3256=CARTESIAN_POINT ( 'NONE',  ( 13.10878000956375722, 16.62975971659733787, 6.403471165590654657 ) ) ;
#3260=CARTESIAN_POINT ( 'NONE',  ( -0.6063867502221114147, 20.39392809349225999, 4.918772829083649434 ) ) ;
#3264=CARTESIAN_POINT ( 'NONE',  ( -0.1849527129589544072, 21.03045532914853055, 5.150944214860931680 ) ) ;
#3266=CARTESIAN_POINT ( 'NONE',  ( 3.902814694466206102, 17.50837036387243373, -0.5262828315819897407 ) ) ;
#3274=CARTESIAN_POINT ( 'NONE',  ( 9.246163857139698905, 15.41858152414332750, -2.865988929752159464 ) ) ;
#3276=CARTESIAN_POINT ( 'NONE',  ( 8.395333527031370480, 21.35108299968154455, -0.1513204485400149457 ) ) ;
#3282=CARTESIAN_POINT ( 'NONE',  ( 10.10356450120315763, 20.54903548560601578, 4.403050154276548334 ) ) ;
#3283=CARTESIAN_POINT ( 'NONE',  ( 12.00018126865166401, 10.33025398667194139, 0.6449774946455864022 ) ) ;
#3290=CARTESIAN_POINT ( 'NONE',  ( 3.171475446957850775, 11.89587513260652152, 6.915618804319352719 ) ) ;
#3293=CARTESIAN_POINT ( 'NONE',  ( 6.634334687536620478, 20.47748668554710960, 6.460578472925798899 ) ) ;
#3300=CARTESIAN_POINT ( 'NONE',  ( 11.86776211864144770, 20.19146305430580313, -3.151330312819546453 ) ) ;
#3307=CARTESIAN_POINT ( 'NONE',  ( 2.006824028408880967, 12.19579955713188646, 1.406014205417876806 ) ) ;
#3316=CARTESIAN_POINT ( 'NONE',  ( 11.40924028808832524, 19.77353779035612291, -2.514324500111221994 ) ) ;
#3324=CARTESIAN_POINT ( 'NONE',  ( 9.272449929266908697, 15.41853785818361366, 7.143357861250589913 ) ) ;
#3330=CARTESIAN_POINT ( 'NONE',  ( 0.2584401386766148612, 11.97670218361793282, 2.636262851981420408 ) ) ;
#3332=CARTESIAN_POINT ( 'NONE',  ( 3.848227522671471501, 14.05442396375854130, -0.1621833816910843162 ) ) ;
#3339=CARTESIAN_POINT ( 'NONE',  ( 11.09713900613744286, 13.72201164258680173, 7.095940182945178698 ) ) ;
#3341=CARTESIAN_POINT ( 'NONE',  ( 13.23764915724263247, 17.68517305658646421, 7.025134865669341977 ) ) ;
#3344=CARTESIAN_POINT ( 'NONE',  ( 7.493139529700894030, 21.70524941769282989, 3.085289908977460804 ) ) ;
#3349=CARTESIAN_POINT ( 'NONE',  ( 7.058968441123867343, 18.03812148340534094, 7.310900384194754409 ) ) ;
#3354=CARTESIAN_POINT ( 'NONE',  ( 7.168925875378048040, 11.43880029099476126, 4.249497758341346021 ) ) ;
#3357=CARTESIAN_POINT ( 'NONE',  ( 3.384013584124889729, 18.28285541323128172, 8.939367623630410264 ) ) ;
#3365=CARTESIAN_POINT ( 'NONE',  ( 11.37517772858290677, 16.82229854605489550, 7.558283270811076981 ) ) ;
#3367=CARTESIAN_POINT ( 'NONE',  ( 13.14561042020424075, 14.29266759713506652, 6.004341513937229813 ) ) ;
#3369=CARTESIAN_POINT ( 'NONE',  ( 4.635123512035450588, 12.02159401923784010, 5.456644224042059399 ) ) ;
#3378=CARTESIAN_POINT ( 'NONE',  ( 13.49155064010361471, 21.41280428856536489, 2.268588950130180582 ) ) ;
#3379=CARTESIAN_POINT ( 'NONE',  ( 11.22736586087230393, 14.04501930844190660, 6.381908989529498477 ) ) ;
#3381=CARTESIAN_POINT ( 'NONE',  ( 9.493963008126993230, 14.64601895156848776, 7.857208408461620053 ) ) ;
#3386=CARTESIAN_POINT ( 'NONE',  ( 10.37956912121652131, 20.06616296009919864, 5.118516414627194422 ) ) ;
#3387=CARTESIAN_POINT ( 'NONE',  ( 11.19977597401542901, 12.02381550237932295, 5.862906665875985190 ) ) ;
#3392=CARTESIAN_POINT ( 'NONE',  ( 10.93899656833006695, 16.07662961819365677, -4.343109068444145571 ) ) ;
#3393=CARTESIAN_POINT ( 'NONE',  ( 1.795302335458940579, 11.90891113418242142, 1.891703290912318147 ) ) ;
#3396=CARTESIAN_POINT ( 'NONE',  ( 6.271597670968151128, 21.07808100295144982, 5.497337236915185166 ) ) ;
#3401=CARTESIAN_POINT ( 'NONE',  ( 1.917016422406038645, 14.23731939350392217, 0.6161444402295471745 ) ) ;
#3405=CARTESIAN_POINT ( 'NONE',  ( 2.061500982823199823, 18.90949574706995406, -0.05049993479792989209 ) ) ;
#3416=CARTESIAN_POINT ( 'NONE',  ( 11.21942781118996990, 21.35256525590422072, 2.014744391537809598 ) ) ;
#3423=CARTESIAN_POINT ( 'NONE',  ( 8.349616978403640033, 11.53155059953441075, 2.515314769403827366 ) ) ;
#3424=CARTESIAN_POINT ( 'NONE',  ( 3.429437941603723505, 15.04225738252103461, 8.249934406976112911 ) ) ;
#3428=CARTESIAN_POINT ( 'NONE',  ( -0.02301601734996851917, 17.64104708308499880, 0.1929137087451379406 ) ) ;
#3432=CARTESIAN_POINT ( 'NONE',  ( 3.509439300273259565, 17.99578554531247576, 8.209304056720553078 ) ) ;
#3439=CARTESIAN_POINT ( 'NONE',  ( 7.252818009422052903, 21.72673311005876329, 3.332971805317985758 ) ) ;
#3441=CARTESIAN_POINT ( 'NONE',  ( 13.02404159230300174, 18.96437007834888888, 6.572007044681392074 ) ) ;
#3443=CARTESIAN_POINT ( 'NONE',  ( 9.484727789049149038, 14.55342286457404555, 7.702955061670587966 ) ) ;
#3444=CARTESIAN_POINT ( 'NONE',  ( 6.206528234269004685, 20.44464562225766358, 5.215226569823482983 ) ) ;
#3451=CARTESIAN_POINT ( 'NONE',  ( 7.965518406716108224, 21.40982604368873865, 3.095704102008969283 ) ) ;
#3452=CARTESIAN_POINT ( 'NONE',  ( 5.376417996899292895, 15.42671590247574542, 7.949579020774653060 ) ) ;
#3453=CARTESIAN_POINT ( 'NONE',  ( 5.957292673923675785, 11.58109048093756321, 0.5680188385854727517 ) ) ;
#3456=CARTESIAN_POINT ( 'NONE',  ( 2.812310173516594958, 12.03281576442448042, 5.089945059218950796 ) ) ;
#3461=( LENGTH_UNIT ( ) NAMED_UNIT ( * ) SI_UNIT ( .MILLI., .METRE. ) );
#3465=CARTESIAN_POINT ( 'NONE',  ( 9.621872815474498353, 21.81549092655993860, 3.148079541620338428 ) ) ;
#3468=CARTESIAN_POINT ( 'NONE',  ( 12.91587739171063021, 18.12504211422740141, 6.097017937141830934 ) ) ;
#3470=CARTESIAN_POINT ( 'NONE',  ( 3.788989557899201888, 18.74075759514924400, -0.1305876994136269953 ) ) ;
#3475=CARTESIAN_POINT ( 'NONE',  ( 6.308080149185702368, 10.92909866215502213, 2.816645635463620678 ) ) ;
#3478=CARTESIAN_POINT ( 'NONE',  ( 11.59058392313026076, 11.69902548067542192, -0.9553338480370143770 ) ) ;
#3479=CARTESIAN_POINT ( 'NONE',  ( 11.16177022631493720, 16.27078869972547892, -3.700522497431344426 ) ) ;
#3480=CARTESIAN_POINT ( 'NONE',  ( 3.871967422488196142, 13.36420590592894264, 7.787245618273578529 ) ) ;
#3481=CARTESIAN_POINT ( 'NONE',  ( 11.99291685403952101, 21.69057506433588145, 3.971327024042194509 ) ) ;
#3487=CARTESIAN_POINT ( 'NONE',  ( 10.30207946694087262, 20.21713832266318533, 4.919229887006573598 ) ) ;
#3488=CARTESIAN_POINT ( 'NONE',  ( 13.59613746992887506, 22.20171528482708112, 2.423511226437077948 ) ) ;
#3493=CARTESIAN_POINT ( 'NONE',  ( 11.39852134277141360, 19.53005087718068111, -3.485485373183195623 ) ) ;
#3494=CARTESIAN_POINT ( 'NONE',  ( 3.137202520011495466, 21.36287299093768155, 3.610942509148120205 ) ) ;
#3497=CARTESIAN_POINT ( 'NONE',  ( 6.099937697436127237, 21.27555018051177171, 5.034626513405442871 ) ) ;
#3507=CARTESIAN_POINT ( 'NONE',  ( 1.684397325192768413, 16.20931629175901634, -0.6950957481128374749 ) ) ;
#3520=CARTESIAN_POINT ( 'NONE',  ( 6.628279328482711286, 11.82958596167992127, 4.306176057588643857 ) ) ;
#3521=CARTESIAN_POINT ( 'NONE',  ( 7.459674749802357674, 12.98268228153804138, 7.394826790990479459 ) ) ;
#3528=CARTESIAN_POINT ( 'NONE',  ( 7.542404986124462418, 13.51227111306877582, -1.211156836538626713 ) ) ;
#3534=CARTESIAN_POINT ( 'NONE',  ( -0.005519112348255535150, 12.92290799471926555, 1.396275220874262368 ) ) ;
#3539=CARTESIAN_POINT ( 'NONE',  ( 3.451617604026494757, 12.51757774536594070, 6.438078665016687019 ) ) ;
#3543=CARTESIAN_POINT ( 'NONE',  ( 5.749044579667681454, 11.19290776549860134, 1.467727128716227680 ) ) ;
#3546=CARTESIAN_POINT ( 'NONE',  ( 11.77504171138678579, 21.82382164323249185, 3.283033003548121886 ) ) ;
#3551=CARTESIAN_POINT ( 'NONE',  ( 9.488210770742556477, 14.67898782071606689, 7.740838414784177779 ) ) ;
#3552=CARTESIAN_POINT ( 'NONE',  ( 6.695256992210804725, 11.71104153968872197, 4.085482631342693516 ) ) ;
#3556=CARTESIAN_POINT ( 'NONE',  ( 1.355844778331848799, 20.27946762757392563, 3.649167961216476463 ) ) ;
#3560=CARTESIAN_POINT ( 'NONE',  ( 13.39449014422897122, 13.16814630638014272, 5.497670784391714527 ) ) ;
#3561=CARTESIAN_POINT ( 'NONE',  ( 6.815620469402779769, 10.91373323652594252, 4.223291697927726851 ) ) ;
#3562=CARTESIAN_POINT ( 'NONE',  ( -0.1849527129589544072, 21.03045532914853055, 5.150944214860931680 ) ) ;
#3564=EDGE_CURVE ( 'NONE', #14025, #8219, #17865, .T. ) ;
#3566=CARTESIAN_POINT ( 'NONE',  ( 0.1086559561431187093, 17.19705222221691088, 0.7960978371211332449 ) ) ;
#3574=CARTESIAN_POINT ( 'NONE',  ( 11.41259685292655668, 16.31337187110278464, 7.583935353899422083 ) ) ;
#3577=CARTESIAN_POINT ( 'NONE',  ( 13.08605924474404425, 16.89445423263737567, 6.385784896790035248 ) ) ;
#3579=CARTESIAN_POINT ( 'NONE',  ( 2.134098633783316323, 19.31779869980666220, 1.050363145643365748 ) ) ;
#3582=CARTESIAN_POINT ( 'NONE',  ( 4.871060933462843856, 20.35131442480351183, 1.748582030751478111 ) ) ;
#3591=CARTESIAN_POINT ( 'NONE',  ( 11.22303388661927137, 15.74982258328167717, 6.891629373590611785 ) ) ;
#3592=CARTESIAN_POINT ( 'NONE',  ( 12.27006042634966931, 20.89186537925146325, -1.183231535759053710 ) ) ;
#3593=CARTESIAN_POINT ( 'NONE',  ( 4.880215608511783820, 20.21972024448168170, 0.5016143470315571617 ) ) ;
#3594=CARTESIAN_POINT ( 'NONE',  ( 11.14637220089711001, 12.02381550237932295, 5.878899239644039376 ) ) ;
#3600=CARTESIAN_POINT ( 'NONE',  ( 7.570358912651840910, 21.81389254086020202, 3.244435738127268376 ) ) ;
#3607=CARTESIAN_POINT ( 'NONE',  ( 3.634833444273914083, 19.07995194538682071, -0.6453590074123158882 ) ) ;
#3610=CARTESIAN_POINT ( 'NONE',  ( 7.548729492735156477, 15.22146907589735676, 8.284681895849521638 ) ) ;
#3616=ADVANCED_FACE ( 'NONE', ( #5114 ), #6144, .T. ) ;
#3634=CARTESIAN_POINT ( 'NONE',  ( 10.92369501690972200, 12.61980174807018251, 5.367099221840908818 ) ) ;
#3635=CARTESIAN_POINT ( 'NONE',  ( -0.1924500159166692703, 15.59650202059448354, -0.009168507438969686341 ) ) ;
#3641=CARTESIAN_POINT ( 'NONE',  ( 7.519266203142771943, 13.69322247944533189, -1.339971849629911782 ) ) ;
#3650=CARTESIAN_POINT ( 'NONE',  ( 2.344389418299225980, 20.87639896374770032, 6.272429502486324360 ) ) ;
#3652=CARTESIAN_POINT ( 'NONE',  ( 2.174318833424090602, 16.42212273390128985, -0.1944002137027950050 ) ) ;
#3657=CARTESIAN_POINT ( 'NONE',  ( 11.03612856729982816, 18.39344551543849704, -4.120841951098963563 ) ) ;
#3660=CARTESIAN_POINT ( 'NONE',  ( 13.07567957613725618, 18.69954703227123716, 6.688832392068873034 ) ) ;
#3665=CARTESIAN_POINT ( 'NONE',  ( 9.494052425882697932, 15.50413968533264963, 7.929839997388628881 ) ) ;
#3666=CARTESIAN_POINT ( 'NONE',  ( -0.6181405386100876642, 20.05178378372840342, 3.961315155216848183 ) ) ;
#3668=CARTESIAN_POINT ( 'NONE',  ( 5.899279335236281341, 18.34365586212437549, -0.9761941005625609513 ) ) ;
#3671=CARTESIAN_POINT ( 'NONE',  ( 1.286080621724394302, 20.22460181342998098, 3.469449174071038922 ) ) ;
#3674=CARTESIAN_POINT ( 'NONE',  ( 6.093765842861319726, 19.19176664446208136, -1.521969077160680861 ) ) ;
#3676=CARTESIAN_POINT ( 'NONE',  ( 0.7454037288853153642, 11.31615121391088152, 4.862722110801131592 ) ) ;
#3684=CARTESIAN_POINT ( 'NONE',  ( 9.028135976095729376, 21.80991532760212337, 1.508259505891954344 ) ) ;
#3688=CARTESIAN_POINT ( 'NONE',  ( 11.18059225887507324, 16.35212281796569656, -3.590113610534638067 ) ) ;
#3690=CARTESIAN_POINT ( 'NONE',  ( 1.780830151919097659, 17.97529088148248277, 0.2652343077119106995 ) ) ;
#3694=SHAPE_DEFINITION_REPRESENTATION ( #2425, #10883 ) ;
#3699=CARTESIAN_POINT ( 'NONE',  ( 6.323699694823708306, 11.70956187560891237, 2.868955871455586948 ) ) ;
#3702=CARTESIAN_POINT ( 'NONE',  ( 10.28015363549983263, 20.34374524028692122, 4.926689491331847748 ) ) ;
#3703=CARTESIAN_POINT ( 'NONE',  ( 8.215498187051487378, 11.48837196139402295, 1.847920089096604102 ) ) ;
#3704=CARTESIAN_POINT ( 'NONE',  ( 6.457449847458724967, 11.64278443974904320, 1.165535279167791316 ) ) ;
#3705=CARTESIAN_POINT ( 'NONE',  ( 7.525827410530302686, 21.81319771123894213, 3.257719107942246950 ) ) ;
#3710=CARTESIAN_POINT ( 'NONE',  ( 8.647929108115961938, 10.74346438930206027, 3.686466043081342736 ) ) ;
#3714=CARTESIAN_POINT ( 'NONE',  ( 9.303952506480500872, 14.60406769983332076, -2.545567318552978353 ) ) ;
#3715=PRODUCT_DEFINITION ( 'UNKNOWN', '', #12664, #10552 ) ;
#3717=CARTESIAN_POINT ( 'NONE',  ( 12.75852270247490949, 22.12259436858274242, 0.1659619235736507770 ) ) ;
#3718=CARTESIAN_POINT ( 'NONE',  ( 6.533579059798534594, 20.03265763155913959, 7.061703031544717568 ) ) ;
#3727=CARTESIAN_POINT ( 'NONE',  ( 0.04319471458505506206, 15.89914589079416807, 0.8258939165814165317 ) ) ;
#3731=CARTESIAN_POINT ( 'NONE',  ( 3.733140608333783916, 15.17434541625935651, -0.5071927740268031837 ) ) ;
#3735=CARTESIAN_POINT ( 'NONE',  ( 3.370024690280242208, 21.31626652883829465, 3.345821271410136077 ) ) ;
#3748=CARTESIAN_POINT ( 'NONE',  ( 12.16242873554583959, 20.88809130931168312, -1.148875002998984041 ) ) ;
#3749=CARTESIAN_POINT ( 'NONE',  ( 3.938429258113647968, 19.12622466589174053, -0.8127979641362345076 ) ) ;
#3752=CARTESIAN_POINT ( 'NONE',  ( 4.648553867220805991, 11.09625097007389094, 4.080894491436514393 ) ) ;
#3755=CARTESIAN_POINT ( 'NONE',  ( 7.796429656384849416, 12.28811609040251085, 0.04948816907226474826 ) ) ;
#3757=CARTESIAN_POINT ( 'NONE',  ( 3.338557919237726601, 13.67037593795628148, 7.539146506506522627 ) ) ;
#3762=CARTESIAN_POINT ( 'NONE',  ( 2.520972058354161049, 20.65036714207981206, 6.740181459500954375 ) ) ;
#3765=CARTESIAN_POINT ( 'NONE',  ( 0.8347132962655614552, 12.00400186595892293, 3.168484099998905901 ) ) ;
#3772=CARTESIAN_POINT ( 'NONE',  ( 9.192284307488497674, 19.28339334790884152, -2.815733911810373247 ) ) ;
#3774=CARTESIAN_POINT ( 'NONE',  ( 11.90889849114380716, 21.69093323893340397, 3.651447091914156395 ) ) ;
#3778=CARTESIAN_POINT ( 'NONE',  ( 9.496579142445281008, 15.25906563848011110, 7.888626892806992252 ) ) ;
#3779=CARTESIAN_POINT ( 'NONE',  ( -0.2797058817397305996, 20.30753595452681992, 4.828421465540532864 ) ) ;
#3781=CARTESIAN_POINT ( 'NONE',  ( 6.212096097470904965, 11.84283872956120121, 2.029147759238299376 ) ) ;
#3785=CARTESIAN_POINT ( 'NONE',  ( 9.500433685271497453, 18.52979832374122182, 7.486654841140969907 ) ) ;
#3786=CARTESIAN_POINT ( 'NONE',  ( 0.6580577011572460444, 20.32439072914841915, 1.809299870180519632 ) ) ;
#3787=CARTESIAN_POINT ( 'NONE',  ( 0.7837585588936004655, 20.18907768623580878, 7.715511287553819209 ) ) ;
#3796=CARTESIAN_POINT ( 'NONE',  ( 10.90717967712175351, 19.59065766869934322, 6.581256167405926227 ) ) ;
#3798=CARTESIAN_POINT ( 'NONE',  ( 11.16427926597950915, 16.07250702038418311, -3.584404996504540364 ) ) ;
#3801=CARTESIAN_POINT ( 'NONE',  ( 1.004559003390568472, 18.49730447209151762, 8.359447931242584673 ) ) ;
#3805=CARTESIAN_POINT ( 'NONE',  ( 4.409735924645852734, 19.51568168759821020, 0.5807916733966671519 ) ) ;
#3808=CARTESIAN_POINT ( 'NONE',  ( 7.513641844582591212, 14.65140826333467139, -1.943504412708490614 ) ) ;
#3809=CARTESIAN_POINT ( 'NONE',  ( 4.288245895386477713, 20.16661322485262531, 5.765686568166492165 ) ) ;
#3810=CARTESIAN_POINT ( 'NONE',  ( 10.72173680743496149, 11.64719608603622270, 3.872061749179875001 ) ) ;
#3811=CARTESIAN_POINT ( 'NONE',  ( 5.387809698622330501, 11.72601213311298274, 5.352900495692114902 ) ) ;
#3812=CARTESIAN_POINT ( 'NONE',  ( 11.10116566411557137, 18.39169315105245417, -4.135447224377957198 ) ) ;
#3820=CARTESIAN_POINT ( 'NONE',  ( 11.06727400676183670, 17.45221349387399812, 6.693287419277384132 ) ) ;
#3821=CARTESIAN_POINT ( 'NONE',  ( 11.56876908001934900, 20.24893436370382105, -3.130508153246869263 ) ) ;
#3824=CARTESIAN_POINT ( 'NONE',  ( 9.490928692825109536, 12.85459832499831201, -1.457268345192402226 ) ) ;
#3827=CARTESIAN_POINT ( 'NONE',  ( -1.187794103216660790, 20.48604666719226230, 3.371823117913468337 ) ) ;
#3830=CARTESIAN_POINT ( 'NONE',  ( 7.367551414186734426, 12.78932470803417765, 7.116237235135340455 ) ) ;
#3838=CARTESIAN_POINT ( 'NONE',  ( 1.881385393434782394, 15.19240802041391802, 0.2309439307633842919 ) ) ;
#3853=CARTESIAN_POINT ( 'NONE',  ( 11.91509809843844003, 11.13638386089868249, 0.7869662318407120161 ) ) ;
#3854=CARTESIAN_POINT ( 'NONE',  ( 3.508358100546943525, 15.44872671029758671, -1.459857323000175899 ) ) ;
#3857=CARTESIAN_POINT ( 'NONE',  ( 5.598674578815908909, 15.44076680689341607, 8.728037113477167708 ) ) ;
#3863=CARTESIAN_POINT ( 'NONE',  ( 8.009488492024781081, 19.38248615295674426, -1.109337938200560369 ) ) ;
#3865=CARTESIAN_POINT ( 'NONE',  ( 3.400495240568472077, 16.13495438657706771, 8.445061970360232095 ) ) ;
#3873=CARTESIAN_POINT ( 'NONE',  ( 1.555617767666469975, 21.18131178815229987, 4.150713132340920097 ) ) ;
#3876=CARTESIAN_POINT ( 'NONE',  ( 3.341345536767371005, 19.49937761787746382, 7.593489763050116359 ) ) ;
#3882=CARTESIAN_POINT ( 'NONE',  ( 10.85322530146255282, 18.36121671486396778, -3.976481845014243177 ) ) ;
#3884=CARTESIAN_POINT ( 'NONE',  ( 11.87485077258540933, 10.52519879175988038, 0.2400876501387014805 ) ) ;
#3888=CARTESIAN_POINT ( 'NONE',  ( 9.462450425703316625, 14.07471438502956218, 7.526408680303447341 ) ) ;
#3889=CARTESIAN_POINT ( 'NONE',  ( 3.215393543773535256, 17.96135795615357011, 8.214310353060460201 ) ) ;
#3892=CARTESIAN_POINT ( 'NONE',  ( 5.640316583454905164, 13.99766401133218174, -0.7584365737669227503 ) ) ;
#3895=CARTESIAN_POINT ( 'NONE',  ( 11.69298665771319357, 13.72201164258680173, 6.917504522580232518 ) ) ;
#3896=CARTESIAN_POINT ( 'NONE',  ( 4.780383433206969457, 11.98883979544040201, 4.693647510922787980 ) ) ;
#3897=CARTESIAN_POINT ( 'NONE',  ( 2.062732473717475035, 11.83352507831272149, 1.765483589054170244 ) ) ;
#3898=CARTESIAN_POINT ( 'NONE',  ( 0.1227838744961313316, 20.95892070510404182, 5.974958143557400625 ) ) ;
#3901=CARTESIAN_POINT ( 'NONE',  ( 3.918141522112466024, 12.81903963674880131, 0.8919207467421174096 ) ) ;
#3907=CARTESIAN_POINT ( 'NONE',  ( 11.32837441058685535, 13.16913511479088683, 6.657235606396362471 ) ) ;
#3910=CARTESIAN_POINT ( 'NONE',  ( 11.15056158858318902, 14.80538177552531742, -3.352690886573022055 ) ) ;
#3913=CARTESIAN_POINT ( 'NONE',  ( 0.9804779173902414824, 12.40032227216336125, 6.306356520460885129 ) ) ;
#3921=CARTESIAN_POINT ( 'NONE',  ( 10.20950810520924179, 20.26079639706886226, -1.226483415077589401 ) ) ;
#3922=CARTESIAN_POINT ( 'NONE',  ( 4.147649111953238155, 20.32216908442184078, 5.402681071153457637 ) ) ;
#3925=CARTESIAN_POINT ( 'NONE',  ( 5.895566845034227121, 14.03105527214651715, 7.837517794756466039 ) ) ;
#3932=CARTESIAN_POINT ( 'NONE',  ( 11.33996423452750335, 22.16594858500680232, 2.023480447774197444 ) ) ;
#3935=CARTESIAN_POINT ( 'NONE',  ( 9.319472022997786098, 16.19024704327322084, -2.854579263552438295 ) ) ;
#3938=CARTESIAN_POINT ( 'NONE',  ( 3.622151847267213398, 20.92444076583792167, 5.284828060340222677 ) ) ;
#3963=CARTESIAN_POINT ( 'NONE',  ( 3.627712153688075869, 17.35305612800781816, -1.455835595266307125 ) ) ;
#3966=CARTESIAN_POINT ( 'NONE',  ( 4.917538461146517825, 11.31976844172629271, 5.235219669757365857 ) ) ;
#3982=CARTESIAN_POINT ( 'NONE',  ( 3.426798112698273613, 17.95067475860813744, 8.948262651118973565 ) ) ;
#3984=CARTESIAN_POINT ( 'NONE',  ( 1.165675658960684258, 19.99706093811970220, 1.906448648540375324 ) ) ;
#3991=CARTESIAN_POINT ( 'NONE',  ( 11.85589261522914128, 21.52809012965692403, -1.417360321702582970 ) ) ;
#3993=CARTESIAN_POINT ( 'NONE',  ( 11.32652070754218698, 11.63326539784401170, -2.087448442563799134 ) ) ;
#3998=CARTESIAN_POINT ( 'NONE',  ( 7.482895972121536232, 12.31879885248479667, -1.218862190161812409 ) ) ;
#4000=CARTESIAN_POINT ( 'NONE',  ( 2.943417611999118666, 20.19995037221810108, 2.177142770243966741 ) ) ;
#4002=CARTESIAN_POINT ( 'NONE',  ( 5.677412915715525976, 13.63288455579914071, -0.5314653111491820514 ) ) ;
#4007=CARTESIAN_POINT ( 'NONE',  ( 9.728942020902382026, 11.81448552380872208, -1.613679459648534653 ) ) ;
#4008=CARTESIAN_POINT ( 'NONE',  ( -0.3522849415351315683, 21.11360319320700185, 4.780382278449337718 ) ) ;
#4009=CARTESIAN_POINT ( 'NONE',  ( 0.2729244852844739944, 20.85630707936518036, 6.375157578189681651 ) ) ;
#4012=CARTESIAN_POINT ( 'NONE',  ( 0.7458913913427336340, 12.12637795047220202, 4.864350555078584826 ) ) ;
#4017=CARTESIAN_POINT ( 'NONE',  ( 9.925807051316079210, 10.75363849649213144, 0.5961705298080919313 ) ) ;
#4023=CARTESIAN_POINT ( 'NONE',  ( 12.07662037374150188, 11.20872780036083149, 1.062083825547142091 ) ) ;
#4024=CARTESIAN_POINT ( 'NONE',  ( 5.369103247086697728, 15.71570224551708428, -2.120753809282792002 ) ) ;
#4026=CARTESIAN_POINT ( 'NONE',  ( 2.745045924436487983, 19.21529397045534182, 7.464326575930528840 ) ) ;
#4032=CARTESIAN_POINT ( 'NONE',  ( 9.207133947949060371, 21.14801334772412034, 1.738871791010894174 ) ) ;
#4034=CARTESIAN_POINT ( 'NONE',  ( 11.95356391707709243, 20.94917700551698303, 3.645593293397387136 ) ) ;
#4039=CARTESIAN_POINT ( 'NONE',  ( 11.22049204336262029, 14.97478453086299766, 6.637898145237717706 ) ) ;
#4040=CARTESIAN_POINT ( 'NONE',  ( 9.107295249990597696, 21.95697059135326512, 1.669600826508311320 ) ) ;
#4045=CARTESIAN_POINT ( 'NONE',  ( 9.431633194775894680, 13.20025053816172189, -1.758368973243622957 ) ) ;
#4048=CARTESIAN_POINT ( 'NONE',  ( 5.088084651243378609, 15.68947463651248420, 8.601854303313373862 ) ) ;
#4051=CARTESIAN_POINT ( 'NONE',  ( 7.156657753775511388, 11.88141511607538092, 6.132460277425193063 ) ) ;
#4057=CARTESIAN_POINT ( 'NONE',  ( 0.03417565917660739944, 14.83535024179863804, 1.090746620095099040 ) ) ;
#4061=CARTESIAN_POINT ( 'NONE',  ( 2.146289851715664998, 18.00879166459082370, 0.3733188029809513253 ) ) ;
#4062=CARTESIAN_POINT ( 'NONE',  ( 13.02203208521239652, 11.26511959538250096, 4.614517720664577105 ) ) ;
#4073=CARTESIAN_POINT ( 'NONE',  ( 3.279053066004760542, 11.89954130989696246, 6.881081710522694905 ) ) ;
#4076=CARTESIAN_POINT ( 'NONE',  ( 5.570283759808590140, 14.18670928006132215, 8.353561429919604819 ) ) ;
#4085=CARTESIAN_POINT ( 'NONE',  ( 3.010873720258615549, 19.62469427726395921, 7.998214828720064951 ) ) ;
#4087=CARTESIAN_POINT ( 'NONE',  ( 1.189115539264649524, 19.87555530259703929, 7.508218902050214361 ) ) ;
#4096=CARTESIAN_POINT ( 'NONE',  ( 8.681707164006697397, 21.55462128078298178, 1.846373227260097227 ) ) ;
#4100=CARTESIAN_POINT ( 'NONE',  ( 12.36232094770518408, 10.46176486781214088, 2.258949820783138218 ) ) ;
#4104=CARTESIAN_POINT ( 'NONE',  ( 7.762073279291525019, 19.65299917282199971, -1.873378395566488219 ) ) ;
#4105=CARTESIAN_POINT ( 'NONE',  ( 4.950627004242664775, 12.10224027996176233, 5.328968407580981115 ) ) ;
#4107=CARTESIAN_POINT ( 'NONE',  ( 5.587073591125067296, 15.32039277778152275, -1.277284589391624481 ) ) ;
#4110=CARTESIAN_POINT ( 'NONE',  ( 4.592488401674089005, 11.87781438748830531, 3.847380809352867193 ) ) ;
#4112=CARTESIAN_POINT ( 'NONE',  ( 6.831402082338472681, 20.09449018309318191, 7.036973853986666860 ) ) ;
#4115=CARTESIAN_POINT ( 'NONE',  ( 3.170692993479493182, 17.96108129601270775, 8.227029222725301238 ) ) ;
#4122=CARTESIAN_POINT ( 'NONE',  ( 11.36994341220144022, 13.54146173944704579, 6.880576314206986233 ) ) ;
#4125=CARTESIAN_POINT ( 'NONE',  ( 5.510835403679958056, 13.03497559724449850, -1.051663230879403166 ) ) ;
#4130=CARTESIAN_POINT ( 'NONE',  ( 5.545311189636909610, 20.74516219335661660, 3.520903296636215707 ) ) ;
#4135=CARTESIAN_POINT ( 'NONE',  ( 5.901462123111614666, 12.70293317459338134, 0.1691424549115569387 ) ) ;
#4137=CARTESIAN_POINT ( 'NONE',  ( 9.693733691225084215, 18.90712183571880090, -2.322483269049387733 ) ) ;
#4143=CARTESIAN_POINT ( 'NONE',  ( 5.450687119353768928, 17.48300910350427628, 8.674115758454949088 ) ) ;
#4148=CARTESIAN_POINT ( 'NONE',  ( 9.136086461789291846, 18.56746232396120533, 7.683010205099245482 ) ) ;
#4151=CARTESIAN_POINT ( 'NONE',  ( 9.371701772490553140, 16.88370700927627155, -2.834813229451389027 ) ) ;
#4153=CARTESIAN_POINT ( 'NONE',  ( 0.2090372314103253748, 20.09402757005803153, 6.163100425531474080 ) ) ;
#4154=CARTESIAN_POINT ( 'NONE',  ( 4.037559778546858880, 20.21972024448168170, 0.7539604779301642967 ) ) ;
#4166=CARTESIAN_POINT ( 'NONE',  ( 9.235757461302830151, 17.37326356681460382, -3.689043915829297582 ) ) ;
#4176=CARTESIAN_POINT ( 'NONE',  ( 5.003479159263154230, 21.41895532286982018, 1.986973093797242074 ) ) ;
#4179=CARTESIAN_POINT ( 'NONE',  ( 3.620832965735171438, 17.22857179101344016, -1.359620387843638367 ) ) ;
#4183=CARTESIAN_POINT ( 'NONE',  ( 1.255127740655926250, 12.99292128794711232, 7.191113729468309401 ) ) ;
#4192=CARTESIAN_POINT ( 'NONE',  ( 2.471328934078918849, 11.32048519468527203, 3.459614447656988112 ) ) ;
#4194=CARTESIAN_POINT ( 'NONE',  ( 1.614653659784055284, 18.72099911278871787, 8.534676711928359083 ) ) ;
#4196=CARTESIAN_POINT ( 'NONE',  ( 13.20954647625931777, 22.11403031342653591, 1.997722137595396852 ) ) ;
#4202=CARTESIAN_POINT ( 'NONE',  ( 12.44599801692499241, 11.60770318476056140, 4.553026975270451970 ) ) ;
#4205=CARTESIAN_POINT ( 'NONE',  ( 12.07372255579661946, 10.41170888677670270, 1.064424525701137103 ) ) ;
#4210=CARTESIAN_POINT ( 'NONE',  ( 7.389527843533306495, 12.82742614983489737, -1.666067054070730302 ) ) ;
#4213=CARTESIAN_POINT ( 'NONE',  ( 6.633674063341000071, 20.34825906491803238, 0.8060356396175938354 ) ) ;
#4214=CARTESIAN_POINT ( 'NONE',  ( 7.322682645118421263, 14.91079802554269307, 7.412562723462624348 ) ) ;
#4218=CARTESIAN_POINT ( 'NONE',  ( 13.21515623208546764, 11.34183091107056107, 4.504288056618959146 ) ) ;
#4221=CARTESIAN_POINT ( 'NONE',  ( 5.559603178726561623, 13.84461567157916662, 8.313571739785118098 ) ) ;
#4222=CARTESIAN_POINT ( 'NONE',  ( -0.1072886869958045164, 21.03162608686091062, 5.359064832216835939 ) ) ;
#4225=CARTESIAN_POINT ( 'NONE',  ( 6.982204062069592432, 12.34291428558256065, 5.600203218024798701 ) ) ;
#4232=CARTESIAN_POINT ( 'NONE',  ( 11.18085364544609384, 12.25195592965612690, 5.936477548793301473 ) ) ;
#4236=CARTESIAN_POINT ( 'NONE',  ( 5.445077015079114346, 13.57693074510927289, -1.403816391461112589 ) ) ;
#4246=CARTESIAN_POINT ( 'NONE',  ( 11.22474155257526007, 14.44257473674272241, -3.359826663698572080 ) ) ;
#4250=CARTESIAN_POINT ( 'NONE',  ( 10.71187475869725247, 21.11843953786754113, 0.2883095389576884049 ) ) ;
#4254=CARTESIAN_POINT ( 'NONE',  ( 3.288597934804766698, 21.28193718814916480, 3.125135824630198567 ) ) ;
#4260=CARTESIAN_POINT ( 'NONE',  ( 12.40139705607254861, 19.98821005853033483, 4.883289743443808284 ) ) ;
#4262=CARTESIAN_POINT ( 'NONE',  ( 1.363855527533811562, 17.01011102508672224, 8.799023506260708061 ) ) ;
#4264=CARTESIAN_POINT ( 'NONE',  ( 1.363973292582373320, 16.43321537790008335, -0.2831975433082900562 ) ) ;
#4275=CARTESIAN_POINT ( 'NONE',  ( 0.4312365985166283777, 18.52905954593687454, 1.381589547113361460 ) ) ;
#4292=CARTESIAN_POINT ( 'NONE',  ( 7.293525192738406382, 18.51518438473548045, 8.055948870987359456 ) ) ;
#4295=CARTESIAN_POINT ( 'NONE',  ( 3.587117570992901960, 13.66083647730730277, -0.6928666555306400854 ) ) ;
#4308=CARTESIAN_POINT ( 'NONE',  ( 2.122429293774134251, 11.85923521650776280, 1.930479901139369403 ) ) ;
#4317=CARTESIAN_POINT ( 'NONE',  ( 8.572546314900550968, 11.84307591169006102, 5.427209531905369033 ) ) ;
#4320=CARTESIAN_POINT ( 'NONE',  ( 13.37977302674483226, 14.47986448106203206, 6.886294595076251746 ) ) ;
#4326=CARTESIAN_POINT ( 'NONE',  ( 7.324677171929614872, 13.28816258335607081, -1.995452644984494261 ) ) ;
#4327=CARTESIAN_POINT ( 'NONE',  ( 4.264170397703306747, 12.02909395710813989, 2.247622554162475694 ) ) ;
#4328=CARTESIAN_POINT ( 'NONE',  ( 6.422875249409071508, 19.96740888111275680, 0.2665559906438186299 ) ) ;
#4332=CARTESIAN_POINT ( 'NONE',  ( 6.866916592308192513, 11.04801462030960124, 4.445165589993000488 ) ) ;
#4334=CARTESIAN_POINT ( 'NONE',  ( 13.61076747458670866, 21.46618676209390841, 1.782491636468937379 ) ) ;
#4336=CARTESIAN_POINT ( 'NONE',  ( 4.569264072537790433, 10.97102203747262195, 3.822939839603590961 ) ) ;
#4337=CARTESIAN_POINT ( 'NONE',  ( 1.470004468695772726, 12.67845410451087673, 8.026080939803462044 ) ) ;
#4339=CARTESIAN_POINT ( 'NONE',  ( 7.324228559365892899, 14.94885212140055408, 7.531391849507111047 ) ) ;
#4347=CARTESIAN_POINT ( 'NONE',  ( 9.812260450953351310, 10.90820011318799132, 0.1177049192506583880 ) ) ;
#4351=CARTESIAN_POINT ( 'NONE',  ( 5.607071462432890563, 12.48575941491167107, -0.5813519368072119775 ) ) ;
#4356=CARTESIAN_POINT ( 'NONE',  ( 5.571415501051473207, 20.74427618698123510, 3.589970083868847528 ) ) ;
#4360=CARTESIAN_POINT ( 'NONE',  ( 7.721407704011980400, 16.36585256730476701, -2.399376772047163708 ) ) ;
#4365=CARTESIAN_POINT ( 'NONE',  ( 3.207890707543083586, 21.23115320172808040, 2.906853089031384840 ) ) ;
#4373=CARTESIAN_POINT ( 'NONE',  ( 11.55108798147146310, 21.17147518458597943, 2.638599769568476194 ) ) ;
#4377=CARTESIAN_POINT ( 'NONE',  ( 1.448403523286458494, 16.16488452566092349, 8.848146419262569395 ) ) ;
#4381=CARTESIAN_POINT ( 'NONE',  ( 4.859321299514149928, 12.65090407144326257, 7.048876997207147888 ) ) ;
#4391=CARTESIAN_POINT ( 'NONE',  ( 9.347939006732550737, 17.21989818313373988, -2.888331931755111714 ) ) ;
#4393=APPLICATION_CONTEXT ( 'automotive_design' ) ;
#4406=CARTESIAN_POINT ( 'NONE',  ( 1.170218911684995478, 11.63698894629814085, 6.546186411866827370 ) ) ;
#4409=CARTESIAN_POINT ( 'NONE',  ( 4.083167597562495033, 19.59760028129526788, -0.3681794837021826194 ) ) ;
#4413=CARTESIAN_POINT ( 'NONE',  ( 1.062191812101273003, 12.47827038174564684, 6.250278051991300821 ) ) ;
#4421=CARTESIAN_POINT ( 'NONE',  ( 3.517454366401044918, 13.17929039423700743, 8.136532573000508251 ) ) ;
#4431=CARTESIAN_POINT ( 'NONE',  ( 10.40657903342879997, 11.56703545653052068, 4.000892017491787911 ) ) ;
#4434=CARTESIAN_POINT ( 'NONE',  ( 11.85443195533146010, 20.90808010024898067, -2.310623319762369121 ) ) ;
#4439=CARTESIAN_POINT ( 'NONE',  ( 7.947508136585422100, 20.23276147138264491, -1.405158123477003418 ) ) ;
#4440=CARTESIAN_POINT ( 'NONE',  ( 6.703263711442990491, 20.44835075257027412, 0.9868673461823399551 ) ) ;
#4441=CARTESIAN_POINT ( 'NONE',  ( 6.676020821304478936, 11.81234876462786687, 4.091397116453036276 ) ) ;
#4443=CARTESIAN_POINT ( 'NONE',  ( 7.812630522065525440, 11.33951387506710162, -0.1560246795265585462 ) ) ;
#4447=CARTESIAN_POINT ( 'NONE',  ( 7.496365336133834489, 16.64380874522678155, 8.500741285933822056 ) ) ;
#4448=CARTESIAN_POINT ( 'NONE',  ( 1.627952902251037060, 13.66371438389476189, 8.848553374140269767 ) ) ;
#4451=CARTESIAN_POINT ( 'NONE',  ( 2.463800489352728995, 20.09148914161242061, 6.261814795623706686 ) ) ;
#4457=CARTESIAN_POINT ( 'NONE',  ( 9.081081133818898365, 14.53291942956394145, -3.329645429468344187 ) ) ;
#4460=CARTESIAN_POINT ( 'NONE',  ( 5.667851893490138515, 18.56944215186095803, -1.718953128397392671 ) ) ;
#4462=CARTESIAN_POINT ( 'NONE',  ( 4.441799159996215884, 19.87391983916490190, 6.423165949441382416 ) ) ;
#4468=CARTESIAN_POINT ( 'NONE',  ( 5.888305848254707264, 13.94198686298930134, -1.024452031420564957 ) ) ;
#4469=CARTESIAN_POINT ( 'NONE',  ( 7.129426711373165304, 20.03265763155913959, 6.883267371180108007 ) ) ;
#4479=CARTESIAN_POINT ( 'NONE',  ( 11.38971108731577608, 21.23201434281770261, 2.202812224794820306 ) ) ;
#4481=CARTESIAN_POINT ( 'NONE',  ( 1.434811090846531023, 16.35893803067423136, 8.856001068397819864 ) ) ;
#4485=( LENGTH_UNIT ( ) NAMED_UNIT ( * ) SI_UNIT ( .MILLI., .METRE. ) );
#4491=CARTESIAN_POINT ( 'NONE',  ( 12.77710113932175062, 11.94611577877984132, 4.222729064079776329 ) ) ;
#4492=CARTESIAN_POINT ( 'NONE',  ( 2.369555810156617426, 18.89992366948760250, 0.8526494300588405295 ) ) ;
#4493=CARTESIAN_POINT ( 'NONE',  ( 11.64042750901279533, 20.25175440475918265, -3.155339158323879012 ) ) ;
#4504=CARTESIAN_POINT ( 'NONE',  ( 1.989525294996288496, 11.82982598436980126, 1.785142876290339853 ) ) ;
#4507=CARTESIAN_POINT ( 'NONE',  ( 4.204571555674638361, 19.96231018478896146, -0.06522048258607304749 ) ) ;
#4519=CARTESIAN_POINT ( 'NONE',  ( 2.884421797144688160, 11.35064653914199262, 5.241908264952396479 ) ) ;
#4528=CARTESIAN_POINT ( 'NONE',  ( 8.941343084498610594, 15.40389167150912009, -2.864627239135745462 ) ) ;
#4531=CARTESIAN_POINT ( 'NONE',  ( 10.92162063437064923, 15.44784284617675674, -4.283584550483333864 ) ) ;
#4536=CARTESIAN_POINT ( 'NONE',  ( 6.309743394496731383, 19.72050476477846459, -0.01792138457645678709 ) ) ;
#4540=CARTESIAN_POINT ( 'NONE',  ( 3.324034007969909332, 16.94026534804002537, 8.402710725375246881 ) ) ;
#4545=CARTESIAN_POINT ( 'NONE',  ( 0.3942685348548155000, 11.70427427261698128, 3.243497937280782839 ) ) ;
#4548=CARTESIAN_POINT ( 'NONE',  ( 0.5010645890953140391, 18.57485916386803382, 1.285821070430232860 ) ) ;
#4554=CARTESIAN_POINT ( 'NONE',  ( 5.241325608820580406, 15.44426253303012508, -2.166424616879202958 ) ) ;
#4556=CARTESIAN_POINT ( 'NONE',  ( 10.55427167348027595, 21.69986197937489081, -0.09835946977028746374 ) ) ;
#4558=B_SPLINE_SURFACE_WITH_KNOTS ( 'NONE', 3, 3, ( 
 ( #18092, #17877, #1376, #6357, #19842, #8018, #3054, #19526, #2831, #19950, #1275, #11229, #4716, #6032, #14899, #3153, #18203, #17979, #19623, #2723, #7696, #9778, #21174, #16545, #9880, #6247, #14788, #11556, #21288, #2949, #14687, #9565, #7801, #12804, #14576, #4824, #9457, #8119, #21618, #11456, #16228, #6477, #4391, #13129, #11125, #16445, #9677, #13241, #949, #14457, #1055, #6146, #12914, #4491, #7912, #16335, #11342, #1172, #21394, #13019, #19725, #4598, #11663, #15111, #3378, #20046, #17075 ),
 ( #5230, #13663, #15436, #5027, #1699, #16646, #1492, #15331, #8238, #11779, #8440, #1810, #15212, #12109, #16961, #264, #42, #11883, #18398, #1918, #155, #20364, #8555, #18719, #13344, #18510, #13772, #6899, #10109, #11991, #3702, #5132, #18832, #3591, #20476, #21830, #6682, #8663, #10330, #7005, #15012, #3274, #5345, #21728, #6580, #16856, #4917, #1599, #10006, #16760, #18612, #8341, #13444, #20152, #6794, #13552, #3478, #20260, #10214, #9095, #13895, #19276, #2255, #7565, #7343, #17625, #15543 ),
 ( #820, #7246, #5453, #17182, #4135, #8764, #10876, #5892, #15772, #2368, #21045, #8881, #12442, #8993, #5561, #17290, #375, #2138, #14327, #18937, #2477, #9206, #7447, #3808, #15990, #7127, #10776, #20595, #4032, #19169, #12653, #19381, #10443, #5797, #17519, #2021, #12217, #17415, #10544, #20812, #15874, #15664, #596, #491, #3921, #14004, #20706, #19045, #12319, #10666, #14109, #5679, #700, #20939, #14221, #3027, #14539, #11201, #4246, #10984, #2917, #17741, #21260, #17952, #11308, #2802, #21583 ),
 ( #11098, #9429, #14657, #21467, #1248, #4468, #7668, #1026, #7988, #21364, #6115, #9535, #19808, #12992, #13098, #21144, #1141, #12882, #19601, #5997, #16095, #9647, #13209, #6442, #4360, #16200, #16306, #9750, #925, #4683, #7882, #6220, #2697, #16414, #2589, #16513, #1345, #9322, #12770, #14429, #19697, #14865, #17851, #19494, #7772, #4570, #18057, #14761, #6325, #11426, #18173, #8090, #3560, #10300, #19919, #17045, #15303, #14983, #3126, #5109, #15185, #21696, #20338, #18585, #16929, #11858, #126 ),
 ( #8314, #3354, #13638, #6763, #6878, #6552, #16828, #15084, #6649, #13315, #9849, #3451, #6979, #15413, #20019, #9974, #13412, #18689, #16618, #5207, #1669, #4994, #18368, #10184, #240, #1892, #8637, #4792, #4889, #11525, #8407, #18267, #11633, #1461, #1573, #11, #21797, #10083, #13527, #3238, #8209, #1778, #16732, #20120, #11751, #18483, #11962, #20234, #8523, #20788, #13979, #10850, #20905, #20677, #9180, #5313, #17388, #5771, #12294, #14194, #7094, #2111, #347, #15518, #15847, #574, #18804 ),
 ( #15961, #675, #13861, #2337, #17159, #20565, #2453, #10635, #3674, #19250, #12525, #8852, #5536, #792, #3785, #10417, #13746, #12413, #17265, #20443, #467, #7319, #12077, #14080, #1999, #5425, #10518, #12190, #19019, #2229, #18914, #15635, #8966, #7219, #3895, #15745, #7421, #5653, #19141, #4007, #10748, #17493, #9072, #19350, #1519, #11584, #19974, #21228, #8263, #6504, #4845, #14928, #9911, #4218, #9404, #4940, #8148, #17827, #18320, #16784, #17927, #3300, #21643, #11691, #5968, #19461, #21750 ),
 ( #7642, #4332, #16173, #6604, #10958, #15036, #11175, #14510, #12738, #3178, #10034, #13367, #20074, #7540, #16070, #21020, #3080, #18431, #14403, #5867, #11073, #4443, #2672, #19577, #9802, #901, #14303, #13267, #12628, #17711, #2561, #9294, #16677, #21117, #998, #7747, #6084, #12857, #16569, #1405, #5591, #2285, #4166, #9351, #10908, #17774, #9024, #5713, #20843, #12473, #2621, #2506, #19197, #4062, #2401, #849, #10804, #14459, #14355, #5920, #12685, #4493, #21730, #8020, #1057, #16649, #9884 ),
 ( #20050, #13243, #18094, #7804, #21502, #3057, #15013, #1279, #6585, #4601, #6148, #9566, #19729, #14578, #11560, #2725, #6359, #21289, #21620, #8121, #1495, #21396, #2954, #11128, #17878, #9781, #9460, #6250, #9679, #18205, #16448, #13346, #11460, #8241, #14792, #13133, #12916, #16337, #19844, #16229, #11231, #19626, #19954, #17980, #11345, #13021, #4720, #16547, #2833, #1176, #4826, #14903, #1380, #6480, #7916, #14690, #18298, #3155, #1922, #5135, #8344, #1705, #8667, #15335, #15216, #10219, #20479 ),
 ( #1814, #45, #13558, #6688, #16763, #10335, #13901, #380, #5031, #16859, #20263, #3705, #1602, #5350, #8558, #11887, #3381, #17079, #7131, #10446, #17184, #4920, #13447, #18401, #160, #15549, #11782, #3276, #8445, #6903, #6798, #16965, #13667, #20155, #11665, #3594, #2024, #8767, #10010, #15116, #267, #21833, #18514, #11995, #18615, #10113, #12112, #3481, #20368, #5233, #15439, #18837, #7009, #13776, #14008, #8998, #7249, #497, #822, #7451, #3812, #5565, #5682, #2371, #928, #7569, #20710 ) ),
 .UNSPECIFIED., .F., .F., .F.,
 ( 4, 1, 1, 1, 1, 1, 4 ),
 ( 4, 1, 1, 1, 1, 1, 1, 1, 1, 1, 1, 1, 1, 1, 1, 1, 1, 1, 1, 1, 1, 1, 1, 1, 1, 1, 1, 1, 1, 1, 1, 1, 1, 1, 1, 1, 1, 1, 1, 1, 1, 1, 1, 1, 1, 1, 1, 1, 1, 1, 1, 1, 1, 1, 1, 1, 1, 1, 1, 1, 1, 1, 1, 1, 4 ),
 ( -0.01121212662510000062, 0.000000000000000000, 0.1250000000000000000, 0.2500000000000000000, 0.3750000000000000000, 0.5000000000000000000, 0.5112121266250999607 ),
 ( -0.02000000000000000042, -0.003749999999999999861, 0.01250000000000000069, 0.02875000000000000125, 0.04499999999999999833, 0.06124999999999999889, 0.07749999999999999944, 0.09375000000000000000, 0.1100000000000000006, 0.1262500000000000011, 0.1424999999999999878, 0.1587500000000000022, 0.1749999999999999889, 0.1912500000000000033, 0.2074999999999999900, 0.2237500000000000044, 0.2399999999999999911, 0.2562499999999999778, 0.2725000000000000200, 0.2887500000000000067, 0.3049999999999999933, 0.3212499999999999800, 0.3375000000000000222, 0.3537500000000000089, 0.3699999999999999956, 0.3862499999999999822, 0.4025000000000000244, 0.4187500000000000111, 0.4349999999999999978, 0.4512499999999999845, 0.4675000000000000266, 0.4837500000000000133, 0.5000000000000000000, 0.5162499999999999867, 0.5324999999999999734, 0.5487499999999999600, 0.5649999999999999467, 0.5812500000000000444, 0.5975000000000000311, 0.6137500000000000178, 0.6300000000000000044, 0.6462499999999999911, 0.6624999999999999778, 0.6787499999999999645, 0.6949999999999999512, 0.7112500000000000488, 0.7275000000000000355, 0.7437500000000000222, 0.7600000000000000089, 0.7762499999999999956, 0.7924999999999999822, 0.8087499999999999689, 0.8249999999999999556, 0.8412500000000000533, 0.8575000000000000400, 0.8737500000000000266, 0.8900000000000000133, 0.9062500000000000000, 0.9224999999999999867, 0.9387499999999999734, 0.9549999999999999600, 0.9712499999999999467, 0.9875000000000000444, 1.003749999999999920, 1.020000000000000018 ),
 .UNSPECIFIED. ) ;
#4560=CARTESIAN_POINT ( 'NONE',  ( 8.305577890988885770, 21.07935306927017294, 5.301748380739248034 ) ) ;
#4562=CARTESIAN_POINT ( 'NONE',  ( 1.342236859452698328, 13.15608644122636228, 7.515139044313254857 ) ) ;
#4565=CARTESIAN_POINT ( 'NONE',  ( 6.748805940682723659, 19.22513578221937891, 6.619665475902611007 ) ) ;
#4570=CARTESIAN_POINT ( 'NONE',  ( 10.97561116649450241, 21.20110815220486344, 0.1820916674951629788 ) ) ;
#4573=CARTESIAN_POINT ( 'NONE',  ( 0.4623469015994441933, 11.62092872259188070, 3.129209433992582223 ) ) ;
#4576=CARTESIAN_POINT ( 'NONE',  ( 6.763134108677117950, 11.26290425026184217, 2.704746052809542611 ) ) ;
#4585=CARTESIAN_POINT ( 'NONE',  ( 10.69489229547795972, 21.01502399469208271, 0.3287616349347236011 ) ) ;
#4598=CARTESIAN_POINT ( 'NONE',  ( 11.69919614587864132, 19.71652463870320204, -2.532988136784334099 ) ) ;
#4599=CARTESIAN_POINT ( 'NONE',  ( 2.473378706908319291, 19.20449835410846617, 1.096051056300948900 ) ) ;
#4601=CARTESIAN_POINT ( 'NONE',  ( 6.247691938729453831, 20.69450185495974281, -0.2536055519876236342 ) ) ;
#4612=CARTESIAN_POINT ( 'NONE',  ( 6.759686242205972029, 20.09752422452572418, 7.061613146868085167 ) ) ;
#4615=CARTESIAN_POINT ( 'NONE',  ( 3.511489924716158395, 15.15732606925634762, -1.285905515786881947 ) ) ;
#4621=CARTESIAN_POINT ( 'NONE',  ( 2.356492409553436751, 12.28457074719288755, 2.882335299874351886 ) ) ;
#4623=CARTESIAN_POINT ( 'NONE',  ( 4.035585374492060673, 12.61491249240588530, 1.301411686255661726 ) ) ;
#4628=CARTESIAN_POINT ( 'NONE',  ( 3.428905286597181856, 12.67427477258878810, 7.691402442796377414 ) ) ;
#4640=CARTESIAN_POINT ( 'NONE',  ( 8.218929569428507165, 20.70901284984930157, 0.2465254262590220458 ) ) ;
#4641=FACE_OUTER_BOUND ( 'NONE', #11685, .T. ) ;
#4642=CARTESIAN_POINT ( 'NONE',  ( 10.94240633158067411, 14.34350891603136091, -4.001608750109906687 ) ) ;
#4649=CARTESIAN_POINT ( 'NONE',  ( 8.109733825337782420, 20.49485801409760199, 4.711921892921808741 ) ) ;
#4650=CARTESIAN_POINT ( 'NONE',  ( 6.949628868194021258, 12.30010770274149046, 5.335163355835638832 ) ) ;
#4654=CARTESIAN_POINT ( 'NONE',  ( 13.75689827559843970, 21.65865639734760251, 1.766977752662861390 ) ) ;
#4656=CARTESIAN_POINT ( 'NONE',  ( 5.550539117013853385, 13.84493627167355179, 8.315640499742142921 ) ) ;
#4657=CARTESIAN_POINT ( 'NONE',  ( 1.482627815308283026, 12.73650106816228700, 8.087698260707639974 ) ) ;
#4660=CARTESIAN_POINT ( 'NONE',  ( 0.5452244933112915248, 12.38707500932596162, 3.405961392030337542 ) ) ;
#4671=CARTESIAN_POINT ( 'NONE',  ( 13.58729491768447417, 22.20239475586336297, 2.426319669798093326 ) ) ;
#4672=CARTESIAN_POINT ( 'NONE',  ( 9.410645419839852366, 11.94156677812711287, -1.622654999013667609 ) ) ;
#4675=CARTESIAN_POINT ( 'NONE',  ( 8.797223678989327666, 20.03400673711370672, 6.593457860109054103 ) ) ;
#4678=CARTESIAN_POINT ( 'NONE',  ( 1.089122662289458976, 12.39630382929348151, 6.275382864778182856 ) ) ;
#4683=CARTESIAN_POINT ( 'NONE',  ( 10.03171560225656478, 21.13787900135836395, 3.342723603854336645 ) ) ;
#4684=CARTESIAN_POINT ( 'NONE',  ( 4.972972795178391081, 18.58281789573423026, 7.435623437359064170 ) ) ;
#4685=CARTESIAN_POINT ( 'NONE',  ( 3.122592833242820554, 20.84690199368946040, 1.788550936533952251 ) ) ;
#4690=CARTESIAN_POINT ( 'NONE',  ( 6.651328749655917250, 11.03939126535642146, 2.721905128854394285 ) ) ;
#4698=CARTESIAN_POINT ( 'NONE',  ( 10.95239689897913316, 12.51241342390697753, 5.072527772439351601 ) ) ;
#4702=CARTESIAN_POINT ( 'NONE',  ( 9.558959319209352046, 18.22385816987663176, -2.518794820452257444 ) ) ;
#4706=CARTESIAN_POINT ( 'NONE',  ( 6.649638745689235186, 12.00122113815488056, 5.925618445732687256 ) ) ;
#4710=CARTESIAN_POINT ( 'NONE',  ( 3.934324214432870281, 17.71509372232019075, -0.4743072054864678755 ) ) ;
#4716=CARTESIAN_POINT ( 'NONE',  ( 8.089493120333704823, 20.59481639511846041, 4.745424403458926577 ) ) ;
#4717=CARTESIAN_POINT ( 'NONE',  ( 2.901177870377362744, 20.07788797494241706, 2.155083431282422080 ) ) ;
#4720=CARTESIAN_POINT ( 'NONE',  ( 11.30433373149261556, 22.16594858500680232, 2.034150544939726135 ) ) ;
#4730=CARTESIAN_POINT ( 'NONE',  ( 3.389842854487740365, 15.44796252803982206, -1.429507839081749720 ) ) ;
#4733=CARTESIAN_POINT ( 'NONE',  ( 5.431705152844418016, 21.53778799175918124, 3.212981151218359255 ) ) ;
#4737=CARTESIAN_POINT ( 'NONE',  ( 1.083593175512994611, 12.51931675915923137, 6.352092480932011398 ) ) ;
#4746=CARTESIAN_POINT ( 'NONE',  ( 1.893820563527240486, 18.08758566162994086, -0.4124606427257835328 ) ) ;
#4755=CARTESIAN_POINT ( 'NONE',  ( 10.60300064863796976, 14.29921781272587289, -3.573945592432405061 ) ) ;
#4761=CARTESIAN_POINT ( 'NONE',  ( 9.203126350871984940, 16.69853532098021986, 7.213164781469691533 ) ) ;
#4763=CARTESIAN_POINT ( 'NONE',  ( 6.541934835182226848, 11.72101710144985276, 3.494563511944335232 ) ) ;
#4767=CARTESIAN_POINT ( 'NONE',  ( 3.405894365792090817, 21.44911200421750053, 3.521272260944334764 ) ) ;
#4768=CARTESIAN_POINT ( 'NONE',  ( 1.311185941550153222, 12.10675315277394759, 7.278560453910660755 ) ) ;
#4773=CARTESIAN_POINT ( 'NONE',  ( 5.184979831338328182, 12.95168332381294185, 6.668061790751404594 ) ) ;
#4780=CARTESIAN_POINT ( 'NONE',  ( 8.943237316433746642, 15.28165795756530265, -3.613428226286483191 ) ) ;
#4782=CARTESIAN_POINT ( 'NONE',  ( 9.219739506579587740, 12.92579275786359716, -2.519071767018113750 ) ) ;
#4784=CARTESIAN_POINT ( 'NONE',  ( 8.663904165564538573, 20.38058929159417687, 6.250049521530280039 ) ) ;
#4786=CARTESIAN_POINT ( 'NONE',  ( 3.923274285735534939, 20.52844081774288298, 5.086198801183424933 ) ) ;
#4787=CARTESIAN_POINT ( 'NONE',  ( 6.349023019544413060, 11.72897180233325187, 2.639096833093112604 ) ) ;
#4792=CARTESIAN_POINT ( 'NONE',  ( 8.896463448791882556, 20.99150983053873887, -0.1081733280006275666 ) ) ;
#4793=CARTESIAN_POINT ( 'NONE',  ( 5.334080576704635313, 14.09280588451894012, 7.447742775086575229 ) ) ;
#4796=CARTESIAN_POINT ( 'NONE',  ( -0.6273374921548363625, 20.81272068207762516, 3.698821178046660219 ) ) ;
#4809=CARTESIAN_POINT ( 'NONE',  ( 13.04945465967934837, 13.27366431607636699, 5.426863059856754212 ) ) ;
#4813=CARTESIAN_POINT ( 'NONE',  ( 0.1476213763842004201, 12.30129727290108121, 3.491265826091432878 ) ) ;
#4818=CARTESIAN_POINT ( 'NONE',  ( 4.087777094530046007, 18.47353267629715035, -0.1674047009188593116 ) ) ;
#4824=CARTESIAN_POINT ( 'NONE',  ( 10.98836716658659718, 12.61615142531242206, 5.351275285785762392 ) ) ;
#4826=CARTESIAN_POINT ( 'NONE',  ( 13.34863692440958793, 16.76855268369192586, 7.282520765264200335 ) ) ;
#4830=CARTESIAN_POINT ( 'NONE',  ( 10.29169076519744586, 20.23694724301938663, 4.892464605147674561 ) ) ;
#4831=CARTESIAN_POINT ( 'NONE',  ( 11.49851465602529821, 15.66517251583919901, 7.649551592746075102 ) ) ;
#4836=CARTESIAN_POINT ( 'NONE',  ( 1.507113407974402630, 17.33792227738861058, 9.643085118255577015 ) ) ;
#4839=CARTESIAN_POINT ( 'NONE',  ( 6.826301903410996630, 20.01283248996876196, 6.955117793078509081 ) ) ;
#4845=CARTESIAN_POINT ( 'NONE',  ( 13.63939561152206004, 16.76121402582646880, 7.104551226395147800 ) ) ;
#4849=CARTESIAN_POINT ( 'NONE',  ( 1.716548453638899963, 16.68013709720543503, -0.6901774513339551387 ) ) ;
#4857=CARTESIAN_POINT ( 'NONE',  ( 8.647516245636284182, 12.11223639541018215, 5.228518803211497534 ) ) ;
#4864=CARTESIAN_POINT ( 'NONE',  ( 9.274122820243968945, 15.20243951512090597, 7.097396118508335405 ) ) ;
#4867=CARTESIAN_POINT ( 'NONE',  ( 3.648350219661197436, 14.72343274211524644, 9.065328312466423455 ) ) ;
#4868=CARTESIAN_POINT ( 'NONE',  ( 0.08586711205702327043, 12.50995321353708079, 1.839738799454192275 ) ) ;
#4871=CARTESIAN_POINT ( 'NONE',  ( 5.460367653841071700, 14.21946822237472752, 7.588426468924110324 ) ) ;
#4876=CARTESIAN_POINT ( 'NONE',  ( 10.82391557466618792, 14.15586088870902515, -4.040410652065021146 ) ) ;
#4878=CARTESIAN_POINT ( 'NONE',  ( 9.501351411502088951, 19.27355507002826229, -2.869603047228580728 ) ) ;
#4880=CARTESIAN_POINT ( 'NONE',  ( 9.179518564026135863, 18.59391849750369374, 7.516351665735313325 ) ) ;
#4889=CARTESIAN_POINT ( 'NONE',  ( 9.524362993972204094, 21.55462128078298178, 1.594027096361315232 ) ) ;
#4890=CARTESIAN_POINT ( 'NONE',  ( 5.297840055243947965, 11.43043024698558163, 5.501502898240879347 ) ) ;
#4900=CARTESIAN_POINT ( 'NONE',  ( 12.96002489183415562, 12.72746115195602101, 4.972234354664247569 ) ) ;
#4904=CARTESIAN_POINT ( 'NONE',  ( -0.07563368751253243816, 20.26160593876955929, 6.296573392346809683 ) ) ;
#4913=CARTESIAN_POINT ( 'NONE',  ( 6.007537124480966995, 11.30044911324893242, 2.933760949667521434 ) ) ;
#4917=CARTESIAN_POINT ( 'NONE',  ( 11.29207773696401240, 21.35684717879324168, 1.993224277495995844 ) ) ;
#4920=CARTESIAN_POINT ( 'NONE',  ( 7.696232935528439789, 11.34385124051986260, -0.1186037254217440495 ) ) ;
#4924=CARTESIAN_POINT ( 'NONE',  ( 10.77485793864860497, 18.93952712132382032, 6.088229833558084003 ) ) ;
#4925=CARTESIAN_POINT ( 'NONE',  ( 13.44644525748832287, 14.65557762784733598, 7.052608399104622450 ) ) ;
#4931=CARTESIAN_POINT ( 'NONE',  ( 2.384201206460603295, 20.83040400030756345, 6.653898520983334564 ) ) ;
#4934=CARTESIAN_POINT ( 'NONE',  ( 5.263634754952733807, 21.48398394320635063, 2.754189575719125926 ) ) ;
#4939=CARTESIAN_POINT ( 'NONE',  ( 1.989949280992425962, 13.58121736296352644, 1.066273477831844341 ) ) ;
#4940=CARTESIAN_POINT ( 'NONE',  ( 12.27481390375581149, 10.41612365926042116, 0.5751452393686051767 ) ) ;
#4941=CARTESIAN_POINT ( 'NONE',  ( 4.322661532824636943, 12.01334099290857260, 2.632746656654277650 ) ) ;
#4945=CARTESIAN_POINT ( 'NONE',  ( 1.836581059345375300, 12.93351256954322182, 0.5952454918390250871 ) ) ;
#4955=CARTESIAN_POINT ( 'NONE',  ( 7.445348592948711541, 21.00148274865230036, 3.220760063665622397 ) ) ;
#4957=CARTESIAN_POINT ( 'NONE',  ( 0.3054000514189714743, 20.95646860120554322, 6.387721792624859063 ) ) ;
#4963=CARTESIAN_POINT ( 'NONE',  ( 9.205773807864597202, 13.78306251088634227, 6.508323188782061841 ) ) ;
#4970=CARTESIAN_POINT ( 'NONE',  ( 0.6614644217660635706, 20.17319333280023130, 1.780821157163276602 ) ) ;
#4973=CARTESIAN_POINT ( 'NONE',  ( 6.069746319406092105, 12.28013972695870137, 0.9435336904642243061 ) ) ;
#4981=CARTESIAN_POINT ( 'NONE',  ( 7.437265405598497026, 11.41928500448566375, 0.003538791784208922958 ) ) ;
#4983=CARTESIAN_POINT ( 'NONE',  ( 12.49109536803858767, 20.73224863311122235, 5.227285940140482978 ) ) ;
#4987=CARTESIAN_POINT ( 'NONE',  ( 6.518464590081749499, 21.03009675402047307, 0.4263782151239406404 ) ) ;
#4990=CARTESIAN_POINT ( 'NONE',  ( 6.554211239163197256, 19.72323599584319709, 6.144497509861348128 ) ) ;
#4994=CARTESIAN_POINT ( 'NONE',  ( 8.201431583584922080, 11.69576222774042229, -0.06186996528689033686 ) ) ;
#4995=CARTESIAN_POINT ( 'NONE',  ( 5.377269426412026654, 15.26854398707441263, 7.911424674534676349 ) ) ;
#4997=CARTESIAN_POINT ( 'NONE',  ( 0.8188405504440110505, 20.20188058797412012, 7.869697537972164980 ) ) ;
#5002=CARTESIAN_POINT ( 'NONE',  ( 0.01038544335751814124, 14.29169281587572371, 1.257015631361889652 ) ) ;
#5006=SURFACE_STYLE_USAGE ( .BOTH. , #11866 ) ;
#5011=CARTESIAN_POINT ( 'NONE',  ( 10.70434257023885749, 11.78744898684672648, 3.934915454683276081 ) ) ;
#5014=CARTESIAN_POINT ( 'NONE',  ( 12.43084882143255676, 11.33874016961500253, 2.586588179875889182 ) ) ;
#5017=CARTESIAN_POINT ( 'NONE',  ( 1.538271623210065053, 14.85629794888722266, 0.2443331916369595735 ) ) ;
#5023=CARTESIAN_POINT ( 'NONE',  ( 6.008293396711528622, 11.33814340415402100, 2.936286190031843546 ) ) ;
#5027=CARTESIAN_POINT ( 'NONE',  ( 6.099401774668048226, 11.87301092205614061, 1.618424562767362351 ) ) ;
#5029=CARTESIAN_POINT ( 'NONE',  ( 8.133926869846012764, 20.59418330540166053, 4.731814609752428957 ) ) ;
#5031=CARTESIAN_POINT ( 'NONE',  ( 5.748166118559234761, 19.23834655595790011, -1.494793178587818128 ) ) ;
#5037=CARTESIAN_POINT ( 'NONE',  ( 8.430798958192390558, 20.36791151137297362, -0.04873577611252521286 ) ) ;
#5038=CARTESIAN_POINT ( 'NONE',  ( 11.34324718026622136, 17.71682859275886557, 7.525604685906813529 ) ) ;
#5044=CARTESIAN_POINT ( 'NONE',  ( 11.78095237921021621, 20.74046845656823734, -2.506342087363637727 ) ) ;
#5046=CARTESIAN_POINT ( 'NONE',  ( 0.3927195269979631975, 20.25378384025834322, 1.942505237861241740 ) ) ;
#5049=CARTESIAN_POINT ( 'NONE',  ( 6.562780996375648712, 20.62143860797926465, 6.272862003966319655 ) ) ;
#5051=CARTESIAN_POINT ( 'NONE',  ( 0.2130741384702063979, 13.20354400989074151, 2.231225264059853775 ) ) ;
#5061=CARTESIAN_POINT ( 'NONE',  ( 1.762868328497313453, 17.14743653705518867, -0.6379456634701065054 ) ) ;
#5073=CARTESIAN_POINT ( 'NONE',  ( 12.79864249265565412, 13.16814630638014272, 5.676106444755931513 ) ) ;
#5080=CARTESIAN_POINT ( 'NONE',  ( 9.016910062489662536, 12.61851657500311852, 5.516817133326245681 ) ) ;
#5088=CARTESIAN_POINT ( 'NONE',  ( -0.04318575428918173392, 17.49843205272302527, 0.1587271788072038559 ) ) ;
#5091=CARTESIAN_POINT ( 'NONE',  ( 1.797397970145764079, 14.26529943814340129, 8.410342253699687021 ) ) ;
#5097=CARTESIAN_POINT ( 'NONE',  ( 6.928561174131742106, 14.40990712224419745, -2.484241094878467226 ) ) ;
#5098=CARTESIAN_POINT ( 'NONE',  ( 10.89704555651259099, 21.97159967450292939, 0.8476583213610661138 ) ) ;
#5101=CARTESIAN_POINT ( 'NONE',  ( 9.317271201742652664, 12.75577108541303240, 6.731794365810285896 ) ) ;
#5102=CARTESIAN_POINT ( 'NONE',  ( 5.388874681376627507, 14.21749487271361190, 7.613809980626520257 ) ) ;
#5109=CARTESIAN_POINT ( 'NONE',  ( 11.41680985899818168, 16.27085401118786834, -3.868117637540980258 ) ) ;
#5111=CARTESIAN_POINT ( 'NONE',  ( 2.556540001888353508, 11.20929286741210085, 3.415214070081132203 ) ) ;
#5114=FACE_OUTER_BOUND ( 'NONE', #10650, .T. ) ;
#5120=CARTESIAN_POINT ( 'NONE',  ( 9.966377742653406813, 21.56226365017680280, 4.095160954391674046 ) ) ;
#5123=CARTESIAN_POINT ( 'NONE',  ( 13.16814363374584040, 15.42447050205943171, 6.337326380791521885 ) ) ;
#5125=CARTESIAN_POINT ( 'NONE',  ( 5.328913628694865068, 20.92139076675124443, 3.828052080691475290 ) ) ;
#5132=CARTESIAN_POINT ( 'NONE',  ( 10.75030023683537195, 19.11233889549468046, 6.102107763926431616 ) ) ;
#5133=CARTESIAN_POINT ( 'NONE',  ( 12.48890390579409804, 19.94235689841700321, 5.071047164889341374 ) ) ;
#5134=CARTESIAN_POINT ( 'NONE',  ( 4.135937413354406900, 17.27089909971514103, -1.194672083787219785 ) ) ;
#5135=CARTESIAN_POINT ( 'NONE',  ( 10.89370315683180479, 16.27139426067512318, -4.466024506084000478 ) ) ;
#5140=CARTESIAN_POINT ( 'NONE',  ( 10.96283612688636744, 18.09806758118428149, 6.499183517072732563 ) ) ;
#5141=CARTESIAN_POINT ( 'NONE',  ( 9.495683531383955156, 19.32856220366442201, -2.983829338518813490 ) ) ;
#5145=CARTESIAN_POINT ( 'NONE',  ( 11.24603787521979292, 18.83455621386651657, -3.846526465982558651 ) ) ;
#5146=CARTESIAN_POINT ( 'NONE',  ( 1.612457752549369516, 18.21888756068997495, -0.2970092401833866469 ) ) ;
#5149=CARTESIAN_POINT ( 'NONE',  ( 6.959724889100487921, 19.62783388037593113, 7.291040551301790629 ) ) ;
#5152=CARTESIAN_POINT ( 'NONE',  ( 0.3312671956846478527, 12.76499037468851228, 2.828231451653164363 ) ) ;
#5159=CARTESIAN_POINT ( 'NONE',  ( 1.748847732169433122, 13.54295735595392713, 0.1347836150705659652 ) ) ;
#5170=CARTESIAN_POINT ( 'NONE',  ( 11.29854319475162505, 11.62217351343478278, -0.9112959381959166993 ) ) ;
#5171=CARTESIAN_POINT ( 'NONE',  ( 1.893587539172431944, 21.28931287393832150, 4.984029115425525625 ) ) ;
#5179=CARTESIAN_POINT ( 'NONE',  ( 7.441962019404808615, 15.55687304735987553, -2.062044669940330976 ) ) ;
#5184=CARTESIAN_POINT ( 'NONE',  ( -0.1512147235091668429, 16.43876524939473427, 0.03898613886197917211 ) ) ;
#5188=CARTESIAN_POINT ( 'NONE',  ( 0.3131061926257734385, 14.25064834509208112, 1.086654584014467684 ) ) ;
#5193=CARTESIAN_POINT ( 'NONE',  ( 7.904713968335747687, 21.25109391276654236, 5.115303111256516821 ) ) ;
#5195=CARTESIAN_POINT ( 'NONE',  ( 12.59241507530448700, 20.47534440713213399, 5.493007318766919056 ) ) ;
#5202=CARTESIAN_POINT ( 'NONE',  ( 9.467427033990846397, 16.24499877588407415, 7.989881806620619642 ) ) ;
#5203=CARTESIAN_POINT ( 'NONE',  ( 5.996572361146331076, 12.27647896852458231, 0.9633039103135406789 ) ) ;
#5207=CARTESIAN_POINT ( 'NONE',  ( 9.028156031046822960, 11.14036371107460255, 3.487870285503237966 ) ) ;
#5208=CARTESIAN_POINT ( 'NONE',  ( 1.849087750985239476, 21.29000687509540413, 4.997418387125741823 ) ) ;
#5211=CARTESIAN_POINT ( 'NONE',  ( 5.367523021788562332, 15.73778643695066393, 8.099033024334408637 ) ) ;
#5215=( NAMED_UNIT ( * ) SI_UNIT ( $, .STERADIAN. ) SOLID_ANGLE_UNIT ( ) );
#5217=CARTESIAN_POINT ( 'NONE',  ( 10.57847960714909341, 20.55760711429452670, 5.741939694044305931 ) ) ;
#5221=CARTESIAN_POINT ( 'NONE',  ( 13.16825386439218804, 15.19382052832209240, 6.286146467198543419 ) ) ;
#5223=CARTESIAN_POINT ( 'NONE',  ( 3.388451077024644320, 15.55943979790526122, -0.6790290128948724968 ) ) ;
#5230=CARTESIAN_POINT ( 'NONE',  ( 6.810114687682450096, 12.02592060257602213, 4.780769153879307787 ) ) ;
#5231=CARTESIAN_POINT ( 'NONE',  ( 13.09416812643731909, 13.21983372403380130, 5.514055102800065278 ) ) ;
#5232=CARTESIAN_POINT ( 'NONE',  ( 2.560652196950205184, 12.18301083390420203, 1.830247191258276729 ) ) ;
#5233=CARTESIAN_POINT ( 'NONE',  ( 13.07015714027482822, 18.81087267297494137, 6.779469008999309487 ) ) ;
#5239=CARTESIAN_POINT ( 'NONE',  ( 8.869677037920350671, 20.91023519772625150, 1.107515482924187999 ) ) ;
#5240=CARTESIAN_POINT ( 'NONE',  ( 10.97615036777638586, 19.57796819772926256, 6.726635352813386426 ) ) ;
#5246=CARTESIAN_POINT ( 'NONE',  ( 5.901476864229157293, 11.26983891803934235, 1.171034228512400022 ) ) ;
#5249=CARTESIAN_POINT ( 'NONE',  ( 6.720649448207257848, 11.03335150912079143, 4.237661643980517923 ) ) ;
#5258=CARTESIAN_POINT ( 'NONE',  ( 4.901426570561191021, 19.87298744257788385, 7.435174622645311260 ) ) ;
#5271=CARTESIAN_POINT ( 'NONE',  ( 11.94242217153389873, 20.96877941592346062, -1.128413410470644029 ) ) ;
#5272=CARTESIAN_POINT ( 'NONE',  ( 3.657526251337493761, 16.52265399103842825, 9.296182230382092015 ) ) ;
#5278=CARTESIAN_POINT ( 'NONE',  ( 7.652417843280233001, 12.83819351580675239, -0.6376004508967495488 ) ) ;
#5285=CARTESIAN_POINT ( 'NONE',  ( 3.450345209542672098, 17.80254839864814542, 8.992318556635597204 ) ) ;
#5289=CARTESIAN_POINT ( 'NONE',  ( 2.146824126175768122, 20.56989294761467946, 4.842749342374482069 ) ) ;
#5295=CARTESIAN_POINT ( 'NONE',  ( 9.692593345077291644, 20.83333359141052199, -1.539594646718391191 ) ) ;
#5300=CARTESIAN_POINT ( 'NONE',  ( 13.34857347338189193, 16.50995800865382890, 7.170687989708792287 ) ) ;
#5304=CARTESIAN_POINT ( 'NONE',  ( 9.450549344251921724, 16.49206086971394569, 7.983172913004323412 ) ) ;
#5305=CARTESIAN_POINT ( 'NONE',  ( 7.265612110562694070, 13.47123956803594069, 6.779132443849506195 ) ) ;
#5307=CARTESIAN_POINT ( 'NONE',  ( 5.812451298883001272, 12.84336716734772210, 0.1757888620865697415 ) ) ;
#5308=CARTESIAN_POINT ( 'NONE',  ( 7.325623915630060878, 15.12110239233129683, 7.475628130178912478 ) ) ;
#5310=CARTESIAN_POINT ( 'NONE',  ( 1.652501564093576292, 20.40137862700089499, 4.418296261410975312 ) ) ;
#5313=CARTESIAN_POINT ( 'NONE',  ( 12.41071875754558640, 10.73085021393864125, 0.5799336287222065511 ) ) ;
#5316=CARTESIAN_POINT ( 'NONE',  ( 4.758138823084279601, 20.54266468784728161, 6.821625993668097188 ) ) ;
#5319=CARTESIAN_POINT ( 'NONE',  ( 0.7370043370095074042, 12.12568132066150106, 4.867010393250122746 ) ) ;
#5329=CARTESIAN_POINT ( 'NONE',  ( 10.47526939876109964, 20.78160439491057332, 5.469098418909443815 ) ) ;
#5331=CARTESIAN_POINT ( 'NONE',  ( 11.98942949869243790, 11.25314847078228198, 0.6870342585492783538 ) ) ;
#5335=PRODUCT_CONTEXT ( 'NONE', #4393, 'mechanical' ) ;
#5337=CARTESIAN_POINT ( 'NONE',  ( 4.623685801006120144, 19.97383893227930329, 1.114202881698282965 ) ) ;
#5339=CARTESIAN_POINT ( 'NONE',  ( 6.144469310126137174, 11.61924814016722074, 2.916029993654237984 ) ) ;
#5345=CARTESIAN_POINT ( 'NONE',  ( 9.357021909119426439, 17.21976690206051330, -2.890337777318933377 ) ) ;
#5347=CARTESIAN_POINT ( 'NONE',  ( 6.143851211478567720, 11.87235548079908298, 1.604867153432555593 ) ) ;
#5348=CARTESIAN_POINT ( 'NONE',  ( 1.061195401963308971, 11.40353646073516103, 4.768344864361504065 ) ) ;
#5350=CARTESIAN_POINT ( 'NONE',  ( 8.763882600799913547, 20.20007397076694033, 6.602868004581734951 ) ) ;
#5357=CARTESIAN_POINT ( 'NONE',  ( 13.38426742744203857, 16.76855268369192586, 7.271850668099400394 ) ) ;
#5361=CARTESIAN_POINT ( 'NONE',  ( 9.360600831854357651, 13.78714971782336107, -2.154141186429150423 ) ) ;
#5364=CARTESIAN_POINT ( 'NONE',  ( 5.341253238563739458, 21.55539096890324302, 3.869257563646466558 ) ) ;
#5367=CARTESIAN_POINT ( 'NONE',  ( 7.432055445221635637, 13.22750976636692677, 7.445346989300424489 ) ) ;
#5378=CARTESIAN_POINT ( 'NONE',  ( 3.392010078599061895, 21.32553552010993414, 3.405406787441542349 ) ) ;
#5389=CARTESIAN_POINT ( 'NONE',  ( 9.206787867131550840, 14.88153510792360024, 7.130031284213801612 ) ) ;
#5390=CARTESIAN_POINT ( 'NONE',  ( 1.754384330265707392, 15.58904521221044170, 9.648152067750672245 ) ) ;
#5393=CARTESIAN_POINT ( 'NONE',  ( 5.593119243055995504, 15.65317711712176063, 8.755201639697592242 ) ) ;
#5397=CARTESIAN_POINT ( 'NONE',  ( 7.484202164504814903, 14.08084388130622244, -1.560156711047595346 ) ) ;
#5403=CARTESIAN_POINT ( 'NONE',  ( 3.083679442600902654, 19.41275837844778351, 8.177690828459004635 ) ) ;
#5406=CARTESIAN_POINT ( 'NONE',  ( 0.1053325033440700720, 20.71056957386564079, 4.678228806545786433 ) ) ;
#5411=CARTESIAN_POINT ( 'NONE',  ( 8.873261155706039460, 17.35598761042906801, -3.486507808218821225 ) ) ;
#5414=CARTESIAN_POINT ( 'NONE',  ( 13.06466659634344651, 18.75638376262387652, 6.663973104921168122 ) ) ;
#5418=CARTESIAN_POINT ( 'NONE',  ( 9.004477611269402715, 11.50997377360702245, 5.301999128193525479 ) ) ;
#5419=CARTESIAN_POINT ( 'NONE',  ( 2.119723087323794442, 17.94179249953145217, 0.2479987765329453031 ) ) ;
#5421=CARTESIAN_POINT ( 'NONE',  ( 5.591081369763479358, 15.58183542640050412, -1.327434291682264345 ) ) ;
#5425=CARTESIAN_POINT ( 'NONE',  ( 7.758187014828991757, 18.34001794662099982, -2.671095701710830550 ) ) ;
#5427=CARTESIAN_POINT ( 'NONE',  ( 5.031007107017858360, 12.45697886261652698, 5.850013550272263885 ) ) ;
#5428=CARTESIAN_POINT ( 'NONE',  ( 13.38780373963751202, 21.37707633678951780, 1.836183508607381443 ) ) ;
#5429=CARTESIAN_POINT ( 'NONE',  ( 1.134588408652542180, 11.63698894629814085, 6.556856509031627311 ) ) ;
#5430=CARTESIAN_POINT ( 'NONE',  ( 1.031431676875810721, 19.63442241222599094, 8.342029421792293675 ) ) ;
#5432=CARTESIAN_POINT ( 'NONE',  ( -0.6715443117284065622, 20.05178378372840342, 3.977307728984901480 ) ) ;
#5439=CARTESIAN_POINT ( 'NONE',  ( 11.01646722322404948, 19.16985564352501825, 6.846897438552763226 ) ) ;
#5441=CARTESIAN_POINT ( 'NONE',  ( 11.94991743495628356, 11.28343550310636090, 0.5166888111268383987 ) ) ;
#5443=CARTESIAN_POINT ( 'NONE',  ( 0.6077902027026849119, 19.54577606275120161, 7.429059100087549439 ) ) ;
#5453=CARTESIAN_POINT ( 'NONE',  ( 6.570365227786298057, 11.61181900198992167, 3.191872150317673018 ) ) ;
#5455=CARTESIAN_POINT ( 'NONE',  ( 8.041622239940769745, 19.55876953989094247, -1.099914718329432439 ) ) ;
#5456=CARTESIAN_POINT ( 'NONE',  ( 0.1525355661814789543, 13.94977879502390294, 0.5504633849951708902 ) ) ;
#5463=CARTESIAN_POINT ( 'NONE',  ( 13.43775099319997146, 14.65538885420913573, 7.055912018318879042 ) ) ;
#5466=CARTESIAN_POINT ( 'NONE',  ( 10.00073136103841343, 11.49997002360925080, 0.8636844994430420419 ) ) ;
#5468=CARTESIAN_POINT ( 'NONE',  ( 13.39756118469465029, 22.16307784260286340, 1.948616576935187750 ) ) ;
#5469=CARTESIAN_POINT ( 'NONE',  ( 3.224325801286248794, 13.16763011922862070, 8.241763163179413709 ) ) ;
#5472=CARTESIAN_POINT ( 'NONE',  ( 6.495082362213654648, 10.90869521295860167, 3.280822230635792369 ) ) ;
#5478=CARTESIAN_POINT ( 'NONE',  ( 0.07294454634050162589, 16.38620845716783592, 0.7942576904715414887 ) ) ;
#5482=CARTESIAN_POINT ( 'NONE',  ( 1.965037718003479705, 16.82931600788473503, 0.08433362572124197820 ) ) ;
#5495=CARTESIAN_POINT ( 'NONE',  ( 12.71261977860552861, 11.95028677413862184, 4.239190098976814980 ) ) ;
#5496=CARTESIAN_POINT ( 'NONE',  ( 2.500687340046055418, 20.82590581279646003, 6.616773250763320569 ) ) ;
#5499=CARTESIAN_POINT ( 'NONE',  ( 4.167336224285882018, 11.37672557165839216, 2.018609927143729887 ) ) ;
#5505=CARTESIAN_POINT ( 'NONE',  ( 7.926815946483072750, 11.95748302575823097, 0.6454573217223682491 ) ) ;
#5507=CARTESIAN_POINT ( 'NONE',  ( 3.415768019861648241, 14.56304571309649099, 8.070112825631751363 ) ) ;
#5513=CARTESIAN_POINT ( 'NONE',  ( 3.401254764629610960, 18.09646818108351951, 8.897540692196587386 ) ) ;
#5516=CARTESIAN_POINT ( 'NONE',  ( 2.278141381403417931, 20.88642215721691997, 4.832218429395563675 ) ) ;
#5521=CARTESIAN_POINT ( 'NONE',  ( 5.089424605553659831, 13.78737461787913077, -1.074966794023267003 ) ) ;
#5524=CARTESIAN_POINT ( 'NONE',  ( 13.22906167343631090, 12.77717586684420148, 6.020701791080536047 ) ) ;
#5528=CARTESIAN_POINT ( 'NONE',  ( 13.28298931428452967, 21.40937655264818318, 1.617576389153118743 ) ) ;
#5529=CARTESIAN_POINT ( 'NONE',  ( 8.692839774141368991, 10.93259986899979097, 3.963448146918763904 ) ) ;
#5530=CARTESIAN_POINT ( 'NONE',  ( 1.098079023573843571, 12.39565097329668042, 6.272954462318547364 ) ) ;
#5532=CARTESIAN_POINT ( 'NONE',  ( 5.598276747425085631, 15.82787884806641188, -1.362751658015930012 ) ) ;
#5536=CARTESIAN_POINT ( 'NONE',  ( 8.500561619910278921, 21.25109391276654236, 4.936867450891936571 ) ) ;
#5538=CARTESIAN_POINT ( 'NONE',  ( 3.536356009984624293, 13.65508413018860168, -0.8098419684375965932 ) ) ;
#5541=CARTESIAN_POINT ( 'NONE',  ( 2.180285587184756402, 12.53249658949568257, 2.158027021525236400 ) ) ;
#5547=CARTESIAN_POINT ( 'NONE',  ( 9.783420551838821311, 21.71607306610668076, 3.592949344949918355 ) ) ;
#5551=CARTESIAN_POINT ( 'NONE',  ( 11.84502782025289847, 11.38735974601924283, 0.06333640615650359962 ) ) ;
#5554=CARTESIAN_POINT ( 'NONE',  ( 0.7231469830875896232, 19.66626656054290123, 2.290770552806581595 ) ) ;
#5557=CARTESIAN_POINT ( 'NONE',  ( 4.471143474535477225, 19.65688249982645175, 0.7326053640163348035 ) ) ;
#5561=CARTESIAN_POINT ( 'NONE',  ( 9.102730975966599303, 18.23105645554593934, 6.913738234213362865 ) ) ;
#5562=CARTESIAN_POINT ( 'NONE',  ( 4.789876627565358369, 19.17887308449560635, 7.014825586549866543 ) ) ;
#5564=CARTESIAN_POINT ( 'NONE',  ( 7.828653474077823304, 16.61588919119046182, 7.980077449799868106 ) ) ;
#5565=CARTESIAN_POINT ( 'NONE',  ( 11.52440248773281617, 20.24847620595872044, -3.116674102378380162 ) ) ;
#5571=CARTESIAN_POINT ( 'NONE',  ( 5.350757514931804515, 15.44490212850582189, -2.194769716375351898 ) ) ;
#5575=CARTESIAN_POINT ( 'NONE',  ( 9.375099485748442874, 13.64553664392443011, -2.068740140728067889 ) ) ;
#5579=CARTESIAN_POINT ( 'NONE',  ( -0.1742194648750999830, 20.56733048332889879, 6.416404061768046674 ) ) ;
#5582=CARTESIAN_POINT ( 'NONE',  ( 7.219865183778306772, 12.09587256105000641, 6.418183704565048942 ) ) ;
#5590=CARTESIAN_POINT ( 'NONE',  ( 2.014813869672630098, 17.23626398232610057, 0.1440630847629725264 ) ) ;
#5591=CARTESIAN_POINT ( 'NONE',  ( 9.222712265903270534, 13.32230603934784163, -2.943534436737037741 ) ) ;
#5606=CARTESIAN_POINT ( 'NONE',  ( 5.828080763218296489, 12.69966494906990206, 0.1882201014488152913 ) ) ;
#5607=CARTESIAN_POINT ( 'NONE',  ( 0.7899212862509950028, 11.31684784372412089, 4.849392175464794619 ) ) ;
#5610=CARTESIAN_POINT ( 'NONE',  ( 5.537923952358154267, 16.68662888302730707, 8.792294931775872513 ) ) ;
#5615=CARTESIAN_POINT ( 'NONE',  ( 7.439309206678073494, 15.11921583032367877, -1.967807152704160734 ) ) ;
#5616=CARTESIAN_POINT ( 'NONE',  ( 1.422955370182567014, 13.97322825811035685, 8.124243789848305752 ) ) ;
#5625=CARTESIAN_POINT ( 'NONE',  ( 1.715417743616410196, 21.19999865368947312, 4.581887404234925576 ) ) ;
#5629=CARTESIAN_POINT ( 'NONE',  ( 6.980491476190183064, 11.62550227300026151, 4.018716726805900308 ) ) ;
#5636=CARTESIAN_POINT ( 'NONE',  ( 9.445988718791797467, 11.13211821786026157, 0.4531721362220474947 ) ) ;
#5638=CARTESIAN_POINT ( 'NONE',  ( 13.25983584171517116, 12.99030557094804550, 6.173116066625142118 ) ) ;
#5643=CARTESIAN_POINT ( 'NONE',  ( 7.655173456064148674, 19.24630943483592205, -2.133094473368749355 ) ) ;
#5644=CARTESIAN_POINT ( 'NONE',  ( 6.336034323945050062, 11.65589518700730132, 2.459063698344419180 ) ) ;
#5648=CARTESIAN_POINT ( 'NONE',  ( 6.077993251687278331, 12.04737542433794495, 1.424762966830985356 ) ) ;
#5649=CARTESIAN_POINT ( 'NONE',  ( 7.225041933885432144, 13.52979383919193701, 6.708482075865046745 ) ) ;
#5653=CARTESIAN_POINT ( 'NONE',  ( 10.60828838171844524, 10.54134736952624252, 2.111780394654666715 ) ) ;
#5654=CARTESIAN_POINT ( 'NONE',  ( 2.262747632565262013, 19.81152135836902062, 0.4607135673276451238 ) ) ;
#5655=CARTESIAN_POINT ( 'NONE',  ( 0.1974682674717982978, 20.91554504214090926, 6.174409461716068748 ) ) ;
#5659=CARTESIAN_POINT ( 'NONE',  ( 4.210766624584501017, 12.02909395710813989, 2.263615127930675541 ) ) ;
#5666=CARTESIAN_POINT ( 'NONE',  ( 10.89352820671717836, 11.26631715233412301, 4.659004019323803369 ) ) ;
#5669=CARTESIAN_POINT ( 'NONE',  ( 11.30708403999637923, 13.02122886099977173, -2.389217618889588390 ) ) ;
#5671=CARTESIAN_POINT ( 'NONE',  ( 5.999549737364129776, 11.29786724840421108, 1.172376165605415910 ) ) ;
#5673=CARTESIAN_POINT ( 'NONE',  ( -0.05205347293826909777, 14.29405283160754614, 1.280296971734305567 ) ) ;
#5679=CARTESIAN_POINT ( 'NONE',  ( 13.28541201854497089, 14.87610706663238247, 6.283089683201566800 ) ) ;
#5681=CARTESIAN_POINT ( 'NONE',  ( 13.10321590180860163, 13.21942167511952171, 5.511931958094891115 ) ) ;
#5682=CARTESIAN_POINT ( 'NONE',  ( 12.11531023645522431, 21.60439101236092085, -1.537999855465251198 ) ) ;
#5691=CARTESIAN_POINT ( 'NONE',  ( 7.402035373046037314, 12.62799681450196054, -1.657535778544305671 ) ) ;
#5696=CARTESIAN_POINT ( 'NONE',  ( 9.348107690663828961, 13.91467961181269786, -2.228914411464946177 ) ) ;
#5698=CARTESIAN_POINT ( 'NONE',  ( 13.03561731774868093, 22.21723951419428289, 0.9385846051497386267 ) ) ;
#5699=CARTESIAN_POINT ( 'NONE',  ( 3.293281583389384704, 17.27089909971514103, -0.9423259528885826741 ) ) ;
#5702=CARTESIAN_POINT ( 'NONE',  ( 7.543722629209693942, 14.82614142317876116, 8.183702551990444718 ) ) ;
#5713=CARTESIAN_POINT ( 'NONE',  ( 12.11059067823646096, 21.69514399574918073, 3.938167792122971633 ) ) ;
#5729=CARTESIAN_POINT ( 'NONE',  ( 1.308477177346879960, 18.94235087979956234, 8.980548047580915849 ) ) ;
#5732=CARTESIAN_POINT ( 'NONE',  ( 5.486362570609389699, 13.28024286532647658, 7.851790441297502809 ) ) ;
#5736=EDGE_CURVE ( 'NONE', #10254, #1010, #11869, .T. ) ;
#5737=CARTESIAN_POINT ( 'NONE',  ( 1.406030455404901236, 13.81240482153004301, 8.014482998805931402 ) ) ;
#5746=CARTESIAN_POINT ( 'NONE',  ( 1.924744121216944492, 21.16741921860587183, 5.146558987964561460 ) ) ;
#5748=CARTESIAN_POINT ( 'NONE',  ( 2.729946285357361280, 19.31779869980666220, 0.8719274852789313801 ) ) ;
#5750=CARTESIAN_POINT ( 'NONE',  ( 13.03965183343015610, 21.58187285162961189, 1.970499231081598079 ) ) ;
#5755=CARTESIAN_POINT ( 'NONE',  ( 11.27191446706569700, 20.19146305430580313, -2.972894652454601605 ) ) ;
#5758=CARTESIAN_POINT ( 'NONE',  ( 12.93435681163277629, 11.44283640310037065, 4.674273103487593950 ) ) ;
#5762=CARTESIAN_POINT ( 'NONE',  ( 7.774415866391942487, 11.36058604623794110, 0.08081017952465485710 ) ) ;
#5763=CARTESIAN_POINT ( 'NONE',  ( 7.035607835188398163, 12.34291428558256065, 5.584210644256598854 ) ) ;
#5766=CARTESIAN_POINT ( 'NONE',  ( 6.035803313514758628, 12.13412562418924878, 1.232330704826734458 ) ) ;
#5771=CARTESIAN_POINT ( 'NONE',  ( 11.63353270475617229, 12.58417018233828166, -2.804383768420597445 ) ) ;
#5773=CARTESIAN_POINT ( 'NONE',  ( 4.967848656229971738, 21.41895532286982018, 1.997643190962260284 ) ) ;
#5774=CARTESIAN_POINT ( 'NONE',  ( 1.576549648455226160, 17.24306997481907899, 9.529489457303672140 ) ) ;
#5777=CARTESIAN_POINT ( 'NONE',  ( 1.950423677167738346, 13.53163558985986192, 0.9959168722820052055 ) ) ;
#5782=CARTESIAN_POINT ( 'NONE',  ( 10.73969208887204019, 10.95696249848220205, 4.001686992780678409 ) ) ;
#5786=CARTESIAN_POINT ( 'NONE',  ( 11.63141746489545980, 11.77663938069181349, -0.8745901904067018284 ) ) ;
#5787=CARTESIAN_POINT ( 'NONE',  ( 5.774788405422635940, 19.06000005006808706, -1.475126938916978769 ) ) ;
#5789=CARTESIAN_POINT ( 'NONE',  ( 2.415885207217761455, 12.01605003366594104, 3.603415997180536845 ) ) ;
#5792=CARTESIAN_POINT ( 'NONE',  ( 5.089517729310932381, 20.57392463301560426, 2.318340695833992715 ) ) ;
#5797=CARTESIAN_POINT ( 'NONE',  ( 11.33002609776169578, 15.75027095350177397, 6.855137435532622447 ) ) ;
#5799=CARTESIAN_POINT ( 'NONE',  ( 11.15970370577760029, 14.44082934938793272, -3.345223894823480038 ) ) ;
#5802=CARTESIAN_POINT ( 'NONE',  ( 4.837794195432601363, 20.03811753756829361, 7.273909691047188097 ) ) ;
#5806=CARTESIAN_POINT ( 'NONE',  ( 11.14506973860339478, 16.78189356879117256, 6.798425575953311650 ) ) ;
#5807=CARTESIAN_POINT ( 'NONE',  ( 10.81988799240761701, 16.27139746542214027, -4.448395456820358085 ) ) ;
#5811=CARTESIAN_POINT ( 'NONE',  ( 9.405431565759853285, 13.38381860909070653, -1.897411705095320089 ) ) ;
#5812=CARTESIAN_POINT ( 'NONE',  ( 1.075305989013234598, 18.45120109744945225, 8.266748288633882780 ) ) ;
#5813=CARTESIAN_POINT ( 'NONE',  ( -0.3990962785833974680, 17.28679025579738138, 0.5365138910678359796 ) ) ;
#5832=CARTESIAN_POINT ( 'NONE',  ( 2.484165171653412330, 11.21351766718956178, 3.437652806735580935 ) ) ;
#5834=CARTESIAN_POINT ( 'NONE',  ( 4.865075149428808032, 11.25209086740643016, 5.008807926723467752 ) ) ;
#5839=CARTESIAN_POINT ( 'NONE',  ( 1.385753006902628703, 13.65946455019744299, 7.893527135823292795 ) ) ;
#5844=CARTESIAN_POINT ( 'NONE',  ( 3.588180185287924484, 13.77383989023144117, 8.530597361598315942 ) ) ;
#5852=CARTESIAN_POINT ( 'NONE',  ( 7.122862576751088248, 21.40982604368873865, 3.348050232907604951 ) ) ;
#5855=CARTESIAN_POINT ( 'NONE',  ( 12.60979462320922373, 10.71893859347252231, 3.290081565980131906 ) ) ;
#5860=CARTESIAN_POINT ( 'NONE',  ( 7.526575487049647961, 18.64928636511069371, -2.428959993994535882 ) ) ;
#5861=CARTESIAN_POINT ( 'NONE',  ( 6.704184490690651366, 11.71035962591412272, 4.082957847732187062 ) ) ;
#5864=CARTESIAN_POINT ( 'NONE',  ( 7.067667105230608371, 20.80763019527516988, 1.945974362385073819 ) ) ;
#5865=CARTESIAN_POINT ( 'NONE',  ( 2.447833637063231205, 19.89874561968573374, 6.469289142455495245 ) ) ;
#5867=CARTESIAN_POINT ( 'NONE',  ( 8.720760638157020850, 10.73926345162572105, 3.665552357571379538 ) ) ;
#5869=CARTESIAN_POINT ( 'NONE',  ( 7.415316962347603180, 12.98226186039768137, 7.408690243710602807 ) ) ;
#5870=CARTESIAN_POINT ( 'NONE',  ( 0.7102513561496924810, 20.31959456549100906, 7.525625334632009000 ) ) ;
#5872=CARTESIAN_POINT ( 'NONE',  ( 0.1976490688386850214, 20.17752205389220066, 6.189897254476726118 ) ) ;
#5881=CARTESIAN_POINT ( 'NONE',  ( 10.02755535553010624, 10.65547162720833185, 1.022515237104560271 ) ) ;
#5884=CARTESIAN_POINT ( 'NONE',  ( 5.810244688662751678, 11.73040477827100325, 0.3453541907369687136 ) ) ;
#5886=CARTESIAN_POINT ( 'NONE',  ( 2.012643648797029616, 17.94014877828372079, 0.2841994374236595511 ) ) ;
#5892=CARTESIAN_POINT ( 'NONE',  ( 5.774107441413635300, 17.24227063501358614, -1.439737884917017707 ) ) ;
#5893=CARTESIAN_POINT ( 'NONE',  ( 4.924203502439124414, 18.75546692123623060, 7.326012498920505323 ) ) ;
#5894=CARTESIAN_POINT ( 'NONE',  ( 9.588774839205283840, 12.37377145998696193, -1.094828636744461292 ) ) ;
#5897=CARTESIAN_POINT ( 'NONE',  ( 5.464785416199259060, 17.37627409491906505, 8.697631989696647636 ) ) ;
#5903=CARTESIAN_POINT ( 'NONE',  ( 6.392593417591551308, 10.79308423060320088, 3.256129757715929163 ) ) ;
#5906=CARTESIAN_POINT ( 'NONE',  ( 10.22638260995712400, 20.36150965861552464, -0.9086538386368623321 ) ) ;
#5908=CARTESIAN_POINT ( 'NONE',  ( 0.8501141161861881512, 19.12429843616597580, 7.755429456263986054 ) ) ;
#5909=CARTESIAN_POINT ( 'NONE',  ( 2.439223677983356708, 11.63542902183100125, 5.280048492248608838 ) ) ;
#5916=CARTESIAN_POINT ( 'NONE',  ( 0.03622098100764838124, 15.71836236879072679, 0.8515907948898381319 ) ) ;
#5920=CARTESIAN_POINT ( 'NONE',  ( 11.00068862475037790, 16.27139746542210119, -4.502538961693060671 ) ) ;
#5930=CARTESIAN_POINT ( 'NONE',  ( 1.805619654075212965, 13.02087111295804256, 0.3827243396642013851 ) ) ;
#5933=CARTESIAN_POINT ( 'NONE',  ( 3.861727869702078042, 18.73760406805453371, -0.8916021778709736223 ) ) ;
#5937=CARTESIAN_POINT ( 'NONE',  ( 2.889068357235882623, 12.18047855553292713, 5.318317885449051374 ) ) ;
#5944=CARTESIAN_POINT ( 'NONE',  ( 2.377763845684053745, 11.40282469389570075, 3.054462267276081278 ) ) ;
#5954=CARTESIAN_POINT ( 'NONE',  ( 6.447884206030225940, 11.65642365002708125, 5.039460170731214106 ) ) ;
#5957=CARTESIAN_POINT ( 'NONE',  ( 12.85806460298763021, 11.22509623584751282, 4.343794590431158120 ) ) ;
#5962=CARTESIAN_POINT ( 'NONE',  ( 7.267304438700130653, 16.63416352659407238, -2.882144068962717576 ) ) ;
#5964=CARTESIAN_POINT ( 'NONE',  ( 6.892979284088748493, 20.66668035358058120, 1.484166371361514747 ) ) ;
#5968=CARTESIAN_POINT ( 'NONE',  ( 13.86187374551126439, 22.11716190621255862, 2.323971484891082184 ) ) ;
#5970=CARTESIAN_POINT ( 'NONE',  ( 0.8098354902157162138, 20.20131944153736114, 7.871963320744100656 ) ) ;
#5971=CARTESIAN_POINT ( 'NONE',  ( 1.655340346233492355, 13.96895574127920625, 9.020042064985599239 ) ) ;
#5976=CARTESIAN_POINT ( 'NONE',  ( 0.1177374572251341928, 17.19689764357661943, 0.7940873122000081663 ) ) ;
#5984=CARTESIAN_POINT ( 'NONE',  ( 10.56390221082172687, 10.71761206645349240, 3.260385432885468227 ) ) ;
#5988=CARTESIAN_POINT ( 'NONE',  ( 12.30618434154357566, 20.85343389055401175, -1.024261053597833371 ) ) ;
#5989=CARTESIAN_POINT ( 'NONE',  ( 6.049413308899639574, 11.22004793005951306, 1.386673510691023292 ) ) ;
#5997=CARTESIAN_POINT ( 'NONE',  ( 8.886489067368289696, 11.45164960235222118, 3.463840564905101171 ) ) ;
#6000=CARTESIAN_POINT ( 'NONE',  ( 7.863974401675383419, 12.04767321495844179, 0.2472099257450396381 ) ) ;
#6008=CARTESIAN_POINT ( 'NONE',  ( 5.020040770389102569, 19.52513284903354673, 7.730226423647035716 ) ) ;
#6014=CARTESIAN_POINT ( 'NONE',  ( 9.792942318191714790, 19.23395335097719538, -1.995198763412909804 ) ) ;
#6016=CARTESIAN_POINT ( 'NONE',  ( 1.255833685023748370, 17.68435013880464624, 8.631050028349431358 ) ) ;
#6019=CARTESIAN_POINT ( 'NONE',  ( 5.052911015069207146, 14.03105527214651715, 8.089863925655100374 ) ) ;
#6032=CARTESIAN_POINT ( 'NONE',  ( 8.599231060378546232, 19.63015825768726330, 6.053049467817567475 ) ) ;
#6044=CARTESIAN_POINT ( 'NONE',  ( 4.684843972026743408, 20.53916262649988056, 6.840992517925734262 ) ) ;
#6047=CARTESIAN_POINT ( 'NONE',  ( 3.552288670928100078, 16.45067739432806064, -1.423831345796362946 ) ) ;
#6052=CARTESIAN_POINT ( 'NONE',  ( 0.9277841963642122769, 12.28846772247859498, 5.618827124256060124 ) ) ;
#6061=CARTESIAN_POINT ( 'NONE',  ( 3.621953361605184885, 14.18517595478938098, 8.745819149335433806 ) ) ;
#6068=ORIENTED_EDGE ( 'NONE', *, *, #16161, .F. ) ;
#6070=CARTESIAN_POINT ( 'NONE',  ( 9.435867950683245908, 21.13787900135836395, 3.521159264218552742 ) ) ;
#6073=CARTESIAN_POINT ( 'NONE',  ( 11.16014847406012223, 18.33592708871418608, -4.033227821418477355 ) ) ;
#6078=CARTESIAN_POINT ( 'NONE',  ( 8.166405835557249304, 10.80616279181379014, 1.748811918552366729 ) ) ;
#6080=CARTESIAN_POINT ( 'NONE',  ( 7.219217501582479102, 20.87764444342654357, 2.348948422008501957 ) ) ;
#6083=CARTESIAN_POINT ( 'NONE',  ( 2.724573480716647289, 19.38658690530843742, 7.155403551711358112 ) ) ;
#6084=CARTESIAN_POINT ( 'NONE',  ( 10.87431863107423169, 10.89466173679246097, 4.149793331543699004 ) ) ;
#6090=CARTESIAN_POINT ( 'NONE',  ( 1.613076528681359756, 14.62668795976242642, -0.4927809465211088202 ) ) ;
#6091=CARTESIAN_POINT ( 'NONE',  ( 1.389669449877557472, 12.36033839947706170, 7.643082816218980113 ) ) ;
#6093=CARTESIAN_POINT ( 'NONE',  ( 6.659626489177622233, 11.71104153968872197, 4.096152728507711949 ) ) ;
#6100=CARTESIAN_POINT ( 'NONE',  ( 11.03847332581440277, 11.68029354362261252, 5.291968781390675503 ) ) ;
#6103=CARTESIAN_POINT ( 'NONE',  ( 5.712404053886056765, 18.78909992803161444, -1.619831271828931829 ) ) ;
#6105=CARTESIAN_POINT ( 'NONE',  ( 2.826950749410920061, 20.19548487530456171, 2.214332391823603530 ) ) ;
#6109=CARTESIAN_POINT ( 'NONE',  ( 6.177452850684594488, 20.35534769734861271, 5.182961054158671033 ) ) ;
#6115=CARTESIAN_POINT ( 'NONE',  ( 7.235976006262752946, 20.89828364148222306, 1.503125890472612358 ) ) ;
#6116=CARTESIAN_POINT ( 'NONE',  ( 5.363225780242031782, 15.84434817051344169, 8.012013768214686138 ) ) ;
#6118=CARTESIAN_POINT ( 'NONE',  ( 6.674888723083876485, 11.58565265486105211, 2.754745497594413450 ) ) ;
#6128=CARTESIAN_POINT ( 'NONE',  ( 9.405185730933931509, 17.20066956042925455, -2.794330434878057101 ) ) ;
#6131=CARTESIAN_POINT ( 'NONE',  ( 0.7938407936894211758, 19.25142560623917376, 7.620760418591133067 ) ) ;
#6133=CARTESIAN_POINT ( 'NONE',  ( 5.870371952983467700, 11.25617621838232196, 2.534352863508499087 ) ) ;
#6142=CARTESIAN_POINT ( 'NONE',  ( 0.3881773077461687649, 18.36706280121488533, 1.288916289607236365 ) ) ;
#6144=B_SPLINE_SURFACE_WITH_KNOTS ( 'NONE', 3, 3, ( 
 ( #132, #5432, #10308, #13532, #10423, #17050, #6657, #8414, #2004, #10525, #1897, #5319, #16833, #12087, #5002, #1674, #3566, #15418, #13753, #11758, #245, #10191, #17, #15191, #15309, #8743, #12197, #10088, #3456, #1578, #16935, #6983, #8319, #15524, #15090, #21803, #20239, #20343, #7101, #13417, #6767, #13643, #5211, #1784, #8529, #9303, #12747, #5659, #3901, #17395, #17500, #19360, #19027, #580, #12418, #8858, #682, #21124, #7427, #10642, #4339, #473, #4225, #2235, #7227, #8973, #14409 ),
 ( #17603, #14309, #15753, #5872, #20684, #7324, #12532, #2457, #7546, #13986, #9185, #4012, #14087, #20792, #9077, #12636, #5976, #19146, #10754, #19468, #2347, #10857, #17271, #4115, #2118, #7648, #15852, #15642, #14200, #20914, #5541, #5777, #19256, #15965, #799, #12299, #10965, #21026, #17717, #2568, #16077, #907, #11080, #1005, #4773, #14848, #14961, #2893, #8073, #11405, #21448, #6419, #21563, #11287, #14520, #7861, #13189, #6305, #21342, #16391, #11504, #19786, #19898, #6093, #7971, #6200, #19679 ),
 ( #16602, #16284, #2681, #8187, #13299, #1330, #13079, #12864, #7754, #17934, #21236, #3106, #4660, #18247, #16495, #9831, #11182, #4548, #18153, #21675, #1440, #4451, #19583, #12971, #9627, #6537, #3006, #18037, #1228, #20001, #9733, #17835, #2779, #14742, #9411, #16179, #9514, #1118, #14638, #21781, #13619, #1758, #18465, #4871, #15283, #15394, #10167, #8502, #11839, #3332, #17024, #327, #10396, #17140, #13837, #20103, #18350, #108, #15499, #219, #20421, #18568, #6629, #15165, #16911, #6858, #4973 ),
 ( #20318, #11730, #9952, #18782, #7071, #11957, #10063, #16811, #5091, #6959, #1651, #8392, #6742, #3215, #5188, #8723, #11939, #13506, #11615, #16713, #5289, #20218, #1551, #3432, #1982, #18668, #15066, #3539, #10275, #1872, #12055, #8294, #8617, #3652, #17687, #5748, #17576, #10828, #10727, #20878, #14173, #550, #17469, #15826, #18894, #9049, #12504, #2538, #2315, #9271, #14061, #15607, #19000, #7297, #8831, #20999, #12170, #653, #17247, #16047, #878, #19329, #8947, #5629, #20543, #9155, #2430 ),
 ( #19226, #19115, #5406, #12390, #4087, #4194, #15938, #444, #12603, #766, #7517, #14282, #3765, #7197, #20767, #13957, #20655, #15724, #3984, #10502, #5516, #12275, #3876, #17363, #2205, #13775, #3480, #44, #8884, #12321, #5232, #10217, #16964, #17078, #18939, #18614, #159, #18723, #8444, #266, #20709, #7008, #1813, #3925, #6797, #3811, #8557, #13557, #15334, #14007, #11886, #5134, #12111, #3593, #6902, #10546, #15215, #2023, #13666, #5564, #8766, #13899, #7130, #20478, #15548, #3704, #10334 ),
 ( #20367, #1921, #19048, #8666, #10445, #16858, #379, #1703, #7248, #15438, #20262, #5348, #18836, #20598, #5456, #12220, #17294, #2141, #15666, #495, #17522, #15878, #14431, #927, #9431, #8996, #600, #16203, #15774, #14223, #12656, #7671, #20942, #17628, #21700, #1462, #4685, #7885, #1250, #8210, #14869, #14764, #9752, #20021, #13211, #4890, #21366, #1347, #21470, #13101, #6222, #16308, #9851, #12993, #19923, #8091, #18062, #4469, #21586, #14985, #16515, #6446, #11429, #2921, #16620, #21799, #9977 ),
 ( #19812, #4796, #1575, #6555, #16735, #8316, #11205, #15087, #11634, #19699, #7990, #18371, #4573, #6327, #6653, #16419, #11313, #17955, #2803, #9538, #18175, #3240, #3029, #1143, #11528, #18269, #14660, #3127, #9650, #5111, #7098, #469, #20446, #17161, #13528, #8740, #1671, #20235, #15414, #5316, #10420, #16830, #12080, #6880, #18586, #11859, #11963, #15520, #8855, #6764, #1781, #15638, #13640, #13749, #7222, #6980, #2114, #10521, #10187, #20124, #18693, #17047, #18484, #3561, #8524, #16930, #3453 ),
 ( #15305, #2000, #18807, #349, #4997, #10085, #13866, #20568, #11753, #10303, #5429, #3676, #8641, #12194, #18916, #20340, #8409, #129, #3786, #242, #5208, #1894, #17267, #3357, #15187, #14, #10851, #9074, #678, #15748, #3897, #19354, #8970, #795, #17600, #5654, #13983, #9182, #2565, #19253, #15962, #20911, #12415, #4221, #9407, #19465, #4336, #1002, #577, #5538, #7542, #2678, #9299, #7645, #5773, #14084, #2341, #4112, #14306, #20789, #20680, #5869, #12529, #19143, #15849, #21023, #12633 ),
 ( #10961, #17714, #4008, #19022, #5970, #16176, #7423, #10752, #17497, #14196, #16074, #904, #14406, #21121, #12296, #12743, #17831, #11076, #10639, #17391, #2231, #9827, #14634, #19580, #21339, #4867, #2776, #17931, #3002, #18032, #1113, #16596, #6090, #8068, #19676, #11611, #14844, #4767, #19894, #19782, #21559, #16490, #9621, #4656, #9729, #12860, #18147, #6415, #18344, #11401, #3210, #1224, #9511, #6197, #16387, #11178, #8183, #21233, #1326, #4447, #19996, #9948, #6533, #2889, #14737, #7751, #18243 ) ),
 .UNSPECIFIED., .F., .F., .F.,
 ( 4, 1, 1, 1, 1, 1, 4 ),
 ( 4, 1, 1, 1, 1, 1, 1, 1, 1, 1, 1, 1, 1, 1, 1, 1, 1, 1, 1, 1, 1, 1, 1, 1, 1, 1, 1, 1, 1, 1, 1, 1, 1, 1, 1, 1, 1, 1, 1, 1, 1, 1, 1, 1, 1, 1, 1, 1, 1, 1, 1, 1, 1, 1, 1, 1, 1, 1, 1, 1, 1, 1, 1, 1, 4 ),
 ( -0.01121212662510000062, 0.000000000000000000, 0.1250000000000000000, 0.2500000000000000000, 0.3750000000000000000, 0.5000000000000000000, 0.5112121266250999607 ),
 ( -0.02000000000000000042, -0.003749999999999999861, 0.01250000000000000069, 0.02875000000000000125, 0.04499999999999999833, 0.06124999999999999889, 0.07749999999999999944, 0.09375000000000000000, 0.1100000000000000006, 0.1262500000000000011, 0.1424999999999999878, 0.1587500000000000022, 0.1749999999999999889, 0.1912500000000000033, 0.2074999999999999900, 0.2237500000000000044, 0.2399999999999999911, 0.2562499999999999778, 0.2725000000000000200, 0.2887500000000000067, 0.3049999999999999933, 0.3212499999999999800, 0.3375000000000000222, 0.3537500000000000089, 0.3699999999999999956, 0.3862499999999999822, 0.4025000000000000244, 0.4187500000000000111, 0.4349999999999999978, 0.4512499999999999845, 0.4675000000000000266, 0.4837500000000000133, 0.5000000000000000000, 0.5162499999999999867, 0.5324999999999999734, 0.5487499999999999600, 0.5649999999999999467, 0.5812500000000000444, 0.5975000000000000311, 0.6137500000000000178, 0.6300000000000000044, 0.6462499999999999911, 0.6624999999999999778, 0.6787499999999999645, 0.6949999999999999512, 0.7112500000000000488, 0.7275000000000000355, 0.7437500000000000222, 0.7600000000000000089, 0.7762499999999999956, 0.7924999999999999822, 0.8087499999999999689, 0.8249999999999999556, 0.8412500000000000533, 0.8575000000000000400, 0.8737500000000000266, 0.8900000000000000133, 0.9062500000000000000, 0.9224999999999999867, 0.9387499999999999734, 0.9549999999999999600, 0.9712499999999999467, 0.9875000000000000444, 1.003749999999999920, 1.020000000000000018 ),
 .UNSPECIFIED. ) ;
#6146=CARTESIAN_POINT ( 'NONE',  ( 13.16968626221765248, 14.87475635823169640, 6.322754070328278075 ) ) ;
#6148=CARTESIAN_POINT ( 'NONE',  ( 6.861624739425660202, 21.59165172380602371, 1.401955922046088210 ) ) ;
#6153=FACE_OUTER_BOUND ( 'NONE', #8027, .T. ) ;
#6162=CARTESIAN_POINT ( 'NONE',  ( 0.2333143917931327360, 19.02276410538376084, 0.6558456349049158751 ) ) ;
#6165=CARTESIAN_POINT ( 'NONE',  ( 3.524832663404014355, 15.96368446185943135, -1.413071295161979712 ) ) ;
#6169=CARTESIAN_POINT ( 'NONE',  ( 1.076515439104938299, 12.50515649462741763, 6.318341509549295409 ) ) ;
#6176=CARTESIAN_POINT ( 'NONE',  ( 3.518193601275699578, 13.18433185408993147, 8.140409692525564012 ) ) ;
#6185=CARTESIAN_POINT ( 'NONE',  ( 5.496113507260316666, 12.63305981940006184, 0.2285824550650361886 ) ) ;
#6188=CARTESIAN_POINT ( 'NONE',  ( 12.00464716003233434, 21.22932480519864029, -1.908312899720273181 ) ) ;
#6193=CARTESIAN_POINT ( 'NONE',  ( 8.499614257248339300, 21.33403448576225259, 0.06076556050593111269 ) ) ;
#6194=CARTESIAN_POINT ( 'NONE',  ( 9.061696275389516941, 17.79575755247912738, 7.005266136422250156 ) ) ;
#6195=CARTESIAN_POINT ( 'NONE',  ( 13.72479379337794825, 21.95613576153688484, 1.820250569444666233 ) ) ;
#6197=CARTESIAN_POINT ( 'NONE',  ( 4.362043098078323133, 20.54185615358932182, 0.4015571536017943366 ) ) ;
#6198=CARTESIAN_POINT ( 'NONE',  ( 1.268452225264728561, 11.99997494541211651, 7.084638612796553936 ) ) ;
#6200=CARTESIAN_POINT ( 'NONE',  ( 6.062088034068962017, 12.01182390341870310, 1.443241840189279701 ) ) ;
#6207=CARTESIAN_POINT ( 'NONE',  ( 9.070049129643198427, 15.38332000535482180, -3.534303114342071783 ) ) ;
#6210=CARTESIAN_POINT ( 'NONE',  ( 11.88511336867002299, 20.02872603525521455, -2.122466797632162283 ) ) ;
#6211=CARTESIAN_POINT ( 'NONE',  ( 6.300610883601452272, 20.63257317582153405, -0.1521459510048163710 ) ) ;
#6213=CARTESIAN_POINT ( 'NONE',  ( -0.7853767243149117894, 19.84627995571224091, 3.566713853412147195 ) ) ;
#6216=APPLICATION_CONTEXT ( 'automotive_design' ) ;
#6220=CARTESIAN_POINT ( 'NONE',  ( 11.08655503941167808, 19.16255833366876260, 6.076062753481236811 ) ) ;
#6222=CARTESIAN_POINT ( 'NONE',  ( 3.804155136816291805, 15.46201706931346465, -1.459015595820115196 ) ) ;
#6225=CARTESIAN_POINT ( 'NONE',  ( 6.537126953640395755, 11.68813007582838281, 2.803481180618996316 ) ) ;
#6234=CARTESIAN_POINT ( 'NONE',  ( 10.10020702742011345, 20.09850238419586788, -1.233466479950767747 ) ) ;
#6237=CARTESIAN_POINT ( 'NONE',  ( 1.089698143903370164, 18.39942038070247676, 8.297769702651454082 ) ) ;
#6247=CARTESIAN_POINT ( 'NONE',  ( 7.626071724256386020, 18.07321731131985842, -1.931034283370769877 ) ) ;
#6250=CARTESIAN_POINT ( 'NONE',  ( 8.404128694230886154, 21.35170238401046205, -0.1542871241044822539 ) ) ;
#6255=EDGE_CURVE ( 'NONE', #21636, #8132, #2844, .T. ) ;
#6262=CARTESIAN_POINT ( 'NONE',  ( 5.488110206262358126, 13.84264232191805100, 8.338955251487456977 ) ) ;
#6265=CARTESIAN_POINT ( 'NONE',  ( 4.408559984239932561, 20.45280785655899436, 0.4597285100094092303 ) ) ;
#6270=CARTESIAN_POINT ( 'NONE',  ( 2.316111848326288136, 12.35794879854923778, 2.694249400427293661 ) ) ;
#6275=CARTESIAN_POINT ( 'NONE',  ( 2.228897815535521243, 11.62399859808463276, 2.403690802849292041 ) ) ;
#6285=CARTESIAN_POINT ( 'NONE',  ( 8.738383752483903422, 18.26872045576617865, 7.110093598169133777 ) ) ;
#6287=CARTESIAN_POINT ( 'NONE',  ( 10.96708857545880278, 16.60965070755050732, -4.348602899851927717 ) ) ;
#6291=CARTESIAN_POINT ( 'NONE',  ( 8.327267709314158495, 20.16378942260824303, 5.275824550407316238 ) ) ;
#6293=CARTESIAN_POINT ( 'NONE',  ( 3.191353643069211543, 17.79477638262715189, 8.193924954953159201 ) ) ;
#6298=CARTESIAN_POINT ( 'NONE',  ( 13.48553132191480763, 22.15489287403912400, 1.921071336905035842 ) ) ;
#6302=CARTESIAN_POINT ( 'NONE',  ( 1.593482295714299557, 17.10159210520789586, 9.552994227452236586 ) ) ;
#6305=CARTESIAN_POINT ( 'NONE',  ( 6.667155597571054138, 19.52118532600693968, 6.488507913781226044 ) ) ;
#6312=CARTESIAN_POINT ( 'NONE',  ( 11.23181352795878141, 22.17023050789328309, 2.056103838605086498 ) ) ;
#6314=CARTESIAN_POINT ( 'NONE',  ( 9.164819943473123232, 13.37848835739949038, -2.805861135747332202 ) ) ;
#6317=CARTESIAN_POINT ( 'NONE',  ( 8.699141033147567370, 20.29604414026289660, 6.341648953013584666 ) ) ;
#6319=CARTESIAN_POINT ( 'NONE',  ( 2.391745392645233892, 20.09535866699502193, 6.285321213869885071 ) ) ;
#6325=CARTESIAN_POINT ( 'NONE',  ( 12.78645908641997941, 20.00510796315846207, 5.045423586650715109 ) ) ;
#6327=CARTESIAN_POINT ( 'NONE',  ( 0.1330856713724426765, 12.52330284320706077, 1.635176554771325064 ) ) ;
#6331=CARTESIAN_POINT ( 'NONE',  ( 6.768681381451962409, 11.33814276891691186, 2.708583584588580173 ) ) ;
#6337=CARTESIAN_POINT ( 'NONE',  ( 10.91631540834134206, 12.36537083236676082, 4.900493360693962686 ) ) ;
#6340=CARTESIAN_POINT ( 'NONE',  ( 9.740401853436322810, 19.04328518575157858, -2.119098382970255656 ) ) ;
#6344=CARTESIAN_POINT ( 'NONE',  ( 1.095999888774144893, 17.17955240639085801, 9.025385985431823244 ) ) ;
#6348=CARTESIAN_POINT ( 'NONE',  ( 3.733612400581542090, 15.38343507826679257, -0.5588609866527980419 ) ) ;
#6357=CARTESIAN_POINT ( 'NONE',  ( 6.090447438359761989, 11.87235548079908298, 1.620859727200755440 ) ) ;
#6359=CARTESIAN_POINT ( 'NONE',  ( 9.503040939678710330, 14.64581734927065249, 7.855185963858965614 ) ) ;
#6371=CARTESIAN_POINT ( 'NONE',  ( 1.638698297806659543, 15.58835493759099400, 9.687949104223214647 ) ) ;
#6374=CARTESIAN_POINT ( 'NONE',  ( 3.511412721642198420, 15.31161194722795216, -1.319329340395489325 ) ) ;
#6380=CARTESIAN_POINT ( 'NONE',  ( 0.5972649247965632346, 12.28758346551315661, 4.089179521135787532 ) ) ;
#6386=CARTESIAN_POINT ( 'NONE',  ( 4.000040237993640169, 12.73801256019466699, 1.129472658065480806 ) ) ;
#6391=CARTESIAN_POINT ( 'NONE',  ( 1.818456832593254191, 17.60937233235423349, -0.5547632684056083008 ) ) ;
#6401=CARTESIAN_POINT ( 'NONE',  ( 8.907572712854108232, 13.29753225131360139, 6.491457205961016719 ) ) ;
#6408=CARTESIAN_POINT ( 'NONE',  ( 8.218225581203913777, 11.57903772877708093, 1.939056832797267704 ) ) ;
#6415=CARTESIAN_POINT ( 'NONE',  ( 4.133078020274367326, 11.26694048801452119, 2.004190681395073170 ) ) ;
#6416=CARTESIAN_POINT ( 'NONE',  ( 1.656824918492299847, 16.43570309294506870, 9.610848083271367415 ) ) ;
#6419=CARTESIAN_POINT ( 'NONE',  ( 3.810589158948427535, 17.18860055147588994, -0.6831702454440164995 ) ) ;
#6427=CARTESIAN_POINT ( 'NONE',  ( 10.33952242563266744, 21.01595720978967918, 5.389057817419801388 ) ) ;
#6429=CARTESIAN_POINT ( 'NONE',  ( 9.951424491271426476, 20.70236077687740206, -1.727763842408016393 ) ) ;
#6432=EDGE_CURVE ( 'NONE', #8132, #21636, #17098, .T. ) ;
#6434=CARTESIAN_POINT ( 'NONE',  ( 6.842398409408770199, 21.43872775588835111, 1.301663748024633804 ) ) ;
#6437=CARTESIAN_POINT ( 'NONE',  ( 2.360830742822978667, 19.25518317520560174, 1.052360069546889987 ) ) ;
#6438=CARTESIAN_POINT ( 'NONE',  ( 6.396056618077795797, 11.71523274630726164, 2.847703469759983008 ) ) ;
#6439=CARTESIAN_POINT ( 'NONE',  ( 6.615032896206390234, 19.57687688253193770, 6.294354736441118980 ) ) ;
#6442=CARTESIAN_POINT ( 'NONE',  ( 7.696359196369368050, 14.62096091062142023, -2.088485338917269729 ) ) ;
#6443=CARTESIAN_POINT ( 'NONE',  ( 5.119829882126274434, 17.94946437092776392, 7.743928121518011132 ) ) ;
#6446=CARTESIAN_POINT ( 'NONE',  ( 7.711067097055989805, 13.03499949018002191, 7.247388574493073499 ) ) ;
#6451=CARTESIAN_POINT ( 'NONE',  ( 6.468185970740263357, 11.70956081790287051, 2.825690715312092038 ) ) ;
#6457=CARTESIAN_POINT ( 'NONE',  ( 11.15047342604716363, 13.70924040045908221, 6.092156091579346011 ) ) ;
#6462=CARTESIAN_POINT ( 'NONE',  ( 12.81596010970969068, 18.61745565307525041, 5.882957067036275411 ) ) ;
#6466=CARTESIAN_POINT ( 'NONE',  ( -0.9505311321298592908, 20.13283946025274318, 4.032600115501251636 ) ) ;
#6474=CARTESIAN_POINT ( 'NONE',  ( 0.4093006246296175821, 18.44896716303925643, 1.333896071427123076 ) ) ;
#6477=CARTESIAN_POINT ( 'NONE',  ( 9.237080217971490370, 15.41846441754162456, -2.863985544511726378 ) ) ;
#6478=CARTESIAN_POINT ( 'NONE',  ( 3.009791520067166104, 20.22182912478766426, 2.433118109139212226 ) ) ;
#6480=CARTESIAN_POINT ( 'NONE',  ( 12.91314300807607474, 11.26870765665696084, 4.644675481207224621 ) ) ;
#6485=CARTESIAN_POINT ( 'NONE',  ( 9.120425135976756081, 21.04856296946614336, 1.778270776082491622 ) ) ;
#6486=CARTESIAN_POINT ( 'NONE',  ( 5.359841762299309309, 15.44500604033330404, -2.196771070663687375 ) ) ;
#6492=CARTESIAN_POINT ( 'NONE',  ( 3.312557453758251391, 18.28455830479323652, 8.964874161621944282 ) ) ;
#6495=CARTESIAN_POINT ( 'NONE',  ( 6.345927281321680269, 20.98284991768050389, 5.697012443342495125 ) ) ;
#6504=CARTESIAN_POINT ( 'NONE',  ( 13.37230979461818237, 18.77374700936764285, 6.607210930384802339 ) ) ;
#6505=CARTESIAN_POINT ( 'NONE',  ( 4.367181163445200909, 11.96053466636032248, 2.834654086721348776 ) ) ;
#6508=FACE_OUTER_BOUND ( 'NONE', #21544, .T. ) ;
#6511=CARTESIAN_POINT ( 'NONE',  ( 2.220423517640655042, 19.49008684387294110, 0.3265225556390483064 ) ) ;
#6520=CARTESIAN_POINT ( 'NONE',  ( 6.640128354688219048, 20.89828364148222306, 1.681561550837193053 ) ) ;
#6527=CARTESIAN_POINT ( 'NONE',  ( 8.778734981106474322, 11.92537842860997266, 4.412194450849771243 ) ) ;
#6529=CARTESIAN_POINT ( 'NONE',  ( 7.062963379299048938, 12.66652504735844609, 5.873350661943272044 ) ) ;
#6533=CARTESIAN_POINT ( 'NONE',  ( 7.106325486155565585, 11.65952799072720047, 6.014680116311857283 ) ) ;
#6534=CARTESIAN_POINT ( 'NONE',  ( 0.1952384575209598350, 18.78947810346299718, 0.6406485339171671400 ) ) ;
#6537=CARTESIAN_POINT ( 'NONE',  ( 3.543013425253076054, 14.97059756667285058, 8.287472907696502133 ) ) ;
#6543=CARTESIAN_POINT ( 'NONE',  ( 12.84123145286963563, 11.26511959538250096, 4.668661225537280579 ) ) ;
#6545=CARTESIAN_POINT ( 'NONE',  ( 9.172305780378046336, 17.26398718446571223, -3.555164033155447267 ) ) ;
#6547=CARTESIAN_POINT ( 'NONE',  ( 9.025443331680945036, 19.27445160448637296, 7.159428889452720490 ) ) ;
#6549=CARTESIAN_POINT ( 'NONE',  ( 5.279567021499281587, 14.21946822237472752, 7.642569973796522476 ) ) ;
#6552=CARTESIAN_POINT ( 'NONE',  ( 5.932080435518681583, 13.78737461787913077, -1.327312924921903114 ) ) ;
#6555=CARTESIAN_POINT ( 'NONE',  ( 0.3694878298779649128, 20.96126479766088124, 6.369946474118858504 ) ) ;
#6559=CARTESIAN_POINT ( 'NONE',  ( 6.757070482422969704, 11.22565637327918253, 2.703836977927735585 ) ) ;
#6568=CARTESIAN_POINT ( 'NONE',  ( 13.15388200968041055, 15.89351787639128233, 6.392798759906445305 ) ) ;
#6577=CARTESIAN_POINT ( 'NONE',  ( 6.010033701850474586, 11.35695304730319144, 2.937139218883811242 ) ) ;
#6580=CARTESIAN_POINT ( 'NONE',  ( 10.10053423927090677, 20.26417264612534197, -1.196608788579085259 ) ) ;
#6585=CARTESIAN_POINT ( 'NONE',  ( 5.756884206421248429, 19.23872087217396398, -1.498017244082868960 ) ) ;
#6589=CARTESIAN_POINT ( 'NONE',  ( 10.72300197756324103, 19.12441493153400174, 5.966615969704548661 ) ) ;
#6590=CARTESIAN_POINT ( 'NONE',  ( 13.39295492035073920, 16.76849418036265149, 7.268524437313808484 ) ) ;
#6595=CARTESIAN_POINT ( 'NONE',  ( 0.1886871975376354371, 20.96126479766088124, 6.424089978990833671 ) ) ;
#6598=CARTESIAN_POINT ( 'NONE',  ( 4.697672132164100844, 20.97227537427880151, 1.222830952479448952 ) ) ;
#6604=CARTESIAN_POINT ( 'NONE',  ( 6.128459561466241823, 11.10665485570860156, 1.321687314850935824 ) ) ;
#6607=CARTESIAN_POINT ( 'NONE',  ( 2.467395655297200729, 20.16159473827618243, 0.9463460702680616121 ) ) ;
#6614=CARTESIAN_POINT ( 'NONE',  ( 10.67670849270701439, 19.10987469415690043, 6.120482877392228183 ) ) ;
#6621=CARTESIAN_POINT ( 'NONE',  ( 9.082171594463483544, 12.91581074416477115, 5.837840052964735627 ) ) ;
#6626=CARTESIAN_POINT ( 'NONE',  ( 0.4730996965358145179, 19.72362395832615078, 1.304202306971568026 ) ) ;
#6629=CARTESIAN_POINT ( 'NONE',  ( 7.098541355495150640, 12.34712571434790007, 5.562580927991336743 ) ) ;
#6634=CARTESIAN_POINT ( 'NONE',  ( 12.77646214304486527, 18.77374700936764285, 6.785646590749020213 ) ) ;
#6637=CARTESIAN_POINT ( 'NONE',  ( 12.41829272412508089, 20.89413022119176944, 5.033827648320388093 ) ) ;
#6640=CARTESIAN_POINT ( 'NONE',  ( 6.099948198004060629, 20.15547429746715125, -0.6732643854471319633 ) ) ;
#6644=CARTESIAN_POINT ( 'NONE',  ( 6.256308338986228179, 11.80107813750363732, 2.226400015944866695 ) ) ;
#6649=CARTESIAN_POINT ( 'NONE',  ( 6.294043155411415569, 19.02104356353402181, -1.302222655867340428 ) ) ;
#6651=CARTESIAN_POINT ( 'NONE',  ( 5.228545106021627475, 13.24170083984223290, 6.829111360130051267 ) ) ;
#6653=CARTESIAN_POINT ( 'NONE',  ( -0.07815241983022847005, 13.90637430850843081, 0.5352566576402777443 ) ) ;
#6657=CARTESIAN_POINT ( 'NONE',  ( 1.342949756012494333, 17.16067149510373469, 8.863113058879841688 ) ) ;
#6662=CARTESIAN_POINT ( 'NONE',  ( 10.79420638430738855, 11.98813216246191793, 4.338092415360138787 ) ) ;
#6666=CARTESIAN_POINT ( 'NONE',  ( 12.76598846464055192, 11.97584668644513606, 4.063973834900838966 ) ) ;
#6668=CARTESIAN_POINT ( 'NONE',  ( 6.214991440876061368, 11.01927814362272251, 2.094123509549327355 ) ) ;
#6677=CARTESIAN_POINT ( 'NONE',  ( 6.105958985786053006, 11.57849375196054176, 2.924589247399322911 ) ) ;
#6682=CARTESIAN_POINT ( 'NONE',  ( 10.67714358499520522, 11.64784025693482228, 3.885139017224132019 ) ) ;
#6684=CARTESIAN_POINT ( 'NONE',  ( 3.459290721496041776, 20.55082906393983322, 3.602416572006893691 ) ) ;
#6686=CARTESIAN_POINT ( 'NONE',  ( 9.922397446926728648, 11.51584134576680363, 0.4461043797960159152 ) ) ;
#6688=CARTESIAN_POINT ( 'NONE',  ( 6.011841773132246658, 11.11134465255707937, 1.358372952244610854 ) ) ;
#6692=CARTESIAN_POINT ( 'NONE',  ( 8.793583754241840467, 20.84408765773402195, 0.9049662790635636389 ) ) ;
#6693=CARTESIAN_POINT ( 'NONE',  ( 7.243059079953789947, 16.38024503317697622, -3.009810408447084473 ) ) ;
#6697=CARTESIAN_POINT ( 'NONE',  ( 11.60020922121511155, 20.23341255231735758, -2.977328076712147276 ) ) ;
#6699=CARTESIAN_POINT ( 'NONE',  ( 3.509209820245474898, 17.35406872798134259, -1.425442992431726452 ) ) ;
#6702=CARTESIAN_POINT ( 'NONE',  ( 7.237772546668600704, 18.50866281033818694, 7.944204046336037273 ) ) ;
#6708=CARTESIAN_POINT ( 'NONE',  ( 0.09188070044341151155, 13.96121064407340739, 1.549658560270714025 ) ) ;
#6712=CARTESIAN_POINT ( 'NONE',  ( 1.967132827584114008, 13.73989441795974287, 0.9368391563488658313 ) ) ;
#6718=CARTESIAN_POINT ( 'NONE',  ( 1.800420485084554656, 13.16437343919289660, 0.4094432821608885997 ) ) ;
#6724=CARTESIAN_POINT ( 'NONE',  ( 7.934317618220886104, 19.55588805595618140, -1.064466008449746592 ) ) ;
#6734=CARTESIAN_POINT ( 'NONE',  ( 9.260356396371024701, 15.85449124615785976, 7.206070117100887629 ) ) ;
#6739=CARTESIAN_POINT ( 'NONE',  ( 0.2450306102960222998, 18.98085523423504739, 0.7556970042913269126 ) ) ;
#6742=CARTESIAN_POINT ( 'NONE',  ( 0.7434690279575192351, 12.30129727290108121, 3.312830165727216336 ) ) ;
#6749=CARTESIAN_POINT ( 'NONE',  ( 10.85821570307754946, 12.08730048838598314, 5.903571453362351562 ) ) ;
#6750=CARTESIAN_POINT ( 'NONE',  ( 12.00567213455676452, 21.57614686056444953, 3.916759121994844328 ) ) ;
#6755=CARTESIAN_POINT ( 'NONE',  ( 9.479939784920428991, 14.42918437847127144, 7.660713865854686055 ) ) ;
#6756=CARTESIAN_POINT ( 'NONE',  ( 0.4361718258524748815, 18.57760016544011705, 1.300908314747322825 ) ) ;
#6759=CARTESIAN_POINT ( 'NONE',  ( 7.312436962488203740, 15.85013007038090649, 7.611556540862124187 ) ) ;
#6763=CARTESIAN_POINT ( 'NONE',  ( 6.499174407287954480, 11.49185006667808118, 1.355446987389384850 ) ) ;
#6764=CARTESIAN_POINT ( 'NONE',  ( 3.643499464412459421, 13.65298187125114282, -0.8458288619479169546 ) ) ;
#6767=CARTESIAN_POINT ( 'NONE',  ( 4.933961842320149671, 18.75973248553390604, 7.440319485191550619 ) ) ;
#6774=CARTESIAN_POINT ( 'NONE',  ( 11.05115549428196253, 12.98897226662114157, 5.556954956783895838 ) ) ;
#6775=CARTESIAN_POINT ( 'NONE',  ( 11.05569795298371716, 18.99266784705168831, 6.938303826124779583 ) ) ;
#6778=EDGE_CURVE ( 'NONE', #14025, #1010, #12092, .T. ) ;
#6779=CARTESIAN_POINT ( 'NONE',  ( 12.48283250700034763, 11.39445025475912132, 2.811724565135549359 ) ) ;
#6783=CARTESIAN_POINT ( 'NONE',  ( 2.855769952450744054, 12.51757774536594070, 6.616514325381632311 ) ) ;
#6794=CARTESIAN_POINT ( 'NONE',  ( 12.40836789703437759, 11.21920808676120274, 2.564551607113802589 ) ) ;
#6795=CARTESIAN_POINT ( 'NONE',  ( 3.051097452952215683, 20.26740773906408322, 2.539636754529451146 ) ) ;
#6796=CARTESIAN_POINT ( 'NONE',  ( 12.82150885573869026, 11.94669871286416196, 4.209032338432463938 ) ) ;
#6797=CARTESIAN_POINT ( 'NONE',  ( 5.701977129479173456, 12.65090407144326257, 6.796530866308510888 ) ) ;
#6798=CARTESIAN_POINT ( 'NONE',  ( 10.40241334969972264, 21.01184353768176294, 5.367285860140727394 ) ) ;
#6804=CARTESIAN_POINT ( 'NONE',  ( 10.92372992060199799, 18.30785699476917827, 6.420144728694466174 ) ) ;
#6805=CARTESIAN_POINT ( 'NONE',  ( 9.160249483111522650, 13.32481467742428016, -2.920332793413628281 ) ) ;
#6809=CARTESIAN_POINT ( 'NONE',  ( 11.20169135129352789, 18.59438219489337740, -3.945768465746844367 ) ) ;
#6812=CARTESIAN_POINT ( 'NONE',  ( -0.6214517246260686800, 21.02721105424156178, 4.868466575270438135 ) ) ;
#6815=CARTESIAN_POINT ( 'NONE',  ( 6.898105259049923887, 19.81015148077474919, 7.136496755853531049 ) ) ;
#6818=CARTESIAN_POINT ( 'NONE',  ( 0.4630128912319489976, 12.46612062059815251, 3.460377433718159423 ) ) ;
#6821=CARTESIAN_POINT ( 'NONE',  ( 2.015936624292824053, 13.40476583923045162, 1.212685581759113340 ) ) ;
#6827=CARTESIAN_POINT ( 'NONE',  ( 1.737391270568420465, 16.91513162182804209, -0.6717990871026022770 ) ) ;
#6841=CARTESIAN_POINT ( 'NONE',  ( 10.02870747286891273, 20.26079639706886226, -1.172339910205614011 ) ) ;
#6842=CARTESIAN_POINT ( 'NONE',  ( 5.667562314204174889, 21.64188095357850372, 3.777664677578456143 ) ) ;
#6848=CARTESIAN_POINT ( 'NONE',  ( 9.239775580759724605, 14.16665682807454196, 6.724960839789129174 ) ) ;
#6854=CARTESIAN_POINT ( 'NONE',  ( -0.06155728683911870780, 13.26885766964012170, 1.106704240812302897 ) ) ;
#6858=CARTESIAN_POINT ( 'NONE',  ( 6.170767000723442308, 12.01572996145620209, 1.412382460721507194 ) ) ;
#6865=CARTESIAN_POINT ( 'NONE',  ( 13.47935068733434250, 22.20657701893900082, 2.459632543707202412 ) ) ;
#6867=CARTESIAN_POINT ( 'NONE',  ( 12.10789021220345241, 21.43823440121504120, 4.195907106397960717 ) ) ;
#6871=CARTESIAN_POINT ( 'NONE',  ( 9.406149962978091139, 13.41239259737459122, 7.189453753586981577 ) ) ;
#6872=CARTESIAN_POINT ( 'NONE',  ( 4.031802018818064326, 20.53258833712626341, 5.054834409609300749 ) ) ;
#6875=CARTESIAN_POINT ( 'NONE',  ( 7.325542279612724528, 15.26830868317408019, 7.512093565127778483 ) ) ;
#6878=CARTESIAN_POINT ( 'NONE',  ( 6.156360451388549926, 12.39088710148332062, -0.1838423150655557059 ) ) ;
#6880=CARTESIAN_POINT ( 'NONE',  ( 5.668910838604148239, 13.84264232191805100, 8.284811746615043049 ) ) ;
#6887=CARTESIAN_POINT ( 'NONE',  ( 11.32797118285666116, 17.32754504092519454, 7.499948195778106452 ) ) ;
#6890=CARTESIAN_POINT ( 'NONE',  ( 13.11430928665658513, 13.86836039950025601, 5.796722067417751312 ) ) ;
#6892=CARTESIAN_POINT ( 'NONE',  ( 3.155748942043203442, 20.73071249212684108, 3.672874311289710203 ) ) ;
#6899=CARTESIAN_POINT ( 'NONE',  ( 8.510511870354847019, 20.63131727706956298, 0.2009566961665696649 ) ) ;
#6900=CARTESIAN_POINT ( 'NONE',  ( 3.560108861471142916, 20.57711495788742440, 3.866665624095278808 ) ) ;
#6901=CARTESIAN_POINT ( 'NONE',  ( 10.78593073986782613, 19.11233889549468046, 6.091437666761631675 ) ) ;
#6902=CARTESIAN_POINT ( 'NONE',  ( 5.440308256469632120, 21.03084409073214189, 1.977388168171128058 ) ) ;
#6903=CARTESIAN_POINT ( 'NONE',  ( 9.756654189145164580, 21.83905339296156356, 3.605447077296963343 ) ) ;
#6911=CARTESIAN_POINT ( 'NONE',  ( 8.231392512103436587, 19.97299568257830060, -0.5599668506537556212 ) ) ;
#6912=CARTESIAN_POINT ( 'NONE',  ( 9.082225001358835925, 11.50047795576720233, 5.498903420274817933 ) ) ;
#6916=CARTESIAN_POINT ( 'NONE',  ( 1.365433128829952825, 14.65425108942523558, -0.3328239235251538308 ) ) ;
#6919=CARTESIAN_POINT ( 'NONE',  ( 7.490479816045854555, 16.63476421355041879, 8.383926577843272554 ) ) ;
#6922=CARTESIAN_POINT ( 'NONE',  ( 0.4729859817002137201, 12.44863435665195084, 3.507523896227905613 ) ) ;
#6931=CARTESIAN_POINT ( 'NONE',  ( 3.555789604696411477, 21.36866284792075987, 3.849869910478822987 ) ) ;
#6941=CARTESIAN_POINT ( 'NONE',  ( 6.315595396583606913, 20.04364414270774120, 0.2372624680991833601 ) ) ;
#6942=CARTESIAN_POINT ( 'NONE',  ( 6.875778001922447480, 20.09399725779506340, 7.023170949626798887 ) ) ;
#6950=CARTESIAN_POINT ( 'NONE',  ( 7.670747655007784438, 17.97917197181799764, -1.865092139437078300 ) ) ;
#6956=CARTESIAN_POINT ( 'NONE',  ( -0.03530231612252059809, 13.09097027921703749, 1.245598840680120167 ) ) ;
#6959=CARTESIAN_POINT ( 'NONE',  ( 1.638778877848424687, 13.09009564387116065, 7.486132227913222081 ) ) ;
#6964=CARTESIAN_POINT ( 'NONE',  ( 8.794480080286872337, 21.87018156742340125, 1.773917468153012322 ) ) ;
#6966=CARTESIAN_POINT ( 'NONE',  ( 11.60172015861852834, 21.94098819457760285, 2.803563881665107616 ) ) ;
#6970=CARTESIAN_POINT ( 'NONE',  ( 8.234954911211584516, 10.76337410253292148, 2.037235491473907700 ) ) ;
#6971=CARTESIAN_POINT ( 'NONE',  ( 3.962787389995165110, 12.81957249642222152, 0.8790192768804812040 ) ) ;
#6974=CARTESIAN_POINT ( 'NONE',  ( 5.588254505849169718, 15.45064704472125250, -1.305107587893242105 ) ) ;
#6979=CARTESIAN_POINT ( 'NONE',  ( 8.585932752112777067, 20.96234599748222038, 4.772909305667436541 ) ) ;
#6980=CARTESIAN_POINT ( 'NONE',  ( 5.731357535509370216, 21.64685404058683815, 3.758912427147279356 ) ) ;
#6983=CARTESIAN_POINT ( 'NONE',  ( 1.941381905217177017, 13.53119643653954363, 0.9980600641242322046 ) ) ;
#6989=CARTESIAN_POINT ( 'NONE',  ( 10.36888746642220305, 20.99033332477807079, 5.185665849892854951 ) ) ;
#6992=CARTESIAN_POINT ( 'NONE',  ( 11.18318634076747742, 16.39223678439043397, -3.590085582233933259 ) ) ;
#6994=CARTESIAN_POINT ( 'NONE',  ( 3.931218227739150528, 11.94740837896324237, 2.317032250256635173 ) ) ;
#6999=CARTESIAN_POINT ( 'NONE',  ( 4.520744627033614016, 19.76795696472709452, 0.8556426533025034420 ) ) ;
#7002=CARTESIAN_POINT ( 'NONE',  ( 6.045917078792466093, 11.48351223332058346, 2.935635005282488663 ) ) ;
#7005=CARTESIAN_POINT ( 'NONE',  ( 9.544384125417266773, 12.37431098505726013, -1.081075134452434749 ) ) ;
#7006=CARTESIAN_POINT ( 'NONE',  ( 3.265424270076857205, 20.45664453107361069, 3.095604235058887266 ) ) ;
#7007=CARTESIAN_POINT ( 'NONE',  ( 6.745733615097072366, 11.82482810032952081, 4.272283726952619709 ) ) ;
#7008=CARTESIAN_POINT ( 'NONE',  ( 5.789917961221411780, 17.41457342482845405, 8.273797100034885332 ) ) ;
#7009=CARTESIAN_POINT ( 'NONE',  ( 13.23690675162799479, 12.74100552075486270, 6.152686933467335528 ) ) ;
#7014=CARTESIAN_POINT ( 'NONE',  ( 11.21878411960198463, 15.42120748821763598, 6.735290914777061211 ) ) ;
#7015=CARTESIAN_POINT ( 'NONE',  ( 9.052665478973109359, 15.28237876918361948, -3.641785826635130174 ) ) ;
#7017=CARTESIAN_POINT ( 'NONE',  ( 9.367590232042878995, 13.71580197176839633, -2.112308633255299384 ) ) ;
#7021=CARTESIAN_POINT ( 'NONE',  ( 4.354639731569010408, 20.46779201619338195, 6.887242084015990251 ) ) ;
#7024=CARTESIAN_POINT ( 'NONE',  ( 7.297179034909929030, 12.43031178068008558, 6.778800246622879833 ) ) ;
#7029=CARTESIAN_POINT ( 'NONE',  ( 2.101062743772215580, 12.98372264194903636, 1.656677011360439877 ) ) ;
#7030=CARTESIAN_POINT ( 'NONE',  ( 3.736893377926853610, 14.96998944597854653, -0.4414175379438642910 ) ) ;
#7035=CARTESIAN_POINT ( 'NONE',  ( 3.998154558026791872, 21.25887251078221496, 5.050199523078231501 ) ) ;
#7049=CARTESIAN_POINT ( 'NONE',  ( 6.855085254147958551, 20.81034843036036008, 1.644237685604219790 ) ) ;
#7050=CARTESIAN_POINT ( 'NONE',  ( 1.179035820486476593, 11.63764180229748213, 6.543292337723209506 ) ) ;
#7053=CARTESIAN_POINT ( 'NONE',  ( 5.114825480111228728, 11.70051646708293269, 6.098904411201394815 ) ) ;
#7060=CARTESIAN_POINT ( 'NONE',  ( 7.752716165273062288, 18.41075878025652557, -1.699111224125438024 ) ) ;
#7067=CARTESIAN_POINT ( 'NONE',  ( 2.112882994232062828, 21.07822518102817000, 5.653028666727347940 ) ) ;
#7071=CARTESIAN_POINT ( 'NONE',  ( 1.011698528169785005, 19.61962022855508181, 7.364809558829694680 ) ) ;
#7077=CARTESIAN_POINT ( 'NONE',  ( 10.47598215385642639, 10.97943152176106274, 4.232648866062586279 ) ) ;
#7080=CARTESIAN_POINT ( 'NONE',  ( 12.60809324200862314, 20.43343092864591881, 5.533879428115382026 ) ) ;
#7085=CARTESIAN_POINT ( 'NONE',  ( 9.182002370748412190, 12.08590500130187628, 6.093407161457568222 ) ) ;
#7086=CARTESIAN_POINT ( 'NONE',  ( 7.082014623697716615, 18.17920521194865913, 7.349654649369399273 ) ) ;
#7089=CARTESIAN_POINT ( 'NONE',  ( 5.588162325894102445, 14.98248962140982599, -1.190334577872725230 ) ) ;
#7094=CARTESIAN_POINT ( 'NONE',  ( 11.65780787164172594, 18.24951553479433031, -3.906928721014021555 ) ) ;
#7095=CARTESIAN_POINT ( 'NONE',  ( 5.184282268542144578, 13.02144258489116702, 6.600906927883145592 ) ) ;
#7098=CARTESIAN_POINT ( 'NONE',  ( 2.170325927336617777, 11.82982598436980126, 1.730999371418365129 ) ) ;
#7099=CARTESIAN_POINT ( 'NONE',  ( 0.8193983463107750165, 20.11811364056184459, 7.806734921283819517 ) ) ;
#7101=CARTESIAN_POINT ( 'NONE',  ( 3.987335596668034388, 20.53326216353070421, 5.068335100042532737 ) ) ;
#7111=CARTESIAN_POINT ( 'NONE',  ( 11.44031352510691946, 15.54975579857636880, 7.527537594959339273 ) ) ;
#7114=CARTESIAN_POINT ( 'NONE',  ( 12.32163425866073148, 11.24196547682344161, 2.114862982211144438 ) ) ;
#7116=CARTESIAN_POINT ( 'NONE',  ( 6.969861975853656411, 13.41850193825106174, 6.940434113064578803 ) ) ;
#7120=CARTESIAN_POINT ( 'NONE',  ( 0.2363768735086284323, 20.63358941134637092, 5.024770624937192842 ) ) ;
#7127=CARTESIAN_POINT ( 'NONE',  ( 7.744502704386849068, 18.07137575567074350, -1.961665155297699137 ) ) ;
#7128=CARTESIAN_POINT ( 'NONE',  ( 4.355808376242262803, 20.06831615587024586, 5.938053330416548370 ) ) ;
#7129=CARTESIAN_POINT ( 'NONE',  ( 5.988546274437528183, 18.80336625489407965, -0.8540819367508141191 ) ) ;
#7130=CARTESIAN_POINT ( 'NONE',  ( 7.492294575654238287, 12.00122113815488056, 5.673272314834056473 ) ) ;
#7131=CARTESIAN_POINT ( 'NONE',  ( 9.028821228240033747, 11.50047795576720233, 5.514895994043016891 ) ) ;
#7139=CARTESIAN_POINT ( 'NONE',  ( 11.16823954825894205, 13.89705342359357054, 6.200388406566677446 ) ) ;
#7140=CARTESIAN_POINT ( 'NONE',  ( 5.792514709454430921, 19.23872087217396398, -1.508687341247886948 ) ) ;
#7144=CARTESIAN_POINT ( 'NONE',  ( 10.28716446386076555, 11.36762743660578145, 2.108319987653204830 ) ) ;
#7147=CARTESIAN_POINT ( 'NONE',  ( 4.701992403669415843, 11.43043024698558163, 5.679938558605459598 ) ) ;
#7150=CARTESIAN_POINT ( 'NONE',  ( 7.494300422474976742, 13.81960511660041746, 7.795597158064130561 ) ) ;
#7156=ORIENTED_EDGE ( 'NONE', *, *, #21877, .F. ) ;
#7158=CARTESIAN_POINT ( 'NONE',  ( 1.933308127472557647, 14.06219242987879703, 0.7237907644290267895 ) ) ;
#7173=CARTESIAN_POINT ( 'NONE',  ( 12.98496071183864586, 13.22236995718078134, 5.543149843602365401 ) ) ;
#7174=CARTESIAN_POINT ( 'NONE',  ( 5.603942890132661780, 13.84493627167355179, 8.299647925973943074 ) ) ;
#7177=CARTESIAN_POINT ( 'NONE',  ( 4.319597228044323778, 11.18970892858293276, 2.675083765875428732 ) ) ;
#7182=CARTESIAN_POINT ( 'NONE',  ( 7.573246980053331967, 17.33572519892136654, -2.036030731767461521 ) ) ;
#7185=CARTESIAN_POINT ( 'NONE',  ( 3.427325199255271126, 15.53052183636367722, 8.374923869955427591 ) ) ;
#7192=CARTESIAN_POINT ( 'NONE',  ( 1.254300738082038125, 21.01230615663556023, 3.340964865855025945 ) ) ;
#7197=CARTESIAN_POINT ( 'NONE',  ( 0.5413756995750967915, 12.83134191367328292, 1.794410497042580266 ) ) ;
#7203=CARTESIAN_POINT ( 'NONE',  ( 10.89469307076425686, 21.76139788190002022, 2.134525428084244947 ) ) ;
#7206=CARTESIAN_POINT ( 'NONE',  ( 13.14944941967905301, 12.29607346375136068, 5.638298986518227807 ) ) ;
#7210=CARTESIAN_POINT ( 'NONE',  ( 9.015524272356790547, 11.53921692834158286, 5.350368841146013743 ) ) ;
#7211=CARTESIAN_POINT ( 'NONE',  ( 0.7257397583488034432, 19.54979116365418079, 7.396820614257542559 ) ) ;
#7213=CARTESIAN_POINT ( 'NONE',  ( 5.929260172323883360, 18.48292898978692023, -0.9131295676930929472 ) ) ;
#7215=CARTESIAN_POINT ( 'NONE',  ( 1.508768852107567504, 20.36732049711449832, 4.044819003516886724 ) ) ;
#7219=CARTESIAN_POINT ( 'NONE',  ( 11.74500383039051776, 15.67423727725497606, 7.485740281064174440 ) ) ;
#7220=CARTESIAN_POINT ( 'NONE',  ( 5.068394031931605426, 12.56749199890325208, 6.028102843334117722 ) ) ;
#7222=CARTESIAN_POINT ( 'NONE',  ( 5.075711589750377506, 21.42306324396562189, 1.964058843707486179 ) ) ;
#7223=CARTESIAN_POINT ( 'NONE',  ( 1.469492836360677179, 17.96208015702665861, 9.343845014913002345 ) ) ;
#7227=CARTESIAN_POINT ( 'NONE',  ( 6.282630550826245219, 11.65589518700730132, 2.475056272112619027 ) ) ;
#7233=CARTESIAN_POINT ( 'NONE',  ( 11.29708385613510657, 17.57508648399901574, 7.446457121411568458 ) ) ;
#7236=CARTESIAN_POINT ( 'NONE',  ( 11.96961372335506901, 11.26714859802527080, 0.6016620342287901657 ) ) ;
#7246=CARTESIAN_POINT ( 'NONE',  ( 6.809079960824258038, 11.82958596167992127, 4.252032552716304536 ) ) ;
#7247=CARTESIAN_POINT ( 'NONE',  ( 12.49792962410951525, 19.94285714604490067, 5.068850365372612465 ) ) ;
#7248=CARTESIAN_POINT ( 'NONE',  ( 1.957605007174791467, 13.96208391574584162, 8.945319323778717191 ) ) ;
#7249=CARTESIAN_POINT ( 'NONE',  ( 11.47115874364255994, 10.98707485392928085, -1.321792392077711487 ) ) ;
#7252=CARTESIAN_POINT ( 'NONE',  ( 11.06571474200560345, 17.46349345829840161, 6.690722436210692514 ) ) ;
#7253=CARTESIAN_POINT ( 'NONE',  ( 7.233972636490444863, 16.38025891712375781, -3.007816387549334003 ) ) ;
#7257=CARTESIAN_POINT ( 'NONE',  ( 9.677015374421488403, 12.13265719289923616, -0.5781317187935294255 ) ) ;
#7260=CARTESIAN_POINT ( 'NONE',  ( -1.007450280090600003, 20.72700438578640458, 3.842530817846650848 ) ) ;
#7273=ORIENTED_EDGE ( 'NONE', *, *, #5736, .F. ) ;
#7281=CARTESIAN_POINT ( 'NONE',  ( 11.51858435347932108, 11.70279650494946289, -0.9316420090841365242 ) ) ;
#7282=CARTESIAN_POINT ( 'NONE',  ( 7.549769109252762789, 16.64380874522678155, 8.484748712165586682 ) ) ;
#7284=CARTESIAN_POINT ( 'NONE',  ( 4.161695538953418705, 11.38564755976896237, 1.994139648140534904 ) ) ;
#7288=CARTESIAN_POINT ( 'NONE',  ( 7.685683886033650047, 12.68839834003130740, -0.4749676218993871823 ) ) ;
#7294=CARTESIAN_POINT ( 'NONE',  ( 2.579465434524714329, 20.56131833015633248, 6.894018011111492150 ) ) ;
#7297=CARTESIAN_POINT ( 'NONE',  ( 4.811918810904475485, 19.96663567226219982, 0.7225885738512296541 ) ) ;
#7303=CARTESIAN_POINT ( 'NONE',  ( 9.334271081287811356, 21.44638057025442279, 3.630935037030034618 ) ) ;
#7306=CARTESIAN_POINT ( 'NONE',  ( 11.56023901238583207, 10.99603790901469225, -1.079658926462704560 ) ) ;
#7310=CARTESIAN_POINT ( 'NONE',  ( 7.235594381361154959, 14.41299800172950185, -2.541178202713186618 ) ) ;
#7311=CARTESIAN_POINT ( 'NONE',  ( 6.005363321636888685, 12.27588422369934129, 0.9603231873459451284 ) ) ;
#7313=CARTESIAN_POINT ( 'NONE',  ( 6.035915765164218350, 18.90302373985587536, -0.6745700400264159624 ) ) ;
#7314=CARTESIAN_POINT ( 'NONE',  ( 7.303925134678800113, 14.37207998726623615, 7.210427461397269866 ) ) ;
#7319=CARTESIAN_POINT ( 'NONE',  ( 8.033113057174002591, 11.41928500448566375, -0.1748968685806625845 ) ) ;
#7324=CARTESIAN_POINT ( 'NONE',  ( 1.078174312258882273, 18.49964734577863368, 8.341151507176290281 ) ) ;
#7329=CARTESIAN_POINT ( 'NONE',  ( 11.41150532678066476, 14.07074566132039095, 7.133435626371687377 ) ) ;
#7333=CARTESIAN_POINT ( 'NONE',  ( 11.69498266538699838, 11.63108941959115050, -0.5923512581102406971 ) ) ;
#7343=CARTESIAN_POINT ( 'NONE',  ( 13.50039319234801383, 21.41212481752907948, 2.265780506769165203 ) ) ;
#7344=CARTESIAN_POINT ( 'NONE',  ( 8.142896893452514107, 20.59481639511846041, 4.729431829690726730 ) ) ;
#7351=CARTESIAN_POINT ( 'NONE',  ( 12.03751388135225042, 21.69121361356170397, 3.958262461564761914 ) ) ;
#7355=CARTESIAN_POINT ( 'NONE',  ( 9.294776336270766492, 15.47881463844799832, -2.777761849933970240 ) ) ;
#7357=CARTESIAN_POINT ( 'NONE',  ( 12.50057563193774790, 21.92868216252701075, -0.5501692431105187353 ) ) ;
#7358=CARTESIAN_POINT ( 'NONE',  ( 3.448783566482409135, 12.50969690204968288, 0.7605462683841421878 ) ) ;
#7361=CARTESIAN_POINT ( 'NONE',  ( 7.523395346134158501, 14.27362971915975187, 7.995196924124165605 ) ) ;
#7382=ORIENTED_EDGE ( 'NONE', *, *, #6255, .F. ) ;
#7384=CARTESIAN_POINT ( 'NONE',  ( 3.813066075967610047, 12.19982130767714246, 0.3790570318242228454 ) ) ;
#7387=CARTESIAN_POINT ( 'NONE',  ( 5.583684207161521584, 15.96835738058210019, 8.791436236743251698 ) ) ;
#7398=CARTESIAN_POINT ( 'NONE',  ( 3.138855641000511287, 19.23123867353615069, 8.310718164606276659 ) ) ;
#7401=CARTESIAN_POINT ( 'NONE',  ( 13.15085279376319782, 22.07249463472189888, 2.009202999722684790 ) ) ;
#7406=CARTESIAN_POINT ( 'NONE',  ( 11.55191247057558890, 21.31987603492770234, 3.934633224169304722 ) ) ;
#7409=CARTESIAN_POINT ( 'NONE',  ( 11.23781920621831176, 11.97727348665198299, -2.482949163614870169 ) ) ;
#7413=CARTESIAN_POINT ( 'NONE',  ( 7.709748992265566869, 19.45393663054224831, -2.000501698392521455 ) ) ;
#7414=CARTESIAN_POINT ( 'NONE',  ( 5.420926794907370727, 15.73778643695066393, 8.083040450566207014 ) ) ;
#7418=CARTESIAN_POINT ( 'NONE',  ( 5.593038387450195437, 14.77714803192029613, -1.122504005036815800 ) ) ;
#7421=CARTESIAN_POINT ( 'NONE',  ( 11.07182980542974171, 10.97943152176106274, 4.054213205698371070 ) ) ;
#7423=CARTESIAN_POINT ( 'NONE',  ( 1.569416217892126708, 17.33683664400565050, 9.619349279799264352 ) ) ;
#7424=CARTESIAN_POINT ( 'NONE',  ( 1.249608508386810257, 18.94596205324141280, 8.865697184473329884 ) ) ;
#7427=CARTESIAN_POINT ( 'NONE',  ( 7.037679341590383331, 18.17949408554134649, 7.363593253874445743 ) ) ;
#7433=CARTESIAN_POINT ( 'NONE',  ( 11.38595208427108929, 13.73655500858925116, 6.976298811495518670 ) ) ;
#7436=CARTESIAN_POINT ( 'NONE',  ( 11.34624642647743720, 12.79290754381931627, -2.192977170836705181 ) ) ;
#7438=CARTESIAN_POINT ( 'NONE',  ( 5.454630584850207242, 17.08472327719105266, -2.114810173200567966 ) ) ;
#7440=CARTESIAN_POINT ( 'NONE',  ( 3.096978994538255314, 17.95937840445101230, 8.244996092440942448 ) ) ;
#7447=CARTESIAN_POINT ( 'NONE',  ( 7.653781805100536850, 13.15088303497838140, -1.081001487685353313 ) ) ;
#7449=CARTESIAN_POINT ( 'NONE',  ( 12.83050491244006786, 11.94611577877984132, 4.206736490311723031 ) ) ;
#7451=CARTESIAN_POINT ( 'NONE',  ( 10.88501636984964804, 16.27139374001615835, -4.462695918007991480 ) ) ;
#7455=CARTESIAN_POINT ( 'NONE',  ( 4.415627886922138146, 20.84303989866938878, 6.171506294094559308 ) ) ;
#7462=CARTESIAN_POINT ( 'NONE',  ( 10.32898373000674219, 10.45400687491624225, 2.198347703374553763 ) ) ;
#7463=COLOUR_RGB ( '', 0.09019608, 0.27058824, 0.51372549) ;
#7466=CARTESIAN_POINT ( 'NONE',  ( 9.567093807291675134, 12.51404170299046648, -1.089912194315524330 ) ) ;
#7468=CARTESIAN_POINT ( 'NONE',  ( 0.6844633117439506975, 19.47873662827283425, 7.356147931787495153 ) ) ;
#7469=CARTESIAN_POINT ( 'NONE',  ( -1.273098367859926805, 20.20483442592724188, 3.536004553022368935 ) ) ;
#7478=CARTESIAN_POINT ( 'NONE',  ( 0.06129756055965347034, 14.31084331889941730, 1.337318312763465800 ) ) ;
#7496=CARTESIAN_POINT ( 'NONE',  ( 5.499327144225777175, 17.51037618698124376, 8.771713425651105567 ) ) ;
#7499=CARTESIAN_POINT ( 'NONE',  ( 5.591725253800921891, 15.70436773459850421, 8.761559460545525369 ) ) ;
#7505=CARTESIAN_POINT ( 'NONE',  ( 2.803679754229469800, 12.09773929403007031, 4.926693614680812239 ) ) ;
#7515=CARTESIAN_POINT ( 'NONE',  ( 2.433075215497880972, 20.76646021035401901, 6.507622753141381722 ) ) ;
#7517=CARTESIAN_POINT ( 'NONE',  ( 1.533183450453754704, 12.01664638779708127, 6.289946621455513309 ) ) ;
#7519=CARTESIAN_POINT ( 'NONE',  ( 13.35334803189539521, 22.16103170555246393, 1.961556584310249596 ) ) ;
#7525=CARTESIAN_POINT ( 'NONE',  ( 12.88673784487023255, 14.76516699303951619, 6.813854300165841593 ) ) ;
#7527=CARTESIAN_POINT ( 'NONE',  ( 12.95722427598218118, 11.51533396550468247, 4.774218139127305527 ) ) ;
#7531=CARTESIAN_POINT ( 'NONE',  ( 7.882649901787743829, 20.03851403430508782, -1.570039674128517859 ) ) ;
#7532=CARTESIAN_POINT ( 'NONE',  ( 7.377632332484820310, 14.94885212140055408, 7.515399275738874785 ) ) ;
#7534=CARTESIAN_POINT ( 'NONE',  ( 6.517250350420195737, 20.15272355558845874, 0.5064415424127612919 ) ) ;
#7535=CARTESIAN_POINT ( 'NONE',  ( 2.152814512047750650, 20.23805962733014852, 5.716278487167510747 ) ) ;
#7540=CARTESIAN_POINT ( 'NONE',  ( 8.881999483277855489, 20.20358612698620249, 6.571188270847311941 ) ) ;
#7542=CARTESIAN_POINT ( 'NONE',  ( 3.463643476966617119, 15.44861990895924819, -1.447185448056517831 ) ) ;
#7546=CARTESIAN_POINT ( 'NONE',  ( 1.459627900731261141, 14.30699635049795226, 8.431327355238760646 ) ) ;
#7552=CARTESIAN_POINT ( 'NONE',  ( 10.94369443579043200, 11.39479583509590199, 4.876173924909795510 ) ) ;
#7556=CARTESIAN_POINT ( 'NONE',  ( 5.572600844917717566, 12.66182956979191587, -0.7461097123436445377 ) ) ;
#7559=CARTESIAN_POINT ( 'NONE',  ( 0.1129728326432310886, 20.32260066561571676, 5.061726021590057023 ) ) ;
#7565=CARTESIAN_POINT ( 'NONE',  ( 12.85337560073962493, 21.48306739246610420, 0.4997394630849344432 ) ) ;
#7566=CARTESIAN_POINT ( 'NONE',  ( 4.614827001460207079, 19.61000027071614227, 6.590015868446513991 ) ) ;
#7568=CARTESIAN_POINT ( 'NONE',  ( 11.26774977721790449, 15.74974973885002250, 6.878961729585737039 ) ) ;
#7569=CARTESIAN_POINT ( 'NONE',  ( 13.99789750971088331, 21.64220180175570363, 3.696402113709151394 ) ) ;
#7571=CARTESIAN_POINT ( 'NONE',  ( 3.861847520083515839, 21.32356625081728296, 4.680827701663748286 ) ) ;
#7574=CARTESIAN_POINT ( 'NONE',  ( 14.25008779104191703, 21.25436666907090455, 4.245038886465763106 ) ) ;
#7578=CARTESIAN_POINT ( 'NONE',  ( 11.88155870319460128, 20.88804905822066971, 3.524732118264728875 ) ) ;
#7580=CARTESIAN_POINT ( 'NONE',  ( 0.2225936923515433874, 20.08366710440301262, 6.197720518317566096 ) ) ;
#7581=CARTESIAN_POINT ( 'NONE',  ( 5.703860639285195155, 11.35334887747070276, 1.266263560432865143 ) ) ;
#7584=( NAMED_UNIT ( * ) SI_UNIT ( $, .STERADIAN. ) SOLID_ANGLE_UNIT ( ) );
#7594=CARTESIAN_POINT ( 'NONE',  ( 1.881684930349333928, 15.09886263991730537, 0.2569686833294808626 ) ) ;
#7603=CARTESIAN_POINT ( 'NONE',  ( 1.745695617745230299, 15.58894874012881182, 9.651474225904069115 ) ) ;
#7606=CARTESIAN_POINT ( 'NONE',  ( 3.835900461743189549, 12.20702721357838172, 0.5463839515351021081 ) ) ;
#7619=CARTESIAN_POINT ( 'NONE',  ( 2.547717337248343039, 11.27265232115933102, 3.789480751304223460 ) ) ;
#7626=CARTESIAN_POINT ( 'NONE',  ( 10.44189738732276140, 19.34515354661070319, 6.540544623818083103 ) ) ;
#7629=CARTESIAN_POINT ( 'NONE',  ( 11.58355748138406938, 10.94906613365873049, -0.9808765445798767191 ) ) ;
#7635=CARTESIAN_POINT ( 'NONE',  ( 7.521814107298904872, 12.14759314724596706, -1.039252882385111709 ) ) ;
#7638=CARTESIAN_POINT ( 'NONE',  ( 8.458318833295095374, 19.91303329138582257, 5.610345679553954135 ) ) ;
#7642=CARTESIAN_POINT ( 'NONE',  ( 7.001331565757744180, 11.28301579719734171, 5.025527442906016162 ) ) ;
#7645=CARTESIAN_POINT ( 'NONE',  ( 4.370808908492361589, 20.54241105020114233, 0.3984924473438536396 ) ) ;
#7646=CARTESIAN_POINT ( 'NONE',  ( 1.685730993150120982, 15.98818651832521809, 9.604930218560687294 ) ) ;
#7648=CARTESIAN_POINT ( 'NONE',  ( 3.435969853487951031, 14.96929529427155714, 8.323793337960825767 ) ) ;
#7654=CARTESIAN_POINT ( 'NONE',  ( 11.39404450035965510, 13.83933078011801499, 7.025478403630279978 ) ) ;
#7659=CARTESIAN_POINT ( 'NONE',  ( 11.82169470351746732, 19.85945549919958353, -2.282691836462475088 ) ) ;
#7661=CARTESIAN_POINT ( 'NONE',  ( 5.736873335961724329, 11.96313308795059172, 0.01662313235952948484 ) ) ;
#7668=CARTESIAN_POINT ( 'NONE',  ( 5.835913855334317724, 15.55272378482423079, -1.593939421784943189 ) ) ;
#7669=CARTESIAN_POINT ( 'NONE',  ( 5.336950776178195355, 16.31355649014509623, 8.043007501857138308 ) ) ;
#7670=CARTESIAN_POINT ( 'NONE',  ( 8.958927231525365187, 12.18567386761292148, 5.087176938866648790 ) ) ;
#7671=CARTESIAN_POINT ( 'NONE',  ( 2.105188602693566224, 13.07595850747188315, 0.3638253081235816588 ) ) ;
#7683=CARTESIAN_POINT ( 'NONE',  ( 10.59060266505083803, 20.91478602822554222, 0.04984095317570090555 ) ) ;
#7686=CARTESIAN_POINT ( 'NONE',  ( 4.178641076556762535, 20.20829226350481989, 6.748569037004350513 ) ) ;
#7696=CARTESIAN_POINT ( 'NONE',  ( 8.170949848228001855, 11.48768387232824217, 1.861147236350632728 ) ) ;
#7697=CARTESIAN_POINT ( 'NONE',  ( 2.188904998575694538, 18.20681673484682861, 0.4591847818817980653 ) ) ;
#7709=CARTESIAN_POINT ( 'NONE',  ( 6.742783883146333146, 10.91793053508332001, 4.244188499288108929 ) ) ;
#7712=CARTESIAN_POINT ( 'NONE',  ( 3.939194837300639573, 19.06718353162318991, -0.7130797351348172608 ) ) ;
#7717=CARTESIAN_POINT ( 'NONE',  ( 3.145532673433270698, 12.72872530801424240, 6.528795813461734099 ) ) ;
#7723=CARTESIAN_POINT ( 'NONE',  ( 2.876035228143350331, 11.34340886899239109, 5.205579515552751779 ) ) ;
#7733=CARTESIAN_POINT ( 'NONE',  ( 7.331740208057938801, 18.10524492707348898, -1.926982220310529570 ) ) ;
#7737=CARTESIAN_POINT ( 'NONE',  ( 10.94579177605037579, 14.27302213158844602, -3.976339498359578339 ) ) ;
#7742=CARTESIAN_POINT ( 'NONE',  ( 7.698216182924317863, 11.55586773472163209, -0.2515938179596974300 ) ) ;
#7743=CARTESIAN_POINT ( 'NONE',  ( 6.966837752621037438, 20.72930966971181377, 1.679252894246652028 ) ) ;
#7747=CARTESIAN_POINT ( 'NONE',  ( 11.26444812368913873, 12.02016517962410269, 5.847082729819134350 ) ) ;
#7751=CARTESIAN_POINT ( 'NONE',  ( 5.965713978883512070, 11.27437957348430153, 1.153757586229308574 ) ) ;
#7752=CARTESIAN_POINT ( 'NONE',  ( 1.704162562805419778, 15.26834743306047670, 9.500263804380585597 ) ) ;
#7754=CARTESIAN_POINT ( 'NONE',  ( 1.566762436808580850, 14.30904236277701003, 8.395310680802657188 ) ) ;
#7761=CARTESIAN_POINT ( 'NONE',  ( 11.44084217265526071, 14.79698256115047350, 7.380351338282362228 ) ) ;
#7764=CARTESIAN_POINT ( 'NONE',  ( 12.19555853789111310, 20.67832640328533600, -1.317058961510981785 ) ) ;
#7765=CARTESIAN_POINT ( 'NONE',  ( 5.520456159175803457, 17.64984982689927762, -2.012547465800341495 ) ) ;
#7767=CARTESIAN_POINT ( 'NONE',  ( 0.1533679602575867273, 17.19689764357661943, 0.7834172150352086694 ) ) ;
#7772=CARTESIAN_POINT ( 'NONE',  ( 10.40081950133698818, 20.33297925226851888, -1.342766371799479330 ) ) ;
#7787=CARTESIAN_POINT ( 'NONE',  ( 12.16163452745204232, 20.48856804812561450, 4.265005074572522759 ) ) ;
#7788=CARTESIAN_POINT ( 'NONE',  ( 1.477062725962008827, 15.58526859550301147, 8.784116692769741164 ) ) ;
#7792=( NAMED_UNIT ( * ) PLANE_ANGLE_UNIT ( ) SI_UNIT ( $, .RADIAN. ) );
#7801=CARTESIAN_POINT ( 'NONE',  ( 11.06523579707593541, 17.51379554528373816, 6.791568276050612418 ) ) ;
#7804=CARTESIAN_POINT ( 'NONE',  ( 6.020660706909825244, 11.11068921130002174, 1.355485640074744591 ) ) ;
#7813=CARTESIAN_POINT ( 'NONE',  ( 2.298378135600148475, 19.81152135836902062, 0.4500434701621164879 ) ) ;
#7816=CARTESIAN_POINT ( 'NONE',  ( 3.608170863617357504, 13.45129126140751019, -0.5713419425411067065 ) ) ;
#7829=CARTESIAN_POINT ( 'NONE',  ( 3.622599477590417560, 16.21029899727770385, 9.208972499662912981 ) ) ;
#7840=CARTESIAN_POINT ( 'NONE',  ( 9.598619977022886829, 11.43307009487834058, 0.5138147689867528234 ) ) ;
#7843=CARTESIAN_POINT ( 'NONE',  ( 12.08409848062061265, 21.36742032689186388, -1.692652775323916003 ) ) ;
#7849=CARTESIAN_POINT ( 'NONE',  ( 8.223934500132745740, 20.88092512594423056, -0.6806936496286138949 ) ) ;
#7850=CARTESIAN_POINT ( 'NONE',  ( 7.371918716459705756, 20.91752996184955293, 2.755765391713364210 ) ) ;
#7859=CARTESIAN_POINT ( 'NONE',  ( 1.679183762215729736, 14.29506049579505067, 9.182897261660000865 ) ) ;
#7861=CARTESIAN_POINT ( 'NONE',  ( 5.607325312162852349, 20.83420574847494322, 3.738502895875575938 ) ) ;
#7868=CARTESIAN_POINT ( 'NONE',  ( 9.163832593674008820, 13.38766655458928767, -2.811206270904612836 ) ) ;
#7871=CARTESIAN_POINT ( 'NONE',  ( 7.990381836082426581, 21.45420684216762908, 4.447820836819799339 ) ) ;
#7873=CARTESIAN_POINT ( 'NONE',  ( 3.365948022932646833, 20.63951482243974311, 3.619662730472012147 ) ) ;
#7882=CARTESIAN_POINT ( 'NONE',  ( 10.61004938962564026, 20.41586353969747947, 4.879409801239452449 ) ) ;
#7884=CARTESIAN_POINT ( 'NONE',  ( 5.236457354293306388, 17.24636926302095929, 7.945963056083468423 ) ) ;
#7885=CARTESIAN_POINT ( 'NONE',  ( 3.733050171586274502, 21.36287299093768155, 3.432506848783466236 ) ) ;
#7888=CARTESIAN_POINT ( 'NONE',  ( 6.767696032117554772, 11.35695232375848107, 2.710251460945410251 ) ) ;
#7897=CARTESIAN_POINT ( 'NONE',  ( 9.518858328804567392, 18.01013026545717111, -2.601155476716757509 ) ) ;
#7898=CARTESIAN_POINT ( 'NONE',  ( 0.6624797471569731089, 19.52062711105720894, 7.302438800931884799 ) ) ;
#7907=CARTESIAN_POINT ( 'NONE',  ( 0.6071489226691182406, 19.09056084336265613, 1.779463758861457023 ) ) ;
#7912=CARTESIAN_POINT ( 'NONE',  ( 12.39952505252417225, 11.21852838486178250, 2.567359074515783934 ) ) ;
#7914=CARTESIAN_POINT ( 'NONE',  ( 2.846561112771937463, 19.99446726697395604, 2.016362468292247634 ) ) ;
#7916=CARTESIAN_POINT ( 'NONE',  ( 12.45929919478725978, 10.42866963796318025, 2.734625762110018954 ) ) ;
#7927=CARTESIAN_POINT ( 'NONE',  ( 1.776609477927864944, 21.29427857361828202, 5.019511698632141083 ) ) ;
#7930=CARTESIAN_POINT ( 'NONE',  ( 4.453886262617038128, 20.54954622212565951, 0.5777918640390905525 ) ) ;
#7936=CARTESIAN_POINT ( 'NONE',  ( 0.7908948794667333138, 12.21508164119194539, 4.984945765070319723 ) ) ;
#7938=CARTESIAN_POINT ( 'NONE',  ( 2.434666203727371858, 12.17329066828716755, 3.243477976185151324 ) ) ;
#7944=CARTESIAN_POINT ( 'NONE',  ( 2.901118926289983690, 11.36639711562255961, 5.314311948376294836 ) ) ;
#7948=CARTESIAN_POINT ( 'NONE',  ( 13.08245519309633309, 21.51426585157789972, 1.947758980082396896 ) ) ;
#7953=CARTESIAN_POINT ( 'NONE',  ( 8.345656034557093150, 19.69124030533750158, 6.193199096954582927 ) ) ;
#7956=CARTESIAN_POINT ( 'NONE',  ( 11.06000417728166418, 12.98885560605806688, -3.324977026302950556 ) ) ;
#7962=CARTESIAN_POINT ( 'NONE',  ( 8.191486769309802796, 20.38885208666888005, 4.925509210000734051 ) ) ;
#7963=CARTESIAN_POINT ( 'NONE',  ( 6.964527527572196952, 12.34030082466796863, 5.404614456109265497 ) ) ;
#7968=CARTESIAN_POINT ( 'NONE',  ( 1.134328099840657966, 11.72196338839733265, 6.483094573881109213 ) ) ;
#7971=CARTESIAN_POINT ( 'NONE',  ( 6.291547558928166417, 11.65658372465740200, 2.472496458133855768 ) ) ;
#7977=CARTESIAN_POINT ( 'NONE',  ( 10.69351799873146902, 10.89466173679246097, 4.203936836416402478 ) ) ;
#7978=CARTESIAN_POINT ( 'NONE',  ( 9.437281383587103889, 11.84308063076154660, -1.503547281869039853 ) ) ;
#7982=CARTESIAN_POINT ( 'NONE',  ( 11.69496188115748048, 19.47354328404300716, -2.596091651573762427 ) ) ;
#7983=CARTESIAN_POINT ( 'NONE',  ( 7.241256223353114585, 21.68187987146653128, 2.393131185843784703 ) ) ;
#7985=CARTESIAN_POINT ( 'NONE',  ( 5.888945687064545353, 12.28013972695870137, 0.9976771953365630718 ) ) ;
#7988=CARTESIAN_POINT ( 'NONE',  ( 6.247512289571992561, 18.85032048260596227, -1.008565764037584023 ) ) ;
#7990=CARTESIAN_POINT ( 'NONE',  ( 1.243233153551759784, 11.63297050342826289, 6.525882853348925927 ) ) ;
#7993=CARTESIAN_POINT ( 'NONE',  ( 6.680663975448227987, 11.57849123843430128, 2.752492323310664180 ) ) ;
#8003=CARTESIAN_POINT ( 'NONE',  ( 12.29938047911826438, 20.21572945018251843, 4.621882145428052979 ) ) ;
#8012=CARTESIAN_POINT ( 'NONE',  ( 3.870040991641794381, 17.28388692985063102, -0.5782205561518194425 ) ) ;
#8015=CARTESIAN_POINT ( 'NONE',  ( 0.7706404128728925329, 19.48544532655929729, 2.171001955729903177 ) ) ;
#8018=CARTESIAN_POINT ( 'NONE',  ( 5.585406168101782143, 13.98417111045325001, -0.8546884854210520244 ) ) ;
#8020=CARTESIAN_POINT ( 'NONE',  ( 12.92989047915411582, 22.29005399844394120, 0.3614750032390292578 ) ) ;
#8027=EDGE_LOOP ( 'NONE', ( #15902, #9560, #7273, #18680 ) ) ;
#8030=CARTESIAN_POINT ( 'NONE',  ( 6.634819837061233905, 10.91373323652594252, 4.277435202800065284 ) ) ;
#8033=CARTESIAN_POINT ( 'NONE',  ( 3.778158909772205476, 12.44086029795262505, 0.2773760682544378908 ) ) ;
#8037=CARTESIAN_POINT ( 'NONE',  ( 0.6379514360146986141, 12.25052848803336758, 4.278287073605215873 ) ) ;
#8039=CARTESIAN_POINT ( 'NONE',  ( 2.515435776023313696, 12.09851621675084665, 3.613288693446259803 ) ) ;
#8040=CARTESIAN_POINT ( 'NONE',  ( 4.151218630365011819, 12.29860231867225728, 1.847275165616512949 ) ) ;
#8045=CARTESIAN_POINT ( 'NONE',  ( 3.605855464307719860, 16.44159216467194540, 9.204281209079420378 ) ) ;
#8052=CARTESIAN_POINT ( 'NONE',  ( 13.13545844809530116, 21.45922784306827324, 1.923808864204277658 ) ) ;
#8056=CARTESIAN_POINT ( 'NONE',  ( 11.01329100639444825, 21.44411105555546015, 2.081521072878112832 ) ) ;
#8059=CARTESIAN_POINT ( 'NONE',  ( 11.16145234711147793, 18.34406730449142842, -4.030487463324528896 ) ) ;
#8063=CARTESIAN_POINT ( 'NONE',  ( 8.300069718050908207, 11.53897452521841061, 2.298314304733178659 ) ) ;
#8065=CARTESIAN_POINT ( 'NONE',  ( 2.899589520589617830, 18.93284891393944847, 7.571049628500222006 ) ) ;
#8068=CARTESIAN_POINT ( 'NONE',  ( 1.642651581313985920, 16.44733452758824654, -0.7885569526307778521 ) ) ;
#8069=CARTESIAN_POINT ( 'NONE',  ( 0.8410692468848214309, 11.43456274839658349, 5.196488955505333074 ) ) ;
#8073=CARTESIAN_POINT ( 'NONE',  ( 3.927156886961982174, 12.81957249642222152, 0.8896893740454994148 ) ) ;
#8078=CARTESIAN_POINT ( 'NONE',  ( 11.08364749134637783, 12.02016517962410269, 5.901226234691837824 ) ) ;
#8081=CARTESIAN_POINT ( 'NONE',  ( 9.075132670590440043, 14.78225112982097222, -3.399159583193371414 ) ) ;
#8083=CARTESIAN_POINT ( 'NONE',  ( 6.671004511676491333, 21.25262578982561124, 0.8364515325576188376 ) ) ;
#8085=CARTESIAN_POINT ( 'NONE',  ( 2.523890540482722766, 12.01182523388594170, 3.570307163362016922 ) ) ;
#8090=CARTESIAN_POINT ( 'NONE',  ( 13.51825059216985103, 14.85126536588636981, 6.305477837050446510 ) ) ;
#8091=CARTESIAN_POINT ( 'NONE',  ( 5.937100890138371057, 21.55539096890324302, 3.690821903281856553 ) ) ;
#8095=CARTESIAN_POINT ( 'NONE',  ( 6.736892714481453659, 11.48351050777079330, 2.728717353481319385 ) ) ;
#8104=CARTESIAN_POINT ( 'NONE',  ( 13.05080356390050156, 13.28370079963820771, 5.434073716250534147 ) ) ;
#8115=CARTESIAN_POINT ( 'NONE',  ( 0.2522477005385261872, 17.74294589129466715, 1.020296498861633427 ) ) ;
#8119=CARTESIAN_POINT ( 'NONE',  ( 10.27701911607673679, 11.26312240063166037, 2.186809789112166058 ) ) ;
#8121=CARTESIAN_POINT ( 'NONE',  ( 8.612298605082777669, 10.74346438930206027, 3.697136140246361613 ) ) ;
#8129=CARTESIAN_POINT ( 'NONE',  ( 8.599976436249926692, 20.62313896856149142, 0.3932540034451326161 ) ) ;
#8130=CARTESIAN_POINT ( 'NONE',  ( 9.116205194245099008, 21.95627871459122105, 1.667017424323884667 ) ) ;
#8132=VERTEX_POINT ( 'NONE', #9961 ) ;
#8135=CARTESIAN_POINT ( 'NONE',  ( 4.297480147115120275, 20.54582653591270258, 0.4177457353544402618 ) ) ;
#8138=CARTESIAN_POINT ( 'NONE',  ( 5.002037701870804653, 21.31635843410325037, 2.042759171744529478 ) ) ;
#8146=CARTESIAN_POINT ( 'NONE',  ( 2.211169688515047138, 12.61253923079801176, 2.196332706544586788 ) ) ;
#8148=CARTESIAN_POINT ( 'NONE',  ( 11.80762148770061337, 11.06331416201678053, -1.379479278252061958 ) ) ;
#8155=CARTESIAN_POINT ( 'NONE',  ( 1.807950215505384373, 13.11484105769346620, 0.4484171696861184442 ) ) ;
#8165=CARTESIAN_POINT ( 'NONE',  ( 8.290641415794244296, 11.45164960235222118, 3.642276225269535317 ) ) ;
#8172=CARTESIAN_POINT ( 'NONE',  ( 8.011435824295395136, 11.80026701718135129, 1.025195225715891834 ) ) ;
#8178=CARTESIAN_POINT ( 'NONE',  ( 3.129583319975353550, 18.08847882444087674, 8.072846311850007339 ) ) ;
#8183=CARTESIAN_POINT ( 'NONE',  ( 6.258027693244144984, 21.18174881316136293, 5.549184756157156784 ) ) ;
#8184=CARTESIAN_POINT ( 'NONE',  ( -0.1855959611067334591, 15.75727966247650613, 0.07784262388770696317 ) ) ;
#8187=CARTESIAN_POINT ( 'NONE',  ( 0.3055297026777472613, 20.17339616899437971, 6.156372013646721264 ) ) ;
#8194=CARTESIAN_POINT ( 'NONE',  ( 9.385781312307386770, 16.63265789203856571, 8.122277095502592914 ) ) ;
#8196=CARTESIAN_POINT ( 'NONE',  ( 9.357963118639132105, 18.58272514913181084, -3.199465920211048697 ) ) ;
#8199=CARTESIAN_POINT ( 'NONE',  ( 6.370539475672911678, 20.77878503102673236, 0.03171506329460684059 ) ) ;
#8202=CARTESIAN_POINT ( 'NONE',  ( -0.2885760015458498362, 20.30684170721071879, 4.831137852936522314 ) ) ;
#8209=CARTESIAN_POINT ( 'NONE',  ( 9.655129386034436934, 13.52835235745250131, -2.703733241061648140 ) ) ;
#8210=CARTESIAN_POINT ( 'NONE',  ( 4.950487383143544307, 20.46779201619338195, 6.708806423651408224 ) ) ;
#8215=CARTESIAN_POINT ( 'NONE',  ( 6.670151187356951894, 11.06004643669878185, 2.717775301413040800 ) ) ;
#8219=VERTEX_POINT ( 'NONE', #333 ) ;
#8224=CARTESIAN_POINT ( 'NONE',  ( 12.83070406023858823, 18.55124415177118991, 5.915695860297560671 ) ) ;
#8231=CARTESIAN_POINT ( 'NONE',  ( 3.743459358786643598, 15.80679344681467846, -0.6324665095716647256 ) ) ;
#8238=CARTESIAN_POINT ( 'NONE',  ( 5.952915771404345691, 18.80336625489407965, -0.8434118395857959083 ) ) ;
#8241=CARTESIAN_POINT ( 'NONE',  ( 11.45419627047315814, 15.66509967140728854, 7.663546619674057148 ) ) ;
#8246=CARTESIAN_POINT ( 'NONE',  ( 9.574632210810730015, 21.03727855150343373, 2.997630161494908130 ) ) ;
#8247=CARTESIAN_POINT ( 'NONE',  ( 9.173463358870977302, 17.37232422777100993, -3.665279000589813929 ) ) ;
#8252=CARTESIAN_POINT ( 'NONE',  ( 4.919162651895962135, 11.34514690749418087, 5.650005697289334883 ) ) ;
#8255=CARTESIAN_POINT ( 'NONE',  ( 5.179964232832246829, 21.44866463646626187, 2.526011547878774799 ) ) ;
#8263=CARTESIAN_POINT ( 'NONE',  ( 12.91332895665777158, 20.46142704777525978, 5.469078331909021706 ) ) ;
#8268=CARTESIAN_POINT ( 'NONE',  ( 1.933513631160261648, 18.30600127081370943, -0.3311359031021076094 ) ) ;
#8272=CARTESIAN_POINT ( 'NONE',  ( 13.11001702788002277, 21.48322523121904482, 1.934949587800859572 ) ) ;
#8277=CARTESIAN_POINT ( 'NONE',  ( 11.02388696027891335, 18.13781435472470349, -3.406593805752508697 ) ) ;
#8287=CARTESIAN_POINT ( 'NONE',  ( 8.577308677684913008, 11.63761981776649179, 3.515469741029564776 ) ) ;
#8291=CARTESIAN_POINT ( 'NONE',  ( 0.3577463236909741440, 19.38239508688243617, 1.021447940004778454 ) ) ;
#8294=CARTESIAN_POINT ( 'NONE',  ( 2.246702380120268572, 13.47654819534348292, 0.8363802434591389723 ) ) ;
#8301=CARTESIAN_POINT ( 'NONE',  ( 8.701198850936064488, 20.20358612698620249, 6.625331775719724092 ) ) ;
#8303=CARTESIAN_POINT ( 'NONE',  ( 9.670731391893321316, 19.91002294283195795, -2.452946502561233810 ) ) ;
#8305=CARTESIAN_POINT ( 'NONE',  ( 6.593580017284943473, 21.14855486304147192, 0.6275595558785633798 ) ) ;
#8310=CARTESIAN_POINT ( 'NONE',  ( 7.038768548784214651, 18.13751136180625778, 7.270069188298340812 ) ) ;
#8314=CARTESIAN_POINT ( 'NONE',  ( 7.290540035995150880, 11.65642365002708125, 4.787114039832606416 ) ) ;
#8316=CARTESIAN_POINT ( 'NONE',  ( 1.382092486215193761, 18.94469375348566231, 8.962251623514621457 ) ) ;
#8319=CARTESIAN_POINT ( 'NONE',  ( 1.833072101810493848, 14.88386107855003360, 0.2418471280350485975 ) ) ;
#8328=CARTESIAN_POINT ( 'NONE',  ( 10.83572638560662327, 12.10937221960885246, 4.528287571500745123 ) ) ;
#8330=CARTESIAN_POINT ( 'NONE',  ( 12.66561601154539041, 19.21253279861005581, 5.535559188462356062 ) ) ;
#8332=CARTESIAN_POINT ( 'NONE',  ( 6.269352038965187113, 10.97123987517479016, 2.325299610618768220 ) ) ;
#8334=CARTESIAN_POINT ( 'NONE',  ( 1.385961804465817515, 14.30904236277701003, 8.449454185675360662 ) ) ;
#8337=CARTESIAN_POINT ( 'NONE',  ( -0.1849527131266449076, 20.23672349358593792, 5.150944217628095068 ) ) ;
#8341=CARTESIAN_POINT ( 'NONE',  ( 13.17838052650600211, 14.87494513186989664, 6.319450451114021483 ) ) ;
#8342=CARTESIAN_POINT ( 'NONE',  ( 12.44399840006683178, 11.21920808676120274, 2.553881509949003092 ) ) ;
#8344=CARTESIAN_POINT ( 'NONE',  ( 11.10986520838597613, 18.39193805972391971, -4.138733212223557167 ) ) ;
#8350=CARTESIAN_POINT ( 'NONE',  ( 8.168579537737969076, 19.82474022107643208, -0.7181693113545990492 ) ) ;
#8351=CARTESIAN_POINT ( 'NONE',  ( 5.801569891678039603, 19.23834655595790011, -1.510785752356017975 ) ) ;
#8356=CARTESIAN_POINT ( 'NONE',  ( -0.04771496096788591101, 12.52330284320706077, 1.689320059643299565 ) ) ;
#8358=CARTESIAN_POINT ( 'NONE',  ( 6.874689736735521528, 19.87943235501797545, 7.077769955840262028 ) ) ;
#8366=CARTESIAN_POINT ( 'NONE',  ( 2.303762633758687173, 19.73751257430979678, 0.5328489609499682533 ) ) ;
#8375=CARTESIAN_POINT ( 'NONE',  ( 10.98303339775889498, 12.79277479448814248, -2.359408852867018958 ) ) ;
#8381=CARTESIAN_POINT ( 'NONE',  ( 9.190889634080209092, 16.82461965218397282, 7.202071835226256269 ) ) ;
#8387=CARTESIAN_POINT ( 'NONE',  ( 0.1737502244468468182, 12.20094924675537307, 2.251015528918583808 ) ) ;
#8392=CARTESIAN_POINT ( 'NONE',  ( 1.061577872868078254, 12.03899270364792073, 4.769622043989930837 ) ) ;
#8397=CARTESIAN_POINT ( 'NONE',  ( 10.63989556519935320, 19.52774875955264022, 6.752680363256145846 ) ) ;
#8398=CARTESIAN_POINT ( 'NONE',  ( 10.62635245719450694, 21.77196383837482330, 0.09988737663030886060 ) ) ;
#8401=CARTESIAN_POINT ( 'NONE',  ( 8.557020710820847142, 10.80609942023040126, 3.389879254953236831 ) ) ;
#8402=CARTESIAN_POINT ( 'NONE',  ( 3.386193242415981075, 13.61441523003558274, 7.601052676155180876 ) ) ;
#8407=CARTESIAN_POINT ( 'NONE',  ( 10.78492640469823982, 20.67808185030680335, 5.014337372028484729 ) ) ;
#8409=CARTESIAN_POINT ( 'NONE',  ( -0.1089046874588744940, 17.37668286801814688, 0.03726443620168150284 ) ) ;
#8414=CARTESIAN_POINT ( 'NONE',  ( 1.471179364221197883, 15.70105570582070520, 8.896772800854545693 ) ) ;
#8421=CARTESIAN_POINT ( 'NONE',  ( 9.285792827353402501, 21.87697856516881956, 2.219697743754897257 ) ) ;
#8424=CARTESIAN_POINT ( 'NONE',  ( 13.11122246924493417, 16.59952282105541954, 6.404990385722812540 ) ) ;
#8427=CARTESIAN_POINT ( 'NONE',  ( 3.081105562148156007, 13.56078169262926281, 7.763509864629036805 ) ) ;
#8431=CARTESIAN_POINT ( 'NONE',  ( 3.831872794198578180, 16.97575148034115244, -0.6279392605359102042 ) ) ;
#8434=CARTESIAN_POINT ( 'NONE',  ( 6.253898308320673394, 11.68813189510091100, 2.888293778337470918 ) ) ;
#8440=CARTESIAN_POINT ( 'NONE',  ( 6.927322632701765848, 20.81446147317312168, 1.621339958521637703 ) ) ;
#8441=CARTESIAN_POINT ( 'NONE',  ( 4.054711315827309370, 20.40797957536717178, 5.161551740127496402 ) ) ;
#8443=CARTESIAN_POINT ( 'NONE',  ( 9.392652412154310682, 17.21976690206051330, -2.901007874484461624 ) ) ;
#8444=CARTESIAN_POINT ( 'NONE',  ( 4.464807677231505068, 20.92444076583792167, 5.032481929441805057 ) ) ;
#8445=CARTESIAN_POINT ( 'NONE',  ( 9.062801421126779999, 21.95627871459122105, 1.683009998091938852 ) ) ;
#8449=CARTESIAN_POINT ( 'NONE',  ( 10.80473891853958612, 18.82471788637430166, 6.156953377096570534 ) ) ;
#8450=CARTESIAN_POINT ( 'NONE',  ( 11.15456943723388861, 18.39169315105245417, -4.151439798146012272 ) ) ;
#8455=CARTESIAN_POINT ( 'NONE',  ( 10.93940955106799073, 14.41445727887342620, -4.025580141893404296 ) ) ;
#8457=CARTESIAN_POINT ( 'NONE',  ( 3.513474866157187293, 12.26666322754141980, 0.5275322538260243110 ) ) ;
#8460=CARTESIAN_POINT ( 'NONE',  ( 5.008754897235177417, 21.32213879784493926, 2.060963987967154853 ) ) ;
#8468=CARTESIAN_POINT ( 'NONE',  ( 3.808323415348045415, 13.81725641533127202, 0.1165697555046887185 ) ) ;
#8473=CARTESIAN_POINT ( 'NONE',  ( 2.850083250245388111, 20.85896612695718133, 1.947395870406601226 ) ) ;
#8483=CARTESIAN_POINT ( 'NONE',  ( 7.563702072044085511, 18.07137575567074350, -1.907521650424996107 ) ) ;
#8485=CARTESIAN_POINT ( 'NONE',  ( 0.7026925879561919386, 20.32382785537196312, 1.796361731335691436 ) ) ;
#8491=CARTESIAN_POINT ( 'NONE',  ( 8.556392325919617292, 11.61851416689291305, 3.423200530932141383 ) ) ;
#8498=CARTESIAN_POINT ( 'NONE',  ( -0.1352155204582886072, 16.66627892838214464, 0.04119029793672387973 ) ) ;
#8502=CARTESIAN_POINT ( 'NONE',  ( 4.328347590241748755, 12.03379079558084186, 2.230145814812864113 ) ) ;
#8509=CARTESIAN_POINT ( 'NONE',  ( 12.94563250920762520, 12.79228088949424169, 6.166948107170512117 ) ) ;
#8511=CARTESIAN_POINT ( 'NONE',  ( 13.33056277106260978, 16.75682411354094015, 7.157340733298330981 ) ) ;
#8516=CARTESIAN_POINT ( 'NONE',  ( 9.107277861881895475, 11.81316815476289506, 5.756061362039455176 ) ) ;
#8517=CARTESIAN_POINT ( 'NONE',  ( 3.474038444628396949, 20.64378046205170136, 3.586838031231339485 ) ) ;
#8523=CARTESIAN_POINT ( 'NONE',  ( 12.97329811073338846, 20.23326750546686270, 5.220295724011733363 ) ) ;
#8524=CARTESIAN_POINT ( 'NONE',  ( 6.364250290165353263, 10.85153064243760213, 2.321502149683346783 ) ) ;
#8529=CARTESIAN_POINT ( 'NONE',  ( 5.176227073658261624, 12.95116610613770369, 6.671170083817433927 ) ) ;
#8535=CARTESIAN_POINT ( 'NONE',  ( 10.96673932127253970, 12.57086297534474717, 5.140911593025348836 ) ) ;
#8536=CARTESIAN_POINT ( 'NONE',  ( 10.89554121559266164, 19.63180904864239196, 6.552446325582041986 ) ) ;
#8540=CARTESIAN_POINT ( 'NONE',  ( 12.42688504315472287, 11.33449225177425213, 2.569421434122930670 ) ) ;
#8542=CARTESIAN_POINT ( 'NONE',  ( 6.404761471570224352, 19.58301787754098200, 6.631544299425215172 ) ) ;
#8552=CARTESIAN_POINT ( 'NONE',  ( 6.124889344102976807, 11.59927643492120097, 2.920436077416646903 ) ) ;
#8555=CARTESIAN_POINT ( 'NONE',  ( 7.544623071831273897, 13.14813038638666143, -1.051744186015200588 ) ) ;
#8556=CARTESIAN_POINT ( 'NONE',  ( 11.74386382974287812, 19.71606648096064163, -2.545816756848700013 ) ) ;
#8557=CARTESIAN_POINT ( 'NONE',  ( 5.006421629233452464, 11.37607716600946084, 3.684801207120545374 ) ) ;
#8558=CARTESIAN_POINT ( 'NONE',  ( 9.198481203478936052, 18.56541443352003640, 7.659581353093840583 ) ) ;
#8563=CARTESIAN_POINT ( 'NONE',  ( 11.03326096593770167, 17.69443056144524107, 6.636539859302792443 ) ) ;
#8564=CARTESIAN_POINT ( 'NONE',  ( 7.878526806895981061, 20.10277937464278253, -1.676873219709654306 ) ) ;
#8571=CARTESIAN_POINT ( 'NONE',  ( 0.8457333743466408649, 11.71888320561318153, 6.611532361588754902 ) ) ;
#8574=CARTESIAN_POINT ( 'NONE',  ( 7.438238543944203585, 17.18978195494404559, 8.325495078195531917 ) ) ;
#8578=CARTESIAN_POINT ( 'NONE',  ( 0.5166294470163060870, 12.37563144599256226, 3.713427293140974417 ) ) ;
#8582=CARTESIAN_POINT ( 'NONE',  ( 1.992723062505909359, 13.56228047875357845, 1.081925201674736048 ) ) ;
#8587=CARTESIAN_POINT ( 'NONE',  ( 4.771131690971144756, 20.19041085357579135, 7.102526296929879912 ) ) ;
#8600=CARTESIAN_POINT ( 'NONE',  ( 6.389564595444752193, 11.61181900198992167, 3.246015655190012339 ) ) ;
#8601=CARTESIAN_POINT ( 'NONE',  ( -0.3077843186941259801, 21.11429744052310298, 4.766995793887819133 ) ) ;
#8608=CARTESIAN_POINT ( 'NONE',  ( 7.449701660363790445, 14.69335886913581213, -1.830007769899437031 ) ) ;
#8614=CARTESIAN_POINT ( 'NONE',  ( 0.2150577513804199647, 12.08184417975117242, 2.440174913249124611 ) ) ;
#8617=CARTESIAN_POINT ( 'NONE',  ( 2.134119274783381925, 14.85629794888722266, 0.06589753127274376732 ) ) ;
#8625=CARTESIAN_POINT ( 'NONE',  ( 7.572317812480900301, 20.04452402401122058, -1.518160419548955309 ) ) ;
#8627=CARTESIAN_POINT ( 'NONE',  ( 13.39245492388289982, 15.33820100747184512, 7.095220746324015337 ) ) ;
#8632=CARTESIAN_POINT ( 'NONE',  ( 9.292241171589457949, 17.94623387717348706, 7.752439896407592457 ) ) ;
#8633=CARTESIAN_POINT ( 'NONE',  ( 0.7904081101278255250, 12.12568132066150106, 4.851017819482066784 ) ) ;
#8635=CARTESIAN_POINT ( 'NONE',  ( 5.651563255009405928, 16.68950339261435545, -1.391004815479667256 ) ) ;
#8637=CARTESIAN_POINT ( 'NONE',  ( 8.359069870979251249, 19.83100852729402064, -1.508148468474054260 ) ) ;
#8638=CARTESIAN_POINT ( 'NONE',  ( 5.378375181977313346, 15.06312536684776227, 7.861873443265979589 ) ) ;
#8641=CARTESIAN_POINT ( 'NONE',  ( 0.3545653445965538109, 11.62494085263212185, 3.163065520695083066 ) ) ;
#8645=CARTESIAN_POINT ( 'NONE',  ( 6.452480818898766124, 10.92909956722771092, 2.773400309299709043 ) ) ;
#8650=CARTESIAN_POINT ( 'NONE',  ( 9.458380351582428958, 21.87037480992658089, 2.696715734057056668 ) ) ;
#8652=CARTESIAN_POINT ( 'NONE',  ( 11.15553486249665482, 14.64160775519011182, -3.299033682045386495 ) ) ;
#8654=CARTESIAN_POINT ( 'NONE',  ( 1.003497587984025108, 20.41800832758468331, 3.587532134645925908 ) ) ;
#8663=CARTESIAN_POINT ( 'NONE',  ( 10.28589934229847280, 11.26381867368412060, 2.184127149925467748 ) ) ;
#8665=CARTESIAN_POINT ( 'NONE',  ( 6.854702814278667233, 12.02528521847468213, 4.767674869364597612 ) ) ;
#8666=CARTESIAN_POINT ( 'NONE',  ( 0.5698505877279143039, 20.87305502788824185, 6.283888600290745252 ) ) ;
#8667=CARTESIAN_POINT ( 'NONE',  ( 12.12410201198690629, 21.60500416633145804, -1.540977856777658639 ) ) ;
#8674=CARTESIAN_POINT ( 'NONE',  ( 7.740651597158667130, 11.34324505471928113, -0.1322639018746852579 ) ) ;
#8678=CARTESIAN_POINT ( 'NONE',  ( 0.5238767203945161599, 20.13149037663900387, 7.903974376171220229 ) ) ;
#8680=ORIENTED_EDGE ( 'NONE', *, *, #3564, .F. ) ;
#8681=CARTESIAN_POINT ( 'NONE',  ( 7.064467163856848586, 11.61461761587226249, 5.722166049371485208 ) ) ;
#8690=CARTESIAN_POINT ( 'NONE',  ( 4.731467607026393907, 20.28102513395944229, 7.000553450486113327 ) ) ;
#8701=CARTESIAN_POINT ( 'NONE',  ( 8.492895593974109758, 11.54146397052094208, 3.562534344333246228 ) ) ;
#8702=CARTESIAN_POINT ( 'NONE',  ( 1.814661426025774071, 13.02131026627836086, 0.3805811478219760513 ) ) ;
#8705=CARTESIAN_POINT ( 'NONE',  ( 4.607010772665877774, 11.08493650962506116, 3.903497619132711094 ) ) ;
#8711=CARTESIAN_POINT ( 'NONE',  ( 7.633935190542764815, 17.76945892008578198, -1.936471469497620390 ) ) ;
#8713=CARTESIAN_POINT ( 'NONE',  ( 3.412213502827448064, 15.93234797188829432, 8.430948932171904886 ) ) ;
#8719=CARTESIAN_POINT ( 'NONE',  ( 3.289252607606479195, 18.65028268025089275, 8.659271349972804899 ) ) ;
#8723=CARTESIAN_POINT ( 'NONE',  ( 0.2840622119934582135, 15.69350566183319273, 0.5951328775468103238 ) ) ;
#8728=CARTESIAN_POINT ( 'NONE',  ( 8.475013748165151739, 20.13899192311416186, 6.625161462038594351 ) ) ;
#8730=CARTESIAN_POINT ( 'NONE',  ( 12.87833794687879774, 19.58183286683828683, 6.222496348469165994 ) ) ;
#8734=CARTESIAN_POINT ( 'NONE',  ( 8.646429374176550553, 10.88129523880938088, 3.767012232034312458 ) ) ;
#8735=CARTESIAN_POINT ( 'NONE',  ( 0.03748398651459098480, 15.70515029433102860, 0.7586468221082122154 ) ) ;
#8737=CARTESIAN_POINT ( 'NONE',  ( 6.194255370365423730, 19.41116075945178920, -0.3004728795146091036 ) ) ;
#8740=CARTESIAN_POINT ( 'NONE',  ( 2.370064745689808294, 19.81445010932126038, 0.4253065698170983011 ) ) ;
#8743=CARTESIAN_POINT ( 'NONE',  ( 3.427273626668901230, 14.96908372069038684, 8.327090403724351830 ) ) ;
#8749=CARTESIAN_POINT ( 'NONE',  ( 11.43397512567650942, 15.80362715008215524, 7.556022402886738654 ) ) ;
#8751=B_SPLINE_CURVE_WITH_KNOTS ( 'NONE', 3,
 ( #9553, #13010, #12568, #2384, #14444, #14675, #4153, #9111, #7580, #938, #21057, #16108, #21161, #19291, #15894, #17864, #1159, #7898, #7468, #21382, #21275, #6131, #5908, #835, #20956, #14239, #12900, #5812, #19614, #6237, #9336, #2710, #10891, #2492, #6016, #17758, #19392, #17640, #9224, #16006, #4262, #2606, #12788, #19511, #4481, #4377, #14556, #11113, #9444, #16216, #1043, #7788, #11217, #17968, #2818, #17349, #18989, #14270, #643, #19424, #20645, #14053, #869, #5616, #5737, #5839, #19102, #2304, #2417, #14161, #15816, #19215, #752, #4183, #17676, #9257, #14922, #3076, #4737, #6169, #13263, #4413, #12934, #16137, #18113, #6052, #14478, #21193, #16353, #7936, #12823, #19642, #1192, #9697, #21522, #8037, #6380, #15241, #8578, #18860, #6922, #15132, #6818, #13363, #10356, #15031, #5152, #20070, #12012, #17100, #15459, #5051, #13578, #9907, #16673, #12133, #11687, #10028, #6708, #17545, #19191, #7478, #12576, #17438, #10571, #12346, #4057, #19299, #10901, #2394, #13919, #19072, #5916, #9123, #3727, #2044, #402, #5478, #12237, #17316, #1167, #1374, #9454, #1053, #8115, #16442, #21615, #9346, #6142, #6474, #4275, #16115, #12912, #14454, #2828, #7907, #21391, #18088, #8015, #2946, #13125, #14785, #10182, #18911, #571, #11958, #16926, #235, #17157, #13743, #3671, #10516, #3556, #15632, #19947, #7215, #17385, #5310, #20674, #124, #12292, #1775, #10296, #15845, #9177, #11069, #16066, #7535, #19347, #995, #12734, #16169, #20901, #10954, #5865, #19457, #2668, #19139, #9401, #6083, #2771, #12855, #9507, #11171, #11721, #8065, #12962, #14732, #11279, #15059, #8178, #21771, #13289, #13388, #6293, #21553, #14953, #18455, #10057, #4540, #16381, #19890, #18141, #13071, #19776, #15274, #3865, #8713, #433, #7185, #1643, #20648, #12163, #3424, #13497, #1974, #13718, #5507, #8821, #17134, #100, #13610, #320, #3757, #17235, #15596, #17679, #2420, #19217, #9041, #543, #20866, #7717, #10720, #11040, #9372, #14373, #10821, #12702, #12379, #16038, #21088, #5937, #12826, #17569, #9147, #7505, #14273, #16248, #19972, #11366, #14599, #19866, #3079, #21749, #8039, #19645, #19748, #7938, #21415, #4621, #6270, #18116, #1403, #2972, #8146, #21642, #11583, #1518, #17205, #7029, #15135, #10239, #6821, #8582, #12015, #4939, #21854, #6712, #11804, #7158, #3401, #1841, #181, #20390, #17103, #1943, #15463, #7594, #3838, #20969, #17321, #17656, #2505, #2619, #9350, #16120, #5482, #20735, #5590, #12351, #19076, #2283, #9021, #12471, #4061, #17549, #7697, #1276, #11558, #9881, #4492, #14458, #19726, #4599, #2724, #2832, #14789, #9458, #1056, #14577, #1173, #7914, #13130, #4717, #9779, #14900, #6478, #6795, #1493, #15332, #7006, #13553, #16962, #6684, #1919, #156, #20365, #6900, #10332, #20048, #13664, #18511, #11992, #10110, #18720, #1700, #8441, #20813, #3922, #2256, #3809, #7128, #9207, #15544, #376, #8882, #20707, #598, #7566, #13896, #12218, #5562, #19170, #14328, #15875, #5893, #16416, #4684, #2698, #11202, #19698, #6443, #21365, #9648, #21145, #19809, #7884, #9323, #18058, #9751, #16096, #2918, #7669, #19495, #16201, #6116, #14762, #21468, #21697, #3452, #4995, #8638, #18690, #11752, #241, #18369, #127, #13747, #10084, #4793, #13639, #9975, #16733, #15085, #6651, #20339, #16829, #18806, #7095, #20444, #10418, #13862, #7220, #5427, #12191, #8853, #12526, #576, #2338, #15848, #15636, #20678, #3896, #14081, #10636, #676, #20906, #4110, #18223, #2975, #9803, #14930, #19749, #14601, #6505, #4941, #11692, #12936, #10035, #13368, #17998, #16466, #8040, #16356, #2855, #4623, #6386, #19867, #11585, #3179, #10360, #2048, #13583, #18749, #15357, #10241, #8468, #11807, #15245, #21855, #13690, #1945, #20184, #18538, #15465, #7030, #3731, #6348, #1693, #8231, #16439, #18503, #10105, #21609, #19944, #8431, #3050, #1269, #8012, #11657, #3266, #4710, #18289, #16538, #13235, #4818, #15005, #21822, #16952, #14000, #20256, #2017, #151, #10540, #3805, #5557, #15433, #6999, #18607, #13657, #5337, #370, #13890, #20359, #3582, #10659, #2132, #8989, #20587, #20934, #5792, #17736, #9425, #12766, #19375, #19164, #4130, #4356, #9317, #10871, #17620, #1023, #2798, #921, #11197, #14426, #2362, #9201, #6109, #11519, #11748, #9969, #2913, #11630, #12986, #9643, #4990, #6439, #21360, #18478, #3022, #18261, #4565, #19805, #14758, #16509, #1568, #9846, #1457, #8310, #1996, #3349, #12073, #13976, #15629, #15300, #10080, #234, #20439, #15181, #12187, #17262, #2106, #20333, #10294, #6759, #11854, #18583, #6875, #5308, #2448, #4214, #9175, #15742, #10952, #7314, #15956, #12624, #20786, #11068, #12732, #787, #5649, #9290, #17825, #17491, #2334, #9068, #6529, #21550, #11606, #14627, #1321, #7963, #4650, #19669, #1219, #16592, #21770, #15058, #11394, #19575, #4441, #16702, #14835, #13181, #4763, #18342, #17923, #17012 ),
 .UNSPECIFIED., .F., .F.,
 ( 4, 3, 3, 3, 3, 3, 3, 3, 3, 3, 3, 3, 3, 3, 3, 3, 3, 3, 3, 3, 3, 3, 3, 3, 3, 3, 3, 3, 3, 3, 3, 3, 3, 3, 3, 3, 3, 3, 3, 3, 3, 3, 3, 3, 3, 3, 3, 3, 3, 3, 3, 3, 3, 3, 3, 3, 3, 3, 3, 3, 3, 3, 3, 3, 3, 3, 3, 3, 3, 3, 3, 3, 3, 3, 3, 3, 3, 3, 3, 3, 3, 3, 3, 3, 3, 3, 3, 3, 3, 3, 3, 3, 3, 3, 3, 3, 3, 3, 3, 3, 3, 3, 3, 3, 3, 3, 3, 3, 3, 3, 3, 3, 3, 3, 3, 3, 3, 3, 3, 3, 3, 3, 3, 3, 3, 3, 3, 3, 3, 3, 3, 3, 3, 3, 3, 3, 3, 3, 3, 3, 3, 3, 3, 3, 3, 3, 3, 3, 3, 3, 3, 3, 3, 3, 3, 3, 3, 3, 3, 3, 3, 3, 3, 3, 3, 3, 3, 3, 3, 3, 3, 3, 3, 3, 3, 3, 3, 3, 3, 3, 3, 3, 3, 3, 3, 3, 3, 3, 3, 3, 3, 3, 3, 3, 3, 3, 3, 3, 3, 3, 3, 3, 3, 3, 3, 3, 3, 3, 3, 3, 4 ),
 ( 0.000000000000000000, 0.006578947365780970537, 0.01249999562829610077, 0.01315789473155989930, 0.01973684209733990100, 0.02631578946311990269, 0.02875001438670990103, 0.03289473682890979578, 0.03947368419468980094, 0.04499999191018719952, 0.04605263156046980610, 0.05263157892624970025, 0.05921052629202970541, 0.06125001564970669610, 0.06578947365780969669, 0.07236842102358960471, 0.07749998933833390780, 0.07894736838936959600, 0.08552631575514958728, 0.09210526312092949530, 0.09375001447617459238, 0.09868421048671950635, 0.1052631578524590023, 0.1099999887899340001, 0.1118421052183189990, 0.1184210525840789924, 0.1249999999498389996, 0.1262500112023720034, 0.1315789473155989930, 0.1381578946813590003, 0.1424999906499269942, 0.1447368420472190109, 0.1513157894129790182, 0.1578947367787389977, 0.1587500068096430184, 0.1644736841444989772, 0.1710526315102589845, 0.1749999946880989865, 0.1776315788761189951, 0.1842105262418790024, 0.1907894736076390096, 0.1912500026574869838, 0.1973684209733990169, 0.2039473683392589998, 0.2075000001683630080, 0.2105263157050190070, 0.2171052630707789866, 0.2236842104365389938, 0.2302631578022990011, 0.2368421051681589840, 0.2400000060332939944, 0.2434210525339189912, 0.2499999998996789985, 0.2562499982428639855, 0.2565789472654390058, 0.2631578946311989853, 0.2697368419970589959, 0.2725000111344089704, 0.2763157893628189754, 0.2828947367285789549, 0.2887499948061880151, 0.2894736840943389899, 0.2960526314600980258, 0.3026315788259580364, 0.3050000144739509755, 0.3092105261917179604, 0.3157894735574779954, 0.3212499912461020402, 0.3223684209232379749, 0.3289473682890980410, 0.3355263156548580206, 0.3375000154242109862, 0.3421052630206180001, 0.3486842103863779796, 0.3537499889259840269, 0.3552631577521380146, 0.3618421051179980252, 0.3684210524837580047, 0.3700000138896000212, 0.3749999998495179843, 0.3815789472152780193, 0.3862499887360519857, 0.3881578945810379988, 0.3947368419468980094, 0.4013157893126579889, 0.4025000103777250371, 0.4078947366784179684, 0.4144736840441780035, 0.4187499909580220114, 0.4210526314099379830, 0.4276315787757979936, 0.4342105261415579731, 0.4350000059446500478, 0.4407894735073180081, 0.4473684208730779877, 0.4512499952738350251, 0.4539473682389379983, 0.4605263156046980333, 0.4671052629704580128, 0.4675000019802649787, 0.4736842103362179923, 0.4802631577019779718, 0.4837500008840890375, 0.4868421050678370388, 0.4934210524335980175, 0.4999999997993569978, 0.5065789471651169773, 0.5131578945308770123, 0.5162500067017939953, 0.5197368418967369674, 0.5263157892624970025, 0.5324999976354098941, 0.5328947366282570375, 0.5394736839940169615, 0.5460526313597769965, 0.5487500115865550088, 0.5526315787256369516, 0.5592105260913969866, 0.5649999940639039986, 0.5657894734571570217, 0.5723684208229169457, 0.5789473681887770118, 0.5812500145853020106, 0.5855263155545369358, 0.5921052629202969708, 0.5974999906071669642, 0.5986842102860570058, 0.6052631576518170409, 0.6118421050176769960, 0.6137500151446890762, 0.6184210523834369200, 0.6249999997491970660, 0.6299999885682440182, 0.6315789471149569900, 0.6381578944807170251, 0.6447368418465769802, 0.6462500132616529891, 0.6513157892123370152, 0.6578947365780970502, 0.6624999887461079373, 0.6644736839438569742, 0.6710526313096170092, 0.6776315786754769643, 0.6787500095369500830, 0.6842105260412369994, 0.6907894734069960352, 0.6949999913246359684, 0.6973684207727559592, 0.7039473681386160253, 0.7105263155043759493, 0.7112500050977950128, 0.7171052628701359843, 0.7236842102358960194, 0.7274999959004379013, 0.7302631576016559434, 0.7368421049675160095, 0.7434210523332759335, 0.7437500013550489841, 0.7499999996990360795, 0.7565789470647958925, 0.7600000016152699267, 0.7631578944305560386, 0.7697368417964159937, 0.7763157891621760287, 0.7828947365279360637, 0.7894736838936959877, 0.7925000073580670268, 0.7960526312594560228, 0.8026315786253159779, 0.8087499969874719641, 0.8092105259910760129, 0.8157894733568360479, 0.8223684207225959719, 0.8250000120025489103, 0.8289473680884560380, 0.8355263154542159620, 0.8412499933217569836, 0.8421052628199759971, 0.8486842101857360321, 0.8552631575514959561, 0.8575000146455890038, 0.8618421049173560222, 0.8684210522831159462, 0.8737499900031009403, 0.8749999996488759813, 0.8815789470146359053, 0.8881578943803950521, 0.8900000148124059818, 0.8947368417462548962, 0.9013157891120149312, 0.9062499882679529994, 0.9078947364777750773, 0.9144736838435350013, 0.9210526312092950363, 0.9225000125942429685, 0.9276315785751549914, 0.9342105259409150264, 0.9387499888219880129, 0.9407894733066750614, 0.9473684206724349854, 0.9539473680382950516, 0.9550000086894259166, 0.9605263154040549756, 0.9671052627698150106, 0.9712499916671659683, 0.9736842101355750456, 0.9802631575013349696, 0.9868421048671950357, 0.9875000041866580647, 0.9934210522329549597, 0.9999999995987149948 ),
 .UNSPECIFIED. ) ;
#8752=CARTESIAN_POINT ( 'NONE',  ( 11.54900921193965857, 11.99113680707610996, -1.243656623600980504 ) ) ;
#8754=CARTESIAN_POINT ( 'NONE',  ( 4.216071159329941587, 19.96663567226219982, 0.9010242342158106821 ) ) ;
#8764=CARTESIAN_POINT ( 'NONE',  ( 5.703757595802129821, 13.98659666219624675, -0.8855850056449419139 ) ) ;
#8765=CARTESIAN_POINT ( 'NONE',  ( 9.580014628452152792, 12.37431098505726013, -1.091745231617962997 ) ) ;
#8766=CARTESIAN_POINT ( 'NONE',  ( 7.883452240851667625, 14.83344068326428022, 7.768530631985846924 ) ) ;
#8767=CARTESIAN_POINT ( 'NONE',  ( 10.28446018311015742, 10.45470314796870248, 2.211657637955910083 ) ) ;
#8774=CARTESIAN_POINT ( 'NONE',  ( 11.09769854542326861, 17.23211763628403403, 6.743335639867776621 ) ) ;
#8775=CARTESIAN_POINT ( 'NONE',  ( 11.14235852144809868, 12.31819272753022254, -2.976272612453031652 ) ) ;
#8777=CARTESIAN_POINT ( 'NONE',  ( 10.69018650721368502, 11.75921469276450182, 3.871793181027931574 ) ) ;
#8780=CARTESIAN_POINT ( 'NONE',  ( 12.94499384098450001, 22.19916506436698000, 0.6856174611774060734 ) ) ;
#8781=CARTESIAN_POINT ( 'NONE',  ( 1.162433488273821647, 12.61021756743670252, 8.063620084594539605 ) ) ;
#8784=CARTESIAN_POINT ( 'NONE',  ( 6.437478173552243277, 10.90738268085100060, 3.037243646032500521 ) ) ;
#8795=CARTESIAN_POINT ( 'NONE',  ( 5.416218533946238090, 17.73239028602085199, 8.614334791690790638 ) ) ;
#8806=CARTESIAN_POINT ( 'NONE',  ( 13.42753679035789105, 21.40794255445344163, 2.286611137732273757 ) ) ;
#8807=CARTESIAN_POINT ( 'NONE',  ( 1.708238430344685144, 13.92071940861192658, 9.099522166506517351 ) ) ;
#8810=CARTESIAN_POINT ( 'NONE',  ( 4.373404510246160726, 11.14075155979819165, 2.905983407409085117 ) ) ;
#8816=CARTESIAN_POINT ( 'NONE',  ( 7.721685948793786558, 12.55088109015116693, -0.3031984390922063399 ) ) ;
#8821=CARTESIAN_POINT ( 'NONE',  ( 3.407061386797684666, 14.37727598515552607, 7.987795225252861897 ) ) ;
#8827=CARTESIAN_POINT ( 'NONE',  ( 3.515735123799623274, 17.35852335215787789, 9.108230659777527549 ) ) ;
#8831=CARTESIAN_POINT ( 'NONE',  ( 5.343034057657806812, 20.72645064840772022, 2.101598573111083113 ) ) ;
#8837=CARTESIAN_POINT ( 'NONE',  ( 9.146678809762240903, 19.11784201969034314, -2.518986951451899436 ) ) ;
#8840=CARTESIAN_POINT ( 'NONE',  ( 11.51458866710784434, 21.99093949232998213, 2.562257468935384530 ) ) ;
#8844=CARTESIAN_POINT ( 'NONE',  ( 13.03574908598719517, 21.42208332277566285, 0.9446814558890389568 ) ) ;
#8845=CARTESIAN_POINT ( 'NONE',  ( 9.288485439755762130, 12.58942835895980572, 6.591978047692478526 ) ) ;
#8846=CARTESIAN_POINT ( 'NONE',  ( 6.327178061961348909, 11.65658372465740200, 2.461826360968837779 ) ) ;
#8847=CARTESIAN_POINT ( 'NONE',  ( 5.606189282461859769, 16.04232475255113499, -1.387877448415188342 ) ) ;
#8852=CARTESIAN_POINT ( 'NONE',  ( 7.848665660996588578, 21.72673311005876329, 3.154536144953404175 ) ) ;
#8853=CARTESIAN_POINT ( 'NONE',  ( 4.966346748821892199, 12.29804937889246119, 5.546774599257833671 ) ) ;
#8855=CARTESIAN_POINT ( 'NONE',  ( 3.884858786145676035, 12.19654146317258103, 0.3546744299869324935 ) ) ;
#8856=CARTESIAN_POINT ( 'NONE',  ( 1.388599495393930683, 18.36893808807919015, 9.176162539399413731 ) ) ;
#8858=CARTESIAN_POINT ( 'NONE',  ( 5.598452204629278839, 20.83490078207852392, 3.741209306395075540 ) ) ;
#8865=CARTESIAN_POINT ( 'NONE',  ( 11.25546319390698535, 17.89488212436745229, 7.371895500363925713 ) ) ;
#8870=CARTESIAN_POINT ( 'NONE',  ( 11.37527975260994850, 18.06908308185732537, -3.317263757504213206 ) ) ;
#8881=CARTESIAN_POINT ( 'NONE',  ( 7.626149225290501654, 21.00148274865230036, 3.166616558793210245 ) ) ;
#8882=CARTESIAN_POINT ( 'NONE',  ( 4.529126002162273679, 19.77844967572892898, 6.376247277523235724 ) ) ;
#8883=CARTESIAN_POINT ( 'NONE',  ( 14.13422953375516045, 20.59196267482642284, 3.825818811277526876 ) ) ;
#8884=CARTESIAN_POINT ( 'NONE',  ( 3.281879507946431573, 11.63542902183100125, 5.027702361350555371 ) ) ;
#8892=CARTESIAN_POINT ( 'NONE',  ( 9.492769369201601748, 16.63237982350910826, 8.085771285227329130 ) ) ;
#8897=CARTESIAN_POINT ( 'NONE',  ( 9.332239567752825593, 16.42172345158643765, -2.863492792668257625 ) ) ;
#8900=CARTESIAN_POINT ( 'NONE',  ( 0.9717421347890942140, 18.89460405061472414, 9.004989399516528437 ) ) ;
#8903=CARTESIAN_POINT ( 'NONE',  ( 7.473138860522134941, 13.60421353648831300, 7.673710903342175982 ) ) ;
#8927=CARTESIAN_POINT ( 'NONE',  ( 13.04321057777464787, 16.70014932840772204, 6.526733902502721563 ) ) ;
#8928=CARTESIAN_POINT ( 'NONE',  ( 7.302229971812547404, 18.51489551114278953, 8.052680363647331419 ) ) ;
#8931=CARTESIAN_POINT ( 'NONE',  ( 5.354525716978236538, 12.51143086260616144, 7.194241134548868821 ) ) ;
#8936=CARTESIAN_POINT ( 'NONE',  ( 7.442367890852062295, 14.90359003035201191, -1.906045328434554653 ) ) ;
#8944=CARTESIAN_POINT ( 'NONE',  ( 2.636384871323212753, 20.46330206851546052, 7.042598730623302217 ) ) ;
#8947=CARTESIAN_POINT ( 'NONE',  ( 7.320132777942092162, 12.26967076330688222, 5.547411630589742515 ) ) ;
#8952=CARTESIAN_POINT ( 'NONE',  ( 8.286930802166120102, 19.91511611422710359, 6.446135514764869789 ) ) ;
#8957=CARTESIAN_POINT ( 'NONE',  ( 11.96407914667388361, 10.46320835736658239, 0.6102883513782707547 ) ) ;
#8961=CARTESIAN_POINT ( 'NONE',  ( 7.434653127054422050, 12.56819603257475748, -1.447669836965668644 ) ) ;
#8962=CARTESIAN_POINT ( 'NONE',  ( 6.215497495051750754, 20.44527992609954126, 5.212841242474709702 ) ) ;
#8964=CARTESIAN_POINT ( 'NONE',  ( 6.126552632935823972, 11.96686506477097645, 1.644263794841153370 ) ) ;
#8966=CARTESIAN_POINT ( 'NONE',  ( 11.59039627428740005, 17.69506805168922980, 7.363997034513484863 ) ) ;
#8970=CARTESIAN_POINT ( 'NONE',  ( 1.621773686558225069, 14.62646646242487769, -0.4960749032165705508 ) ) ;
#8971=CARTESIAN_POINT ( 'NONE',  ( 1.567395821070151074, 17.31328409496832066, 9.515441300692291549 ) ) ;
#8973=CARTESIAN_POINT ( 'NONE',  ( 6.053126112950039328, 12.01118930601124291, 1.445651676772871319 ) ) ;
#8980=CARTESIAN_POINT ( 'NONE',  ( 10.50516453618270951, 10.67034598166200077, 3.014593022769773256 ) ) ;
#8983=CARTESIAN_POINT ( 'NONE',  ( 11.19867328698874687, 16.63172145237887278, -3.589918250282487122 ) ) ;
#8989=CARTESIAN_POINT ( 'NONE',  ( 5.060608184540046572, 20.55003013079386065, 2.242568649026101646 ) ) ;
#8993=CARTESIAN_POINT ( 'NONE',  ( 8.715318583361199245, 19.62664610146546096, 6.014593122911379375 ) ) ;
#8995=CARTESIAN_POINT ( 'NONE',  ( 13.94935210066752163, 20.92845091260043944, 3.339972092365505407 ) ) ;
#8996=CARTESIAN_POINT ( 'NONE',  ( 3.949281531805286072, 14.74976095948969679, 8.888991823293663330 ) ) ;
#8998=CARTESIAN_POINT ( 'NONE',  ( 11.94677749553334323, 10.33025398667194139, 0.6609700684136409210 ) ) ;
#9004=CARTESIAN_POINT ( 'NONE',  ( 11.12364941492027803, 17.00792697408808962, 6.778445003776157662 ) ) ;
#9005=CARTESIAN_POINT ( 'NONE',  ( 11.48982677350561232, 15.66509967140728854, 7.652876522509257207 ) ) ;
#9008=CARTESIAN_POINT ( 'NONE',  ( 9.295090217099296837, 15.49936585922396937, -2.781353060168781255 ) ) ;
#9011=CARTESIAN_POINT ( 'NONE',  ( 3.093622439059696472, 16.50247895544803711, 9.043415154008217272 ) ) ;
#9014=CARTESIAN_POINT ( 'NONE',  ( 7.090215797885481841, 11.68299152395092122, 5.835935845868474026 ) ) ;
#9021=CARTESIAN_POINT ( 'NONE',  ( 2.109252989286876101, 17.81722186424291721, 0.3028858017987954843 ) ) ;
#9024=CARTESIAN_POINT ( 'NONE',  ( 11.41261416030154408, 22.17023050789328309, 2.001960333732383024 ) ) ;
#9033=CARTESIAN_POINT ( 'NONE',  ( 4.090788008712939572, 21.31629319454957994, 5.251805483008242348 ) ) ;
#9036=CARTESIAN_POINT ( 'NONE',  ( 5.279029129154737987, 12.19382779458062771, 6.839692948426927543 ) ) ;
#9041=CARTESIAN_POINT ( 'NONE',  ( 3.240852002830010292, 13.09810700923016036, 7.006825282356911266 ) ) ;
#9047=CARTESIAN_POINT ( 'NONE',  ( 3.600293491139347157, 16.51615582718421393, 9.202227310041637409 ) ) ;
#9049=CARTESIAN_POINT ( 'NONE',  ( 5.230971163609982710, 12.02159401923784010, 5.278208563677478260 ) ) ;
#9051=CARTESIAN_POINT ( 'NONE',  ( 13.15941616736590802, 22.07931810055205446, 2.007639991878180652 ) ) ;
#9056=CARTESIAN_POINT ( 'NONE',  ( 10.31787650444773341, 11.27323348914452161, 4.153725677044106668 ) ) ;
#9060=CARTESIAN_POINT ( 'NONE',  ( 11.97810099218075308, 10.45522238918808178, 0.6684068655140054105 ) ) ;
#9064=CARTESIAN_POINT ( 'NONE',  ( 7.250640286420714453, 16.37904396954605701, -2.887332892799749917 ) ) ;
#9065=CARTESIAN_POINT ( 'NONE',  ( 6.106529886068845947, 12.01118930601124291, 1.429659103004671250 ) ) ;
#9067=CARTESIAN_POINT ( 'NONE',  ( 5.819762523047388392, 17.94946781983131245, -1.138627438642019429 ) ) ;
#9068=CARTESIAN_POINT ( 'NONE',  ( 7.098073765475375829, 12.80169766613603599, 6.043837936590163551 ) ) ;
#9072=CARTESIAN_POINT ( 'NONE',  ( 9.469108807279354778, 17.35598761042881577, -3.664943468583037767 ) ) ;
#9074=CARTESIAN_POINT ( 'NONE',  ( 3.243422562972307688, 11.89954130989696246, 6.891751807687494846 ) ) ;
#9075=CARTESIAN_POINT ( 'NONE',  ( 0.8494540250199152931, 20.05826837460356771, 7.883665465059968014 ) ) ;
#9077=CARTESIAN_POINT ( 'NONE',  ( 0.01944810670579354139, 14.29202264928412092, 1.254942201865596463 ) ) ;
#9082=CARTESIAN_POINT ( 'NONE',  ( 11.44433539449762804, 15.04579128119321219, 7.441666735878229133 ) ) ;
#9085=CARTESIAN_POINT ( 'NONE',  ( 11.29905453907457868, 17.57833764777731744, -3.460908599073576397 ) ) ;
#9087=CARTESIAN_POINT ( 'NONE',  ( 5.402704644578218307, 14.08031241623537255, -1.660995405501500155 ) ) ;
#9095=CARTESIAN_POINT ( 'NONE',  ( 11.12613972328005119, 16.27078869972546116, -3.689852400265816179 ) ) ;
#9097=CARTESIAN_POINT ( 'NONE',  ( 7.679475497374705917, 18.07321731131985842, -1.947026857138824063 ) ) ;
#9106=CARTESIAN_POINT ( 'NONE',  ( 9.243180543658688464, 18.56570064461385527, 7.646858442508960962 ) ) ;
#9109=CARTESIAN_POINT ( 'NONE',  ( 10.68304280333123835, 11.74562633852015203, 3.840012745435023689 ) ) ;
#9111=CARTESIAN_POINT ( 'NONE',  ( 0.2158207035600169243, 20.08891550228490530, 6.180427975396654894 ) ) ;
#9112=CARTESIAN_POINT ( 'NONE',  ( -0.5255128162433173600, 15.65082615746288219, 0.5089085096668227726 ) ) ;
#9115=CARTESIAN_POINT ( 'NONE',  ( 7.454305085027373323, 13.41251517923412706, 7.565232220981850553 ) ) ;
#9123=CARTESIAN_POINT ( 'NONE',  ( 0.03927176397120358403, 15.80852762767634800, 0.8372861472476095246 ) ) ;
#9124=PRODUCT ( 'Locking Pawl Compression Spring', 'Locking Pawl Compression Spring', '', ( #5335 ) ) ;
#9137=CARTESIAN_POINT ( 'NONE',  ( -0.2015346878679116771, 15.59640844431605267, -0.007168570956162228364 ) ) ;
#9140=CARTESIAN_POINT ( 'NONE',  ( 5.590944741272595664, 15.72999216326778260, 8.764459480800841362 ) ) ;
#9147=CARTESIAN_POINT ( 'NONE',  ( 2.818771752949199350, 12.10965044584980888, 4.995725464678207217 ) ) ;
#9153=CARTESIAN_POINT ( 'NONE',  ( 2.936231591482770131, 19.83055965519156416, 7.812606543334467801 ) ) ;
#9155=CARTESIAN_POINT ( 'NONE',  ( 6.368383225667405334, 11.93222000202738187, 1.317153128801042072 ) ) ;
#9161=CARTESIAN_POINT ( 'NONE',  ( 9.625378508224750718, 20.58315642183951866, -1.315007443808327237 ) ) ;
#9164=CARTESIAN_POINT ( 'NONE',  ( 13.38508960593052066, 14.68835664565479604, 6.944885673946169291 ) ) ;
#9169=CARTESIAN_POINT ( 'NONE',  ( 7.953648525153114157, 11.02408685177427117, 0.8496204234235359420 ) ) ;
#9170=CARTESIAN_POINT ( 'NONE',  ( 4.040739369786842339, 20.53326216353070421, 5.052342526274332002 ) ) ;
#9174=CARTESIAN_POINT ( 'NONE',  ( 8.750313129456580796, 19.14012259891230627, 6.327658032475317107 ) ) ;
#9175=CARTESIAN_POINT ( 'NONE',  ( 7.321344744572315655, 14.84602651755674252, 7.391589468013401110 ) ) ;
#9177=CARTESIAN_POINT ( 'NONE',  ( 1.940379840341371898, 20.36792767702591078, 5.166629419378853783 ) ) ;
#9180=CARTESIAN_POINT ( 'NONE',  ( 12.87297671240983732, 10.82393886236346248, 2.518080570580241595 ) ) ;
#9182=CARTESIAN_POINT ( 'NONE',  ( 3.414760669001324800, 21.44980502101282127, 3.518543128841764567 ) ) ;
#9183=CARTESIAN_POINT ( 'NONE',  ( 1.088531530542938830, 19.46978492123518478, 8.481480395730187638 ) ) ;
#9185=CARTESIAN_POINT ( 'NONE',  ( 1.053492159257005678, 12.39630382929348151, 6.286052961942981909 ) ) ;
#9191=CARTESIAN_POINT ( 'NONE',  ( 11.13272815207053412, 12.04177085653310719, 5.716067944331810757 ) ) ;
#9196=CARTESIAN_POINT ( 'NONE',  ( 5.452433434195132378, 13.50695901949029221, -1.362618185186349695 ) ) ;
#9200=CARTESIAN_POINT ( 'NONE',  ( -0.08564303786872971835, 20.23672349479678090, 5.121204619610163711 ) ) ;
#9201=CARTESIAN_POINT ( 'NONE',  ( 6.119526778620084428, 20.42711211122828630, 5.032656639018053824 ) ) ;
#9206=CARTESIAN_POINT ( 'NONE',  ( 7.928377447478991868, 12.05201058041374118, 0.2304873749790961046 ) ) ;
#9207=CARTESIAN_POINT ( 'NONE',  ( 4.411209516546746201, 19.98771269606189449, 6.079393835653899458 ) ) ;
#9208=CARTESIAN_POINT ( 'NONE',  ( 11.37179424920164728, 18.10733791853621710, -3.426064086753738636 ) ) ;
#9217=CARTESIAN_POINT ( 'NONE',  ( 7.631829889725195493, 11.33951387506710162, -0.1018811746545836144 ) ) ;
#9222=CARTESIAN_POINT ( 'NONE',  ( 10.46210129196975558, 11.44384454131881057, 2.868262577821945047 ) ) ;
#9224=CARTESIAN_POINT ( 'NONE',  ( 1.336750686926562848, 17.19894283162252790, 8.761756363425694971 ) ) ;
#9227=CARTESIAN_POINT ( 'NONE',  ( 0.3464597092991406058, 19.87555530259703929, 7.760565032948996134 ) ) ;
#9251=CARTESIAN_POINT ( 'NONE',  ( 6.302627457059999827, 21.18238311700324417, 5.536129331643387275 ) ) ;
#9254=CARTESIAN_POINT ( 'NONE',  ( 3.691539032982900093, 12.86983919638163520, -0.1392865449577171677 ) ) ;
#9257=CARTESIAN_POINT ( 'NONE',  ( 1.190075203671829840, 12.78130600077101064, 6.867397390420004299 ) ) ;
#9267=CARTESIAN_POINT ( 'NONE',  ( 3.648412331247147034, 14.85656584819127879, 8.991936108934527994 ) ) ;
#9271=CARTESIAN_POINT ( 'NONE',  ( 4.032829679376786380, 14.00947850804536721, -0.3008704057647156316 ) ) ;
#9278=CARTESIAN_POINT ( 'NONE',  ( 7.743276922147756203, 20.96234599748222038, 5.025255436566072653 ) ) ;
#9281=CARTESIAN_POINT ( 'NONE',  ( 12.18403663738019738, 10.39853869505617112, 1.520800266583003379 ) ) ;
#9285=CARTESIAN_POINT ( 'NONE',  ( 7.218832108077395837, 14.89085544374305670, -2.696453293844645938 ) ) ;
#9287=CARTESIAN_POINT ( 'NONE',  ( 1.886475874931245800, 14.88386107855003360, 0.2258545542662658556 ) ) ;
#9289=CARTESIAN_POINT ( 'NONE',  ( 6.833200748973188965, 20.60529512528366780, 1.326882497385993620 ) ) ;
#9290=CARTESIAN_POINT ( 'NONE',  ( 7.205660636103451644, 13.38211048488514088, 6.599037780638883355 ) ) ;
#9294=CARTESIAN_POINT ( 'NONE',  ( 11.04974211190474342, 19.58043239906450239, 6.708260239347588971 ) ) ;
#9299=CARTESIAN_POINT ( 'NONE',  ( 3.893743123751922663, 19.12659651351990320, -0.8000309555518917426 ) ) ;
#9300=CARTESIAN_POINT ( 'NONE',  ( 1.039725201830166368, 11.58047422083137157, 6.064744957957070248 ) ) ;
#9303=CARTESIAN_POINT ( 'NONE',  ( 4.897223231123858156, 12.10224027996176233, 5.344960981349180962 ) ) ;
#9308=CARTESIAN_POINT ( 'NONE',  ( 9.536567547932234490, 11.50748222034787105, -1.063888143023027588 ) ) ;
#9312=CARTESIAN_POINT ( 'NONE',  ( 5.401778888224800568, 16.44581222338524640, -2.160592110064928129 ) ) ;
#9317=CARTESIAN_POINT ( 'NONE',  ( 5.597516759145264587, 20.74156677563692597, 3.659026675076807678 ) ) ;
#9322=CARTESIAN_POINT ( 'NONE',  ( 10.60244234216251691, 11.17647817907412211, 2.092258798280409948 ) ) ;
#9323=CARTESIAN_POINT ( 'NONE',  ( 5.243231333258746574, 17.19721735590602663, 7.955804737421353856 ) ) ;
#9325=CARTESIAN_POINT ( 'NONE',  ( 11.63500593880946177, 11.69841282151974227, -0.9689828243709948108 ) ) ;
#9330=CARTESIAN_POINT ( 'NONE',  ( 4.591792411387702444, 20.55650562689407579, 6.636581573250831312 ) ) ;
#9336=CARTESIAN_POINT ( 'NONE',  ( 1.096763541954664856, 18.37323406418106586, 8.312844033778342023 ) ) ;
#9337=CARTESIAN_POINT ( 'NONE',  ( 1.944119829274491229, 19.53481664226216452, 0.8650063851298049888 ) ) ;
#9346=CARTESIAN_POINT ( 'NONE',  ( 0.3678923928972068214, 18.28356801376448360, 1.246736171314209773 ) ) ;
#9350=CARTESIAN_POINT ( 'NONE',  ( 1.928043380615611868, 16.41701505613207956, 0.06728629053293294637 ) ) ;
#9351=CARTESIAN_POINT ( 'NONE',  ( 9.558161459289578943, 19.33115936737788232, -3.006980407988670390 ) ) ;
#9363=CARTESIAN_POINT ( 'NONE',  ( 7.150949527180841869, 11.65893940570930276, 6.001705760337040729 ) ) ;
#9366=CARTESIAN_POINT ( 'NONE',  ( 3.626612422794881052, 17.28006496868525232, -1.351333894438823569 ) ) ;
#9372=CARTESIAN_POINT ( 'NONE',  ( 3.126795315295423983, 12.66988178275929222, 6.437474586529948084 ) ) ;
#9378=CARTESIAN_POINT ( 'NONE',  ( 3.632498785534259866, 14.40071795978559699, 8.832255087646766256 ) ) ;
#9388=CARTESIAN_POINT ( 'NONE',  ( 7.527094280029700712, 11.97223945099518083, 0.3035030689026688155 ) ) ;
#9391=CARTESIAN_POINT ( 'NONE',  ( 13.38623696279685760, 14.73335078723855673, 6.957530059424012592 ) ) ;
#9395=CARTESIAN_POINT ( 'NONE',  ( 7.352509731926520686, 13.08366748006759650, -1.852861239733443410 ) ) ;
#9398=CARTESIAN_POINT ( 'NONE',  ( 7.902835724841917653, 20.71418818157466646, 4.167812925585346662 ) ) ;
#9401=CARTESIAN_POINT ( 'NONE',  ( 2.675095758391589751, 19.49110477356257576, 7.034375472487891301 ) ) ;
#9404=CARTESIAN_POINT ( 'NONE',  ( 12.76954518747143119, 10.51393144722840134, 2.621729904346445483 ) ) ;
#9405=CARTESIAN_POINT ( 'NONE',  ( 13.44218100725569265, 22.16307759405859557, 1.935254454476087238 ) ) ;
#9407=CARTESIAN_POINT ( 'NONE',  ( 5.340688094622302096, 12.35012481907357973, 7.188016169931777277 ) ) ;
#9408=CARTESIAN_POINT ( 'NONE',  ( 0.9906448663280645883, 11.53243573101070218, 5.849629943059694526 ) ) ;
#9411=CARTESIAN_POINT ( 'NONE',  ( 2.193444281137359564, 17.94014877828372079, 0.2300559325516845777 ) ) ;
#9417=CARTESIAN_POINT ( 'NONE',  ( 11.44293608409318708, 15.29742052837710276, 7.486644574264715857 ) ) ;
#9420=CARTESIAN_POINT ( 'NONE',  ( 5.389318750439047179, 16.20232685991933863, -2.152549537583109629 ) ) ;
#9422=CARTESIAN_POINT ( 'NONE',  ( 0.7815218943751861547, 12.12637795047220202, 4.853680457913782220 ) ) ;
#9425=CARTESIAN_POINT ( 'NONE',  ( 5.239375586970837162, 20.67732964299643683, 2.712271571789475644 ) ) ;
#9429=CARTESIAN_POINT ( 'NONE',  ( 7.023078859562801313, 11.74208123617664157, 4.211509649359884477 ) ) ;
#9431=CARTESIAN_POINT ( 'NONE',  ( 3.903910055091213582, 16.51832937791753864, 9.132019056122507195 ) ) ;
#9435=CARTESIAN_POINT ( 'NONE',  ( -0.1849527688498912581, 20.63369000000000142, 5.150944030050081501 ) ) ;
#9442=CARTESIAN_POINT ( 'NONE',  ( 9.965102658262930291, 19.76523925788982083, -1.574950225675940452 ) ) ;
#9444=CARTESIAN_POINT ( 'NONE',  ( 1.472840618554822401, 15.71206864735696662, 8.805158946288562660 ) ) ;
#9446=CARTESIAN_POINT ( 'NONE',  ( 6.421918896133771426, 11.00346980177178224, 4.321624500989655004 ) ) ;
#9454=CARTESIAN_POINT ( 'NONE',  ( 0.1865804364509018876, 17.36630291547838922, 0.9075020708449259565 ) ) ;
#9457=CARTESIAN_POINT ( 'NONE',  ( 10.66833303431421065, 11.64719608603622270, 3.888054322948657493 ) ) ;
#9458=CARTESIAN_POINT ( 'NONE',  ( 2.593946987045366637, 19.51451841538450438, 1.385786389991116030 ) ) ;
#9460=CARTESIAN_POINT ( 'NONE',  ( 7.833861672054659664, 20.10324751469710236, -1.664036087720620172 ) ) ;
#9470=CARTESIAN_POINT ( 'NONE',  ( 5.885296502875437596, 11.58475123937168050, 0.5917220264446930722 ) ) ;
#9473=CARTESIAN_POINT ( 'NONE',  ( 3.633444216715743913, 13.25045984076455774, -0.4357252384333677453 ) ) ;
#9484=CARTESIAN_POINT ( 'NONE',  ( 3.318611589506196058, 12.22314404142716171, 7.169435018240098323 ) ) ;
#9494=CARTESIAN_POINT ( 'NONE',  ( 10.96785682973680132, 15.74068497743424189, 7.058765615034965357 ) ) ;
#9497=CARTESIAN_POINT ( 'NONE',  ( 10.97135499597955821, 13.84880078443595153, -3.805639818675497388 ) ) ;
#9503=CARTESIAN_POINT ( 'NONE',  ( 8.013468311210377948, 20.40777636399528916, -1.234548792046807231 ) ) ;
#9505=CARTESIAN_POINT ( 'NONE',  ( 8.115152695261373950, 20.48792095732073548, 4.726086490775795568 ) ) ;
#9507=CARTESIAN_POINT ( 'NONE',  ( 2.827233722371560454, 19.13019741901238646, 7.400779595140909883 ) ) ;
#9511=CARTESIAN_POINT ( 'NONE',  ( 3.885025484994841793, 19.12622466589174053, -0.7968053903680345496 ) ) ;
#9512=CARTESIAN_POINT ( 'NONE',  ( 1.698356033660393782, 15.60214721349694145, 9.558218796784109017 ) ) ;
#9514=CARTESIAN_POINT ( 'NONE',  ( 3.007751381752465925, 20.19548487530456171, 2.160188886951264209 ) ) ;
#9523=CARTESIAN_POINT ( 'NONE',  ( 9.163629188038463269, 17.17735727408968316, -3.567318444911117936 ) ) ;
#9527=CARTESIAN_POINT ( 'NONE',  ( 12.70203135958802143, 21.28102902729012058, 0.03842769806917034625 ) ) ;
#9528=CARTESIAN_POINT ( 'NONE',  ( 5.839807527371365659, 19.32544709538717953, -1.321624354577452420 ) ) ;
#9530=CARTESIAN_POINT ( 'NONE',  ( 6.219149445766309903, 11.66082179432958377, 2.494857446435102322 ) ) ;
#9535=CARTESIAN_POINT ( 'NONE',  ( 7.835562974045392259, 21.09291897731618093, 3.110782529598515200 ) ) ;
#9538=CARTESIAN_POINT ( 'NONE',  ( 1.335867332802413321, 21.11849136136308047, 3.284394833007574732 ) ) ;
#9540=CARTESIAN_POINT ( 'NONE',  ( 6.751191191974612593, 11.44921631601969203, 2.721930595337344716 ) ) ;
#9551=CARTESIAN_POINT ( 'NONE',  ( 10.16671340789460487, 20.24294540929401975, -1.062930679991952232 ) ) ;
#9553=CARTESIAN_POINT ( 'NONE',  ( -0.1849527131266449076, 20.23672349358593792, 5.150944217628095068 ) ) ;
#9556=CARTESIAN_POINT ( 'NONE',  ( -0.3117854395798596578, 15.69350566183319273, 0.7735685379110269766 ) ) ;
#9560=ORIENTED_EDGE ( 'NONE', *, *, #6778, .T. ) ;
#9565=CARTESIAN_POINT ( 'NONE',  ( 10.74157715189224049, 19.11273924176536099, 6.105315142739899947 ) ) ;
#9566=CARTESIAN_POINT ( 'NONE',  ( 7.534728409618654865, 21.81389254086020202, 3.255105835292287697 ) ) ;
#9577=CARTESIAN_POINT ( 'NONE',  ( 1.577524075207264342, 16.44750854861721834, -0.7742535818055841235 ) ) ;
#9580=CARTESIAN_POINT ( 'NONE',  ( 4.336475100890431200, 20.29160327599122837, 0.2727996324811496898 ) ) ;
#9593=CARTESIAN_POINT ( 'NONE',  ( 3.645750917779165157, 14.75475157674404691, 8.959486830434602922 ) ) ;
#9605=CARTESIAN_POINT ( 'NONE',  ( 8.970099111347026977, 16.58550361725992772, 7.489321828938900083 ) ) ;
#9608=CARTESIAN_POINT ( 'NONE',  ( 11.11774465870644946, 12.58812117891224602, -3.039815099727486647 ) ) ;
#9613=CARTESIAN_POINT ( 'NONE',  ( 7.143155634628241657, 20.85017009081515127, 2.146504125371351268 ) ) ;
#9618=CARTESIAN_POINT ( 'NONE',  ( 13.68236715249897273, 22.02408774531873803, 1.842928636733466297 ) ) ;
#9621=CARTESIAN_POINT ( 'NONE',  ( 5.597898337543679048, 15.64116283607404689, 8.868322025159471877 ) ) ;
#9622=CARTESIAN_POINT ( 'NONE',  ( 1.185536613426001029, 11.80994437923685325, 6.710694494223975681 ) ) ;
#9627=CARTESIAN_POINT ( 'NONE',  ( 3.488048491702187892, 16.48205525895868462, 8.498464847168406777 ) ) ;
#9633=CARTESIAN_POINT ( 'NONE',  ( 6.820530933416198316, 11.28301579719734171, 5.079670947778354595 ) ) ;
#9635=CARTESIAN_POINT ( 'NONE',  ( 10.15167233650402423, 21.12619246702464437, -1.194501015968789881 ) ) ;
#9638=CARTESIAN_POINT ( 'NONE',  ( 7.512256438360484623, 21.70324290413769219, 3.137831150439451378 ) ) ;
#9640=CARTESIAN_POINT ( 'NONE',  ( -0.6269647750601365921, 20.05113242023052322, 3.964184760248283368 ) ) ;
#9643=CARTESIAN_POINT ( 'NONE',  ( 6.490352011916383113, 19.85778700119437445, 5.984496968252292604 ) ) ;
#9647=CARTESIAN_POINT ( 'NONE',  ( 8.122941931605208055, 11.97223945099518083, 0.1250674085377973255 ) ) ;
#9648=CARTESIAN_POINT ( 'NONE',  ( 5.182497302550231666, 17.60298196088504952, 7.859483784311269261 ) ) ;
#9650=CARTESIAN_POINT ( 'NONE',  ( 2.972756920594751495, 11.23314441701904087, 5.199616837626352073 ) ) ;
#9654=CARTESIAN_POINT ( 'NONE',  ( 6.664121936844724203, 11.05293067483325054, 2.719061972016084461 ) ) ;
#9663=CARTESIAN_POINT ( 'NONE',  ( 12.47845653567284252, 19.78773270843656107, 5.077144801013766084 ) ) ;
#9677=CARTESIAN_POINT ( 'NONE',  ( 11.28320163957777034, 21.35754284105190237, 1.995920704044074734 ) ) ;
#9679=CARTESIAN_POINT ( 'NONE',  ( 9.071664746958145287, 21.95697059135326512, 1.680270923673110817 ) ) ;
#9690=CARTESIAN_POINT ( 'NONE',  ( 7.484288373972455943, 14.71660677864375799, 8.297660023429632048 ) ) ;
#9693=CARTESIAN_POINT ( 'NONE',  ( 4.110461435211806958, 11.46719836097712175, 1.771832583802136485 ) ) ;
#9697=CARTESIAN_POINT ( 'NONE',  ( 0.7209684937559326379, 12.21855677317197042, 4.661992077991788719 ) ) ;
#9705=CARTESIAN_POINT ( 'NONE',  ( 3.652517087777511495, 15.28827823227851823, 9.103988936570855728 ) ) ;
#9715=CARTESIAN_POINT ( 'NONE',  ( 12.43409603417085840, 21.88443657126030217, 0.5679272856640997791 ) ) ;
#9717=CARTESIAN_POINT ( 'NONE',  ( 10.94319742441099130, 16.17454428140013789, -4.347327864958337784 ) ) ;
#9723=CARTESIAN_POINT ( 'NONE',  ( 9.221739120490575203, 16.47952005171203638, 7.223770130881796092 ) ) ;
#9726=CARTESIAN_POINT ( 'NONE',  ( 13.66532433034244320, 22.04443180264593138, 1.851018102324262227 ) ) ;
#9729=CARTESIAN_POINT ( 'NONE',  ( 5.331667582216989665, 12.35064203674882144, 7.190230353468857416 ) ) ;
#9730=CARTESIAN_POINT ( 'NONE',  ( 0.3826712150604609786, 11.72341736596831119, 3.192093716112220037 ) ) ;
#9733=CARTESIAN_POINT ( 'NONE',  ( 2.289123268938977773, 12.53619568343860102, 2.127697637126212626 ) ) ;
#9739=CARTESIAN_POINT ( 'NONE',  ( 11.38283456236634983, 15.66465130118744398, 7.689368460568949182 ) ) ;
#9740=CARTESIAN_POINT ( 'NONE',  ( 9.449104951163006305, 19.05165199613717419, -2.994418371723121197 ) ) ;
#9742=CARTESIAN_POINT ( 'NONE',  ( 8.199318354130985753, 21.22306264867357939, 5.015000832792440022 ) ) ;
#9744=CARTESIAN_POINT ( 'NONE',  ( 3.377149599728166862, 13.61484622919644139, 7.603189621071223314 ) ) ;
#9750=CARTESIAN_POINT ( 'NONE',  ( 8.814777221004259644, 20.70901284984930157, 0.06808976589407680913 ) ) ;
#9751=CARTESIAN_POINT ( 'NONE',  ( 5.276951256079190244, 16.94228911491327594, 8.002382959928944217 ) ) ;
#9752=CARTESIAN_POINT ( 'NONE',  ( 5.897833037357203878, 15.65151869617330682, 8.688657562670337953 ) ) ;
#9755=CARTESIAN_POINT ( 'NONE',  ( 6.657844012983366255, 11.04603686758454018, 2.720439051447127721 ) ) ;
#9764=CARTESIAN_POINT ( 'NONE',  ( 9.434918120449587775, 17.44535875574114314, -2.750588363923260893 ) ) ;
#9778=CARTESIAN_POINT ( 'NONE',  ( 7.810570628557063522, 12.04767321495844179, 0.2632024995130942124 ) ) ;
#9779=CARTESIAN_POINT ( 'NONE',  ( 2.929006426436138621, 20.11622341764773125, 2.226180933043676369 ) ) ;
#9781=CARTESIAN_POINT ( 'NONE',  ( 7.419152651973274004, 18.37230293632699230, -2.654332437207524542 ) ) ;
#9784=CARTESIAN_POINT ( 'NONE',  ( 9.160622857117788342, 21.06163945996668119, 1.886083935128181732 ) ) ;
#9785=CARTESIAN_POINT ( 'NONE',  ( 9.810057962265917197, 21.83905339296156356, 3.589454503528180851 ) ) ;
#9793=CARTESIAN_POINT ( 'NONE',  ( 5.392306785532915647, 17.51139020089073028, 8.808111370990710398 ) ) ;
#9796=CARTESIAN_POINT ( 'NONE',  ( 5.682439063020419567, 21.52104170944363304, 3.898124636232009887 ) ) ;
#9802=CARTESIAN_POINT ( 'NONE',  ( 7.305327845366293538, 16.38034437524489206, -3.033659931233324780 ) ) ;
#9803=CARTESIAN_POINT ( 'NONE',  ( 4.541085437132517555, 11.87214774573713072, 3.616631113229732630 ) ) ;
#9807=CARTESIAN_POINT ( 'NONE',  ( 1.681618954495248675, 14.37681556892286672, -0.2945994921972525660 ) ) ;
#9818=CARTESIAN_POINT ( 'NONE',  ( 12.19061143484422693, 20.00510796315846207, 5.223859247015660401 ) ) ;
#9823=CARTESIAN_POINT ( 'NONE',  ( 9.271480332380841460, 14.99039246332198161, 7.037024090030830514 ) ) ;
#9827=CARTESIAN_POINT ( 'NONE',  ( 2.447283566927735521, 20.82590581279646003, 6.632765824531373866 ) ) ;
#9828=CARTESIAN_POINT ( 'NONE',  ( -0.08080654846667670310, 17.19714183529146112, 0.1023781220830352751 ) ) ;
#9831=CARTESIAN_POINT ( 'NONE',  ( 0.1025994048457898045, 15.70581984897159700, 0.7443030867468957146 ) ) ;
#9838=CARTESIAN_POINT ( 'NONE',  ( 13.33071950116100268, 14.65422691944639766, 7.092272786231333725 ) ) ;
#9840=CARTESIAN_POINT ( 'NONE',  ( 9.069792414751740139, 15.30434770100906583, -3.519768623950751962 ) ) ;
#9842=CARTESIAN_POINT ( 'NONE',  ( 8.228154533012041583, 21.18466597396383122, 5.092860201889320315 ) ) ;
#9844=CARTESIAN_POINT ( 'NONE',  ( 2.215916090217208811, 12.53249658949568257, 2.147356924360437347 ) ) ;
#9846=CARTESIAN_POINT ( 'NONE',  ( 6.975053525790806397, 18.43057135737701557, 7.137171834206872845 ) ) ;
#9849=CARTESIAN_POINT ( 'NONE',  ( 7.333616852562694355, 21.20305659848830260, 1.380139826252072544 ) ) ;
#9851=CARTESIAN_POINT ( 'NONE',  ( 4.230681095848447981, 19.07995194538682071, -0.8237946677768968051 ) ) ;
#9855=CARTESIAN_POINT ( 'NONE',  ( 6.622772524087491064, 11.63697146549233175, 2.774099957634049485 ) ) ;
#9865=CARTESIAN_POINT ( 'NONE',  ( 12.97874336893425706, 17.75432315407044115, 6.220344854898855580 ) ) ;
#9869=CARTESIAN_POINT ( 'NONE',  ( 6.345766176488893073, 19.80783775455006435, 6.883578900750740637 ) ) ;
#9880=CARTESIAN_POINT ( 'NONE',  ( 7.421646152376969674, 16.36412484890491115, -2.219134118317299453 ) ) ;
#9881=CARTESIAN_POINT ( 'NONE',  ( 2.323847236009109363, 18.74019614820905844, 0.7500644698246852204 ) ) ;
#9884=CARTESIAN_POINT ( 'NONE',  ( 14.32333359816743545, 21.25787525723532312, 4.225508590508356477 ) ) ;
#9892=CARTESIAN_POINT ( 'NONE',  ( 8.528587150289741459, 20.51903841992993804, 0.2064127866254405752 ) ) ;
#9893=CARTESIAN_POINT ( 'NONE',  ( 9.547366781245800738, 14.64601895156848776, 7.841215834693419318 ) ) ;
#9898=CARTESIAN_POINT ( 'NONE',  ( 4.577338190742489488, 20.54266468784728161, 6.875769498540509339 ) ) ;
#9901=CARTESIAN_POINT ( 'NONE',  ( 7.458443779878670021, 17.00624882743432664, 8.354293789368067991 ) ) ;
#9907=CARTESIAN_POINT ( 'NONE',  ( 0.1909874692627008541, 13.30835273160345800, 2.114876548789060173 ) ) ;
#9911=CARTESIAN_POINT ( 'NONE',  ( 13.54148016078094408, 12.79228088949424169, 5.988512446806296907 ) ) ;
#9917=CARTESIAN_POINT ( 'NONE',  ( 1.664752218687819862, 14.78848634200338452, -0.4464510495472899243 ) ) ;
#9930=CARTESIAN_POINT ( 'NONE',  ( 10.60409020778431000, 11.65180524149912245, 3.905311891646460420 ) ) ;
#9938=CARTESIAN_POINT ( 'NONE',  ( 9.111805414026317607, 13.07579885469743708, 5.988343849954413933 ) ) ;
#9948=CARTESIAN_POINT ( 'NONE',  ( 7.406270976683551055, 12.98268228153804138, 7.410819364758680194 ) ) ;
#9949=CARTESIAN_POINT ( 'NONE',  ( -0.1146841969822216534, 16.89342109921696888, 0.05852849897634891663 ) ) ;
#9952=CARTESIAN_POINT ( 'NONE',  ( -0.01053909864879264136, 20.39392809349225999, 4.740337168719431560 ) ) ;
#9960=CARTESIAN_POINT ( 'NONE',  ( 9.693297870470777511, 21.84389315528099829, 3.625664949012268767 ) ) ;
#9961=CARTESIAN_POINT ( 'NONE',  ( -0.1849527131266449076, 20.23672349358593792, 5.150944217628095068 ) ) ;
#9962=CARTESIAN_POINT ( 'NONE',  ( 9.070785942620656073, 15.46259380661050464, -3.547234420078066996 ) ) ;
#9965=CARTESIAN_POINT ( 'NONE',  ( 7.550459306213158861, 21.69663300857961374, 3.242810284201234960 ) ) ;
#9969=CARTESIAN_POINT ( 'NONE',  ( 6.218012969291997649, 20.30327552937278313, 5.288053756010064888 ) ) ;
#9974=CARTESIAN_POINT ( 'NONE',  ( 9.780308352758851242, 16.60610825764645071, 7.577664015808822207 ) ) ;
#9975=CARTESIAN_POINT ( 'NONE',  ( 5.299730020803123942, 13.73299749091917121, 7.226549125627943937 ) ) ;
#9977=CARTESIAN_POINT ( 'NONE',  ( 6.177406493418641453, 11.65935603284404287, 0.5479154027549586470 ) ) ;
#9982=CARTESIAN_POINT ( 'NONE',  ( 6.643788367457294619, 11.61924653269889163, 2.766513418718104855 ) ) ;
#9992=CARTESIAN_POINT ( 'NONE',  ( 13.13019290195440547, 16.36467473056671196, 6.416790074172170399 ) ) ;
#9996=CARTESIAN_POINT ( 'NONE',  ( 0.8190617032426232846, 18.54739417496245579, 8.495145815602461070 ) ) ;
#10003=CARTESIAN_POINT ( 'NONE',  ( 6.039406833424090237, 11.15496817603752255, 2.913599363317485924 ) ) ;
#10006=CARTESIAN_POINT ( 'NONE',  ( 12.45327340276164740, 19.94235689841700321, 5.081717262054141315 ) ) ;
#10008=CARTESIAN_POINT ( 'NONE',  ( 13.21401102953845275, 14.87494513186989664, 6.308780353949222430 ) ) ;
#10010=CARTESIAN_POINT ( 'NONE',  ( 9.803413267150903110, 10.74905493727258232, 0.2107689867270556017 ) ) ;
#10015=CARTESIAN_POINT ( 'NONE',  ( 8.719136823707652084, 20.76325780187099213, 0.7079147144396957803 ) ) ;
#10016=CARTESIAN_POINT ( 'NONE',  ( 12.50377254232992108, 10.42934933986260049, 2.721148197543237668 ) ) ;
#10021=CARTESIAN_POINT ( 'NONE',  ( 0.7469844135213578040, 20.20533454244034033, 7.893868339785579558 ) ) ;
#10024=CARTESIAN_POINT ( 'NONE',  ( 6.786416855358574196, 20.12019471844387652, 6.853687657227428787 ) ) ;
#10028=CARTESIAN_POINT ( 'NONE',  ( 0.1117406412582209324, 13.80476985362797748, 1.669220243459385022 ) ) ;
#10034=CARTESIAN_POINT ( 'NONE',  ( 6.969492621012407518, 21.59576476661624156, 1.368388097798561631 ) ) ;
#10035=CARTESIAN_POINT ( 'NONE',  ( 4.246403479487743660, 12.12027658721991052, 2.285455345423018869 ) ) ;
#10039=CARTESIAN_POINT ( 'NONE',  ( 1.669125073376063417, 14.66223945716840582, -0.4027805606639273117 ) ) ;
#10047=CARTESIAN_POINT ( 'NONE',  ( 5.593306809071845187, 17.24227063501358614, -1.385594380044606000 ) ) ;
#10048=CARTESIAN_POINT ( 'NONE',  ( -0.6905894489211669152, 20.80806006231328098, 3.719387543999512324 ) ) ;
#10055=CARTESIAN_POINT ( 'NONE',  ( 8.854304133263051213, 12.09810837162069319, 4.755716881274997476 ) ) ;
#10057=CARTESIAN_POINT ( 'NONE',  ( 3.299684148351696322, 17.13945079553905870, 8.374643251542508438 ) ) ;
#10061=CARTESIAN_POINT ( 'NONE',  ( -0.1842567146928706934, 14.65043659803843212, 0.3384235164672123597 ) ) ;
#10063=CARTESIAN_POINT ( 'NONE',  ( 1.691847540349896484, 17.17955240639085801, 8.846950325066879728 ) ) ;
#10069=CARTESIAN_POINT ( 'NONE',  ( 12.05093307044797690, 21.60877823626870153, -1.521190884665024390 ) ) ;
#10071=CARTESIAN_POINT ( 'NONE',  ( 13.30764144135887861, 17.03292647117209668, 7.133305309152374818 ) ) ;
#10076=CARTESIAN_POINT ( 'NONE',  ( 5.975876554808118968, 19.80119422045333621, -0.9882739879990679599 ) ) ;
#10080=CARTESIAN_POINT ( 'NONE',  ( 7.202655614464397615, 17.15635247398953922, 7.564427238666092457 ) ) ;
#10083=CARTESIAN_POINT ( 'NONE',  ( 10.72876945113536706, 10.85891277430018143, 2.065064361200644072 ) ) ;
#10084=CARTESIAN_POINT ( 'NONE',  ( 5.338655627293653616, 14.14790490385028221, 7.478993364272384703 ) ) ;
#10085=CARTESIAN_POINT ( 'NONE',  ( 1.272846674311993720, 18.94235087979956234, 8.991218144746445873 ) ) ;
#10088=CARTESIAN_POINT ( 'NONE',  ( 3.114094397688433880, 12.59169734781732330, 6.492224364648873092 ) ) ;
#10094=CARTESIAN_POINT ( 'NONE',  ( 10.04743712810057765, 21.46699622675163255, 4.316190870212542663 ) ) ;
#10098=CARTESIAN_POINT ( 'NONE',  ( 13.15993927725578949, 14.64227085894461311, 6.133506565519140530 ) ) ;
#10101=CARTESIAN_POINT ( 'NONE',  ( 3.630900445198600668, 12.75273057655540043, 0.9196498124107118644 ) ) ;
#10105=CARTESIAN_POINT ( 'NONE',  ( 3.780468298635305313, 16.45009567437204723, -0.6686140809550422670 ) ) ;
#10106=CARTESIAN_POINT ( 'NONE',  ( 6.107407430018315431, 11.04603590950089043, 2.885280809127467982 ) ) ;
#10109=CARTESIAN_POINT ( 'NONE',  ( 9.098774907988232741, 21.15227197021270200, 1.770799497112857779 ) ) ;
#10110=CARTESIAN_POINT ( 'NONE',  ( 3.956502030732897079, 20.47596928745859302, 4.905481943961070179 ) ) ;
#10111=CARTESIAN_POINT ( 'NONE',  ( 7.855186243077828756, 12.04827940076156167, 0.2502000050339145965 ) ) ;
#10113=CARTESIAN_POINT ( 'NONE',  ( 10.58862850081939300, 21.88976505986162024, 0.07107810111800938468 ) ) ;
#10119=CARTESIAN_POINT ( 'NONE',  ( 10.74361481080007152, 19.05092171070422680, 6.014957688620392595 ) ) ;
#10120=CARTESIAN_POINT ( 'NONE',  ( 10.93842014297040066, 16.27139374001615479, -4.478688491776773972 ) ) ;
#10126=CARTESIAN_POINT ( 'NONE',  ( 11.02468627644401344, 17.30767747894585895, -4.286972664956881118 ) ) ;
#10127=CARTESIAN_POINT ( 'NONE',  ( 1.509340951120249130, 13.07595850747188315, 0.5422609684877979230 ) ) ;
#10130=CARTESIAN_POINT ( 'NONE',  ( 5.852858095612075928, 21.45851731444311383, 4.363222383076143629 ) ) ;
#10138=CARTESIAN_POINT ( 'NONE',  ( 1.693150899634930040, 14.15944726460652348, -0.2048692773969919834 ) ) ;
#10149=CARTESIAN_POINT ( 'NONE',  ( 5.881368144132508746, 18.80106227311165767, -0.8182108359018045451 ) ) ;
#10156=CARTESIAN_POINT ( 'NONE',  ( 8.943100994816060023, 12.35671964186176197, 5.167251557440379450 ) ) ;
#10163=CARTESIAN_POINT ( 'NONE',  ( 0.1527221624363179764, 18.60604061194695547, 0.5457984701511658931 ) ) ;
#10167=CARTESIAN_POINT ( 'NONE',  ( 4.673487404147415702, 11.78541955647214046, 3.777201821681576810 ) ) ;
#10173=CARTESIAN_POINT ( 'NONE',  ( 8.744384562554335716, 11.57391542797248007, 5.551989790062823005 ) ) ;
#10176=CARTESIAN_POINT ( 'NONE',  ( 10.68696473053424967, 21.82883031116149297, 0.2667890350525887744 ) ) ;
#10178=CARTESIAN_POINT ( 'NONE',  ( 9.350008301323910587, 12.97765481918709085, 6.896721531191268184 ) ) ;
#10179=CARTESIAN_POINT ( 'NONE',  ( 7.309199775707146074, 16.58792154420486042, 7.713755225109836466 ) ) ;
#10182=CARTESIAN_POINT ( 'NONE',  ( 0.8373503019344407106, 19.61574039456632690, 2.335197277426223739 ) ) ;
#10184=CARTESIAN_POINT ( 'NONE',  ( 7.733788100231727469, 14.51543401643281150, -2.412536282348112238 ) ) ;
#10187=CARTESIAN_POINT ( 'NONE',  ( 7.367229612691850171, 18.51696245222963455, 8.037950014293697265 ) ) ;
#10191=CARTESIAN_POINT ( 'NONE',  ( 2.347314355769781091, 20.09598732912352403, 6.298940065843233072 ) ) ;
#10198=CARTESIAN_POINT ( 'NONE',  ( 11.12927268506130929, 13.52938648361508100, 5.972454599576855649 ) ) ;
#10199=CARTESIAN_POINT ( 'NONE',  ( 10.64684779959870298, 20.38904377012663716, 5.920590089696055713 ) ) ;
#10202=CARTESIAN_POINT ( 'NONE',  ( 12.53365458789522080, 11.46648469212541244, 3.032982017095954941 ) ) ;
#10204=CARTESIAN_POINT ( 'NONE',  ( 4.921664833983353304, 12.88680353640996223, 6.808023123837544155 ) ) ;
#10211=CARTESIAN_POINT ( 'NONE',  ( 6.113655373600792586, 11.03939097578738071, 2.882924309803769347 ) ) ;
#10214=CARTESIAN_POINT ( 'NONE',  ( 11.11537376329170179, 14.44107328295670634, -3.331267459799296837 ) ) ;
#10216=CARTESIAN_POINT ( 'NONE',  ( 10.13616474230335740, 20.26417264612534197, -1.207278885743884089 ) ) ;
#10217=CARTESIAN_POINT ( 'NONE',  ( 2.299349580604229448, 13.27625335140768215, 0.5631475405237129639 ) ) ;
#10219=CARTESIAN_POINT ( 'NONE',  ( 14.00687195125745887, 21.64281653910636294, 3.694034086410758366 ) ) ;
#10223=CARTESIAN_POINT ( 'NONE',  ( 10.70179625483013730, 19.19642187053233329, 5.916294423283699366 ) ) ;
#10224=CARTESIAN_POINT ( 'NONE',  ( 14.05130128282920232, 21.64220180175570363, 3.680409539941097208 ) ) ;
#10228=CARTESIAN_POINT ( 'NONE',  ( 12.85510060975789060, 22.16293208523041258, 0.4350888124966122428 ) ) ;
#10230=CARTESIAN_POINT ( 'NONE',  ( 5.159230185404290125, 17.48971098885959918, 8.784928378633825474 ) ) ;
#10233=CARTESIAN_POINT ( 'NONE',  ( 7.245977530762245600, 18.46665735122999052, 7.961998677432508664 ) ) ;
#10239=CARTESIAN_POINT ( 'NONE',  ( 2.042440755766480098, 13.25699772772027529, 1.354434111151779474 ) ) ;
#10241=CARTESIAN_POINT ( 'NONE',  ( 3.828036625945912874, 13.64012675898730187, 0.2356414614424844622 ) ) ;
#10246=CARTESIAN_POINT ( 'NONE',  ( 1.666440852445509879, 15.73961440154546310, -0.6526140317216138076 ) ) ;
#10254=VERTEX_POINT ( 'NONE', #17558 ) ;
#10256=CARTESIAN_POINT ( 'NONE',  ( 5.720661490769825441, 12.70293317459338134, 0.2232859597839690347 ) ) ;
#10257=CARTESIAN_POINT ( 'NONE',  ( 7.159729259274372204, 11.65952799072720047, 5.998687542543657436 ) ) ;
#10265=CARTESIAN_POINT ( 'NONE',  ( 7.468644793988906905, 14.27831657605653604, -1.663655224044803926 ) ) ;
#10272=CARTESIAN_POINT ( 'NONE',  ( -0.1334278631421785821, 13.87292853438413687, 0.7019017698175864517 ) ) ;
#10275=CARTESIAN_POINT ( 'NONE',  ( 3.141552985354155059, 11.94763405986570071, 5.008148756522596834 ) ) ;
#10281=CARTESIAN_POINT ( 'NONE',  ( 12.74908984681135138, 22.29005399844394120, 0.4156185081117323432 ) ) ;
#10283=CARTESIAN_POINT ( 'NONE',  ( 10.74838682008468638, 21.87703791083306371, 0.4363949013415037159 ) ) ;
#10289=CARTESIAN_POINT ( 'NONE',  ( 9.073022245511658923, 11.70236418326780203, 5.603503291933394692 ) ) ;
#10290=CARTESIAN_POINT ( 'NONE',  ( 5.642955815196034841, 20.83420574847494322, 3.727832798710557505 ) ) ;
#10294=CARTESIAN_POINT ( 'NONE',  ( 7.300217370997200028, 16.06868654239796257, 7.623995498661889414 ) ) ;
#10296=CARTESIAN_POINT ( 'NONE',  ( 1.860637697812923763, 20.38936078815874353, 4.959448130920145026 ) ) ;
#10300=CARTESIAN_POINT ( 'NONE',  ( 13.11534328330504451, 11.87357545845056173, 4.170984102655784120 ) ) ;
#10303=CARTESIAN_POINT ( 'NONE',  ( 1.458975506666385424, 12.54422677008150089, 8.034613268192803304 ) ) ;
#10308=CARTESIAN_POINT ( 'NONE',  ( -0.3331096548604842722, 20.30753595452681992, 4.844414039309315356 ) ) ;
#10314=CARTESIAN_POINT ( 'NONE',  ( 11.42390536508826138, 16.05844251236355191, 7.572047171115840136 ) ) ;
#10316=CARTESIAN_POINT ( 'NONE',  ( 11.16572056210525865, 14.41814247312392183, -3.213472714937148478 ) ) ;
#10318=CARTESIAN_POINT ( 'NONE',  ( 4.249450599936705153, 19.94879251081626137, 6.535985519458143322 ) ) ;
#10325=CARTESIAN_POINT ( 'NONE',  ( 6.273626380189087470, 10.93980219448746283, 2.827745728986147178 ) ) ;
#10330=CARTESIAN_POINT ( 'NONE',  ( 9.886766943894276238, 11.51584134576680363, 0.4567744769608155231 ) ) ;
#10332=CARTESIAN_POINT ( 'NONE',  ( 3.634673147523096226, 20.58079426707816850, 4.062413416603754435 ) ) ;
#10333=CARTESIAN_POINT ( 'NONE',  ( 12.88900610377207734, 21.48306739246610420, 0.4890693659201348908 ) ) ;
#10334=CARTESIAN_POINT ( 'NONE',  ( 6.344447095476780873, 11.93061510394686131, 0.6566749515117876745 ) ) ;
#10335=CARTESIAN_POINT ( 'NONE',  ( 5.382695099851752651, 13.59057812530450171, -1.531598659755918135 ) ) ;
#10342=CARTESIAN_POINT ( 'NONE',  ( 10.80126525386333824, 10.89862672135422095, 4.169966205966027850 ) ) ;
#10347=CARTESIAN_POINT ( 'NONE',  ( 0.4653477503899910994, 11.40353646073516103, 4.946780524725718386 ) ) ;
#10350=CARTESIAN_POINT ( 'NONE',  ( 6.777766060880455967, 11.08767916761746086, 4.480892634214041159 ) ) ;
#10356=CARTESIAN_POINT ( 'NONE',  ( 0.3974967306201093176, 12.59494073688686555, 3.148956390786026294 ) ) ;
#10359=ORIENTED_EDGE ( 'NONE', *, *, #5736, .T. ) ;
#10360=CARTESIAN_POINT ( 'NONE',  ( 3.962427028851731148, 12.89365793399433180, 0.9426411514076304954 ) ) ;
#10365=CARTESIAN_POINT ( 'NONE',  ( 3.414047624806694436, 21.33360473058343842, 3.465166473578813466 ) ) ;
#10376=CARTESIAN_POINT ( 'NONE',  ( 9.814576312521648305, 11.51990282145384015, 0.4798283062359162687 ) ) ;
#10377=CARTESIAN_POINT ( 'NONE',  ( 0.3991529941856173380, 11.62559268301756177, 3.149969643310115419 ) ) ;
#10380=CARTESIAN_POINT ( 'NONE',  ( 5.589289644602882134, 14.56010236266069136, 8.502823875585745483 ) ) ;
#10387=CARTESIAN_POINT ( 'NONE',  ( 7.457877451773216926, 16.00203316895927586, -2.111994508504527968 ) ) ;
#10393=CARTESIAN_POINT ( 'NONE',  ( 1.014578268522615012, 20.76321888266333104, 2.702579939252432784 ) ) ;
#10396=CARTESIAN_POINT ( 'NONE',  ( 4.199552796348193340, 18.69182423982057273, -0.1726145848212380651 ) ) ;
#10402=CARTESIAN_POINT ( 'NONE',  ( 5.378103913977471784, 12.14871438356658295, -0.1654852939330033190 ) ) ;
#10404=CARTESIAN_POINT ( 'NONE',  ( 13.39275425437221401, 15.07885496629254440, 7.046569758826037422 ) ) ;
#10411=CARTESIAN_POINT ( 'NONE',  ( 9.037210512593977896, 11.60002287198769189, 5.445748904208223884 ) ) ;
#10412=CARTESIAN_POINT ( 'NONE',  ( 3.728962736874319006, 15.57283695825947412, -0.6908591606584689737 ) ) ;
#10414=CARTESIAN_POINT ( 'NONE',  ( 5.706220423065773595, 17.18812784857371767, -1.328853644864197658 ) ) ;
#10417=CARTESIAN_POINT ( 'NONE',  ( 9.747861764205893564, 16.62671289803297370, 7.918352333577308499 ) ) ;
#10418=CARTESIAN_POINT ( 'NONE',  ( 5.132107606870269123, 12.79243504847817547, 6.338296502348789829 ) ) ;
#10420=CARTESIAN_POINT ( 'NONE',  ( 5.244116213687740391, 19.21739139815786146, 8.049907794713583087 ) ) ;
#10423=CARTESIAN_POINT ( 'NONE',  ( 0.6723359852304844342, 19.54979116365418079, 7.412813188025597633 ) ) ;
#10427=CARTESIAN_POINT ( 'NONE',  ( 11.10489018155983310, 18.77048838114807694, 7.052920197992054163 ) ) ;
#10431=CARTESIAN_POINT ( 'NONE',  ( 11.24411629099876109, 17.10760633503948824, -3.541267089923193279 ) ) ;
#10434=CARTESIAN_POINT ( 'NONE',  ( 4.683303992135119387, 18.80848272075206040, 7.590210397258200459 ) ) ;
#10439=CARTESIAN_POINT ( 'NONE',  ( 0.1129727359843346046, 20.94457815707821169, 5.061725698818384522 ) ) ;
#10441=CARTESIAN_POINT ( 'NONE',  ( 6.359934862478964668, 11.71523234649916212, 2.858519856524831315 ) ) ;
#10443=CARTESIAN_POINT ( 'NONE',  ( 11.18095383545338528, 17.51254433608867700, 6.751878116475301006 ) ) ;
#10444=CARTESIAN_POINT ( 'NONE',  ( 14.12523555123927999, 20.59139265233172367, 3.828121585696277140 ) ) ;
#10445=CARTESIAN_POINT ( 'NONE',  ( 1.119724371970266974, 20.13149037663900387, 7.725538715806275825 ) ) ;
#10446=CARTESIAN_POINT ( 'NONE',  ( 8.603371928060651541, 10.74414689430484238, 3.699663666938896256 ) ) ;
#10452=CARTESIAN_POINT ( 'NONE',  ( 11.19102542510228382, 12.02330533696836135, 5.866022334646728176 ) ) ;
#10455=CARTESIAN_POINT ( 'NONE',  ( 10.30239665667997251, 11.37017134450840139, 2.174391373805977690 ) ) ;
#10459=CARTESIAN_POINT ( 'NONE',  ( 6.954974101898393712, 18.47894807998623534, 8.074325918837109484 ) ) ;
#10481=CARTESIAN_POINT ( 'NONE',  ( 12.37983225623493411, 19.93927778675710272, 5.100595263939720958 ) ) ;
#10482=CARTESIAN_POINT ( 'NONE',  ( -0.6995384825569825882, 20.80871142581116118, 3.721840415571334049 ) ) ;
#10485=CARTESIAN_POINT ( 'NONE',  ( 4.551862264357088961, 11.07955752190297183, 3.668119238956743633 ) ) ;
#10490=CARTESIAN_POINT ( 'NONE',  ( 7.545096913039198938, 17.11720444957493825, -2.078483839830497004 ) ) ;
#10497=CARTESIAN_POINT ( 'NONE',  ( 0.8685919227001404064, 20.56010016465687684, 2.317533322938851281 ) ) ;
#10502=CARTESIAN_POINT ( 'NONE',  ( 1.698299366653992282, 20.72409300549792022, 3.290495829865351940 ) ) ;
#10507=CARTESIAN_POINT ( 'NONE',  ( 10.32489209301978583, 21.80709644552430149, 0.1772959725815080045 ) ) ;
#10509=CARTESIAN_POINT ( 'NONE',  ( 12.18859454906908546, 21.32141368478257348, 4.415751409964100205 ) ) ;
#10512=CARTESIAN_POINT ( 'NONE',  ( 9.486764370443642846, 15.75061937992353123, 7.955153629647191416 ) ) ;
#10513=CARTESIAN_POINT ( 'NONE',  ( 3.846219661981610471, 17.18860055147588994, -0.6938403426090347104 ) ) ;
#10515=CARTESIAN_POINT ( 'NONE',  ( 5.782398285543762562, 12.98564521233307190, 0.02530286594647560006 ) ) ;
#10516=CARTESIAN_POINT ( 'NONE',  ( 1.315381686729747646, 20.24764554913870995, 3.544931371820004173 ) ) ;
#10518=CARTESIAN_POINT ( 'NONE',  ( 8.168165464054217395, 20.04452402401122058, -1.696596079913171851 ) ) ;
#10521=CARTESIAN_POINT ( 'NONE',  ( 6.940486874547567631, 20.09752422452572418, 7.007469641995731635 ) ) ;
#10522=CARTESIAN_POINT ( 'NONE',  ( 1.255123740014034706, 18.92571547447176172, 8.878479688366162748 ) ) ;
#10525=CARTESIAN_POINT ( 'NONE',  ( 1.297850727783172786, 13.15556036664986195, 7.528907847599255909 ) ) ;
#10532=CARTESIAN_POINT ( 'NONE',  ( 9.221657793164913741, 21.87308296202409963, 2.042460036653409805 ) ) ;
#10534=CARTESIAN_POINT ( 'NONE',  ( 11.34677053555899029, 17.89547928321977466, -3.372900898699195071 ) ) ;
#10536=CARTESIAN_POINT ( 'NONE',  ( 6.384643824615721996, 11.62550227300026151, 4.197152387170460131 ) ) ;
#10540=CARTESIAN_POINT ( 'NONE',  ( 4.351297120991392653, 19.36269373579626674, 0.4388914768103922559 ) ) ;
#10544=CARTESIAN_POINT ( 'NONE',  ( 9.995376944861977364, 11.51990282145384015, 0.4256848013639417672 ) ) ;
#10545=CARTESIAN_POINT ( 'NONE',  ( 9.360757232110890058, 13.73189003748300685, -2.250780131576506360 ) ) ;
#10546=CARTESIAN_POINT ( 'NONE',  ( 6.054335174399104957, 21.23839086782724195, 3.633263926537354749 ) ) ;
#10552=PRODUCT_DEFINITION_CONTEXT ( 'detailed design', #6216, 'design' ) ;
#10555=CARTESIAN_POINT ( 'NONE',  ( 12.15973251502179231, 21.60500416633145804, -1.551647953943186886 ) ) ;
#10558=CARTESIAN_POINT ( 'NONE',  ( 9.842819086504725590, 11.73374667394938164, 0.1685169991754134899 ) ) ;
#10561=CARTESIAN_POINT ( 'NONE',  ( 13.12625987927192739, 22.21723794295526488, 1.191615484091907762 ) ) ;
#10562=CARTESIAN_POINT ( 'NONE',  ( -0.3645692649321460310, 17.35729252269350553, 0.2027727071106186774 ) ) ;
#10565=CARTESIAN_POINT ( 'NONE',  ( 7.400268487603801404, 13.00719617420639551, 7.282345073165821248 ) ) ;
#10571=CARTESIAN_POINT ( 'NONE',  ( 0.04787801191089360864, 14.49629642778351268, 1.235535862485549030 ) ) ;
#10591=CARTESIAN_POINT ( 'NONE',  ( 13.83162162704461373, 20.92405235932746166, 3.372942155665883401 ) ) ;
#10592=CARTESIAN_POINT ( 'NONE',  ( 5.012423084987765343, 21.41828792979770313, 1.984503165450502538 ) ) ;
#10595=CARTESIAN_POINT ( 'NONE',  ( 5.430225438562612972, 12.90007726256580689, 7.561889016175808109 ) ) ;
#10601=CARTESIAN_POINT ( 'NONE',  ( 7.842133636678705777, 12.16369228495859645, 0.2595828833526279689 ) ) ;
#10610=CARTESIAN_POINT ( 'NONE',  ( 1.814948966250774065, 21.19546389864396119, 4.850479613994575168 ) ) ;
#10615=CARTESIAN_POINT ( 'NONE',  ( 13.05845502804394798, 21.54598149573345367, 1.959600843863859243 ) ) ;
#10619=CARTESIAN_POINT ( 'NONE',  ( 13.26602609393551369, 22.11716190621255862, 2.502407145256026588 ) ) ;
#10622=CARTESIAN_POINT ( 'NONE',  ( 11.53730135053356776, 11.04591141993689263, -1.177169684089045765 ) ) ;
#10626=CARTESIAN_POINT ( 'NONE',  ( 7.496787083349086167, 18.49057725868834723, -2.494173209474321862 ) ) ;
#10627=CARTESIAN_POINT ( 'NONE',  ( 3.425778229864998359, 16.48230391985759979, 8.522309372965072072 ) ) ;
#10630=CARTESIAN_POINT ( 'NONE',  ( 5.732870978699193820, 17.39963396565737952, -1.291407831173700282 ) ) ;
#10635=CARTESIAN_POINT ( 'NONE',  ( 5.777562495344723992, 17.39297272447799614, -2.183326841469702906 ) ) ;
#10636=CARTESIAN_POINT ( 'NONE',  ( 4.689920459349973036, 11.91097906394028172, 4.285078460903785746 ) ) ;
#10638=CARTESIAN_POINT ( 'NONE',  ( 13.45333066700820979, 21.38713583945818542, 1.818036823379868938 ) ) ;
#10639=CARTESIAN_POINT ( 'NONE',  ( 0.6492888148354383215, 20.32382785537196312, 1.812354305104474150 ) ) ;
#10640=CARTESIAN_POINT ( 'NONE',  ( 0.2710380737689748187, 20.85778803320007313, 6.370138859128364750 ) ) ;
#10642=CARTESIAN_POINT ( 'NONE',  ( 7.264882008937790125, 16.58796963715414208, 7.727752318332806958 ) ) ;
#10649=CARTESIAN_POINT ( 'NONE',  ( 11.27183014273422401, 12.74897102812991179, 6.369117077617454825 ) ) ;
#10650=EDGE_LOOP ( 'NONE', ( #13491, #2936, #8680, #11352 ) ) ;
#10653=CARTESIAN_POINT ( 'NONE',  ( 11.79451413562702911, 11.46334091281098111, -0.1568912284302553251 ) ) ;
#10655=CARTESIAN_POINT ( 'NONE',  ( -0.07820122749697261400, 15.70581984897159700, 0.7984465916195991886 ) ) ;
#10659=CARTESIAN_POINT ( 'NONE',  ( 4.932957014358739123, 20.42853515389766272, 1.908948791967717273 ) ) ;
#10666=CARTESIAN_POINT ( 'NONE',  ( 12.97628609860860394, 18.46234326053249220, 6.039901028563929408 ) ) ;
#10667=CARTESIAN_POINT ( 'NONE',  ( 5.709010112337018938, 17.24330370537085955, -1.425333744364522648 ) ) ;
#10675=CARTESIAN_POINT ( 'NONE',  ( 11.20683540457644334, 15.87299087032793743, 6.798486701180226355 ) ) ;
#10676=CARTESIAN_POINT ( 'NONE',  ( 12.65066698874035112, 20.52417811251926238, 5.611220316870539904 ) ) ;
#10681=CARTESIAN_POINT ( 'NONE',  ( 10.51247066191329083, 11.49109188741821264, 3.088008306483761789 ) ) ;
#10684=CARTESIAN_POINT ( 'NONE',  ( 1.717996366984696488, 12.18301083390420203, 2.082593322157058946 ) ) ;
#10708=CARTESIAN_POINT ( 'NONE',  ( 1.686968993106074510, 16.44735884859098718, -0.8025552312217851814 ) ) ;
#10711=CARTESIAN_POINT ( 'NONE',  ( 4.997041246908954015, 11.45262702614296302, 5.581120543604684237 ) ) ;
#10720=CARTESIAN_POINT ( 'NONE',  ( 3.139362194088404667, 12.70870594642470230, 6.498606875045355835 ) ) ;
#10725=CARTESIAN_POINT ( 'NONE',  ( 3.564885292549716311, 16.92788500666243223, 9.175419982453322021 ) ) ;
#10727=CARTESIAN_POINT ( 'NONE',  ( 4.318272399054353450, 20.61711312421807918, 4.992195515787562599 ) ) ;
#10729=CARTESIAN_POINT ( 'NONE',  ( 13.39756118469465029, 22.16307784260286340, 1.948616576935187750 ) ) ;
#10735=CARTESIAN_POINT ( 'NONE',  ( 8.812473556068928460, 13.52835235745250131, -2.451387110162866367 ) ) ;
#10737=CARTESIAN_POINT ( 'NONE',  ( 13.02604791969851661, 11.75039870752145177, 5.077274524504193032 ) ) ;
#10741=CARTESIAN_POINT ( 'NONE',  ( 7.877529856632134120, 20.02306472266900172, -1.583040783571615151 ) ) ;
#10745=CARTESIAN_POINT ( 'NONE',  ( 5.592841715996570429, 15.66352912673956865, -1.341337588800156411 ) ) ;
#10748=CARTESIAN_POINT ( 'NONE',  ( 9.452961308647887861, 13.36844392990906272, -2.929793466363328491 ) ) ;
#10752=CARTESIAN_POINT ( 'NONE',  ( 1.700980557147387717, 15.58904521221044170, 9.664144641518724654 ) ) ;
#10753=CARTESIAN_POINT ( 'NONE',  ( 0.2748101640027249548, 20.85481667080186341, 6.380173850233394006 ) ) ;
#10754=CARTESIAN_POINT ( 'NONE',  ( 0.7950072837654299507, 19.66973114709098169, 2.266613654961380675 ) ) ;
#10764=CARTESIAN_POINT ( 'NONE',  ( 9.798027642257455483, 10.93122598874641049, 0.05745448286648872915 ) ) ;
#10767=CARTESIAN_POINT ( 'NONE',  ( 11.14545677980454208, 15.43789734212750808, -3.509883341676725443 ) ) ;
#10768=CARTESIAN_POINT ( 'NONE',  ( 5.541718124298840031, 12.84840258351819209, -0.8988864716115243514 ) ) ;
#10770=CARTESIAN_POINT ( 'NONE',  ( 3.307247859361858389, 16.48205525895870593, 8.552608352040381945 ) ) ;
#10776=CARTESIAN_POINT ( 'NONE',  ( 8.115118250563648772, 19.55588805595618140, -1.118609513322449622 ) ) ;
#10777=CARTESIAN_POINT ( 'NONE',  ( 13.54495441322193372, 21.41280428856536489, 2.252596376362126396 ) ) ;
#10785=CARTESIAN_POINT ( 'NONE',  ( 11.20894518263242112, 14.54054042788871648, 6.496243861428408373 ) ) ;
#10786=CARTESIAN_POINT ( 'NONE',  ( 11.43530489704916420, 13.68296282620402238, 7.076276842477176032 ) ) ;
#10789=CARTESIAN_POINT ( 'NONE',  ( 9.293274126941451385, 15.02556043177791878, -2.679682145362060730 ) ) ;
#10792=CARTESIAN_POINT ( 'NONE',  ( 3.588507411891436405, 18.91035477026892409, -0.3510181181459797739 ) ) ;
#10795=CARTESIAN_POINT ( 'NONE',  ( 7.115159381822890872, 11.75569977924905274, 5.947017350195187291 ) ) ;
#10804=CARTESIAN_POINT ( 'NONE',  ( 11.58758032897313761, 10.98269117049956201, -1.359133207363109941 ) ) ;
#10814=CARTESIAN_POINT ( 'NONE',  ( 1.657404189593110644, 14.62646646242487769, -0.5067450003820986870 ) ) ;
#10817=CARTESIAN_POINT ( 'NONE',  ( 5.489998326203298973, 17.16039541831715454, 8.734701079443423666 ) ) ;
#10821=CARTESIAN_POINT ( 'NONE',  ( 3.067686375243920072, 12.50340986505852747, 6.152773509231688642 ) ) ;
#10825=CARTESIAN_POINT ( 'NONE',  ( 1.765172365516369579, 21.20083304101597221, 4.716146812010884481 ) ) ;
#10828=CARTESIAN_POINT ( 'NONE',  ( 3.751596593617982478, 20.73071249212684108, 3.494438650925056233 ) ) ;
#10835=CARTESIAN_POINT ( 'NONE',  ( 5.656518577322932728, 11.49185006667808118, 1.607793118288020962 ) ) ;
#10839=CARTESIAN_POINT ( 'NONE',  ( 13.23440871943589237, 12.81420739021140598, 6.047183941140541030 ) ) ;
#10843=CARTESIAN_POINT ( 'NONE',  ( 7.308308794374226203, 17.13478947702074251, -2.844519879704227705 ) ) ;
#10846=CARTESIAN_POINT ( 'NONE',  ( 5.656977408468667257, 13.81142017241615605, -0.6512533121070646080 ) ) ;
#10850=CARTESIAN_POINT ( 'NONE',  ( 13.72939367483574280, 14.76516699303951619, 6.561508169267058932 ) ) ;
#10851=CARTESIAN_POINT ( 'NONE',  ( 3.524129415282716060, 13.11356558266398231, 8.223647746374714629 ) ) ;
#10857=CARTESIAN_POINT ( 'NONE',  ( 2.356114889612781482, 20.09535866699502193, 6.295991311034685012 ) ) ;
#10864=CARTESIAN_POINT ( 'NONE',  ( 11.43263507844261007, 14.55322455989931107, 7.303294973855595451 ) ) ;
#10867=CARTESIAN_POINT ( 'NONE',  ( 11.42389331219130177, 18.34427701479485506, -3.218461924845117395 ) ) ;
#10868=CARTESIAN_POINT ( 'NONE',  ( 5.376858612653267144, 15.95884149645304007, -2.144506965101294682 ) ) ;
#10871=CARTESIAN_POINT ( 'NONE',  ( 5.623588726797621895, 20.73702223218877094, 3.727985457070243314 ) ) ;
#10876=CARTESIAN_POINT ( 'NONE',  ( 5.654395174991643458, 15.56639808041640372, -1.444955789142327029 ) ) ;
#10877=CARTESIAN_POINT ( 'NONE',  ( 11.23643128109388201, 14.04470801367943267, 6.379844766020851488 ) ) ;
#10881=CARTESIAN_POINT ( 'NONE',  ( 4.065274381575306961, 21.20935756750483137, 5.231433629464312673 ) ) ;
#10883=SHAPE_REPRESENTATION ( 'Locking Pawl Compression Spring', ( #2234 ), #652 ) ;
#10886=CARTESIAN_POINT ( 'NONE',  ( 9.280893739159276734, 12.85627548497952155, 6.982956407158277479 ) ) ;
#10889=CARTESIAN_POINT ( 'NONE',  ( 9.808641443463722354, 11.80443358965426270, 0.01604935767821101880 ) ) ;
#10891=CARTESIAN_POINT ( 'NONE',  ( 1.181662039134980802, 18.03831543248292846, 8.489857044810902309 ) ) ;
#10892=CARTESIAN_POINT ( 'NONE',  ( 4.597652426504708068, 21.03084409073214189, 2.229734299069735748 ) ) ;
#10901=CARTESIAN_POINT ( 'NONE',  ( 0.02681165389613587163, 15.20991100934055851, 0.9596687688324064824 ) ) ;
#10908=CARTESIAN_POINT ( 'NONE',  ( 10.06470537354537242, 20.90551644660764197, -1.710021108312257176 ) ) ;
#10919=CARTESIAN_POINT ( 'NONE',  ( 5.658689206670286964, 21.64257598718208442, 3.780371088097784771 ) ) ;
#10922=CARTESIAN_POINT ( 'NONE',  ( 3.524570301996365007, 14.53812262783368148, -1.106616872351161796 ) ) ;
#10932=CARTESIAN_POINT ( 'NONE',  ( 2.744809781688229311, 11.26550662193089991, 4.638685792162725363 ) ) ;
#10938=CARTESIAN_POINT ( 'NONE',  ( 9.886113621169860366, 10.85891277430018143, 2.317410492099426289 ) ) ;
#10942=CARTESIAN_POINT ( 'NONE',  ( 11.93614680372799164, 10.48196076179804237, 0.4944231461740059563 ) ) ;
#10946=CARTESIAN_POINT ( 'NONE',  ( 7.422254420035173439, 12.63626090060510165, -1.507133129890835477 ) ) ;
#10951=CARTESIAN_POINT ( 'NONE',  ( 7.677630431870579031, 20.85973498604326082, 3.570432132007519410 ) ) ;
#10952=CARTESIAN_POINT ( 'NONE',  ( 7.313927782523842680, 14.57437388699512049, 7.297072825503160942 ) ) ;
#10954=CARTESIAN_POINT ( 'NONE',  ( 2.405822869029970335, 19.95883502769006768, 6.363079012132137890 ) ) ;
#10958=CARTESIAN_POINT ( 'NONE',  ( 5.749403582042253547, 12.07884102837326168, -0.3386244590164438351 ) ) ;
#10961=CARTESIAN_POINT ( 'NONE',  ( -0.9269672813091816010, 20.56277232864792026, 3.255889307845898806 ) ) ;
#10962=CARTESIAN_POINT ( 'NONE',  ( 0.3520923380729273355, 20.79332306228696226, 6.585738808535214872 ) ) ;
#10965=CARTESIAN_POINT ( 'NONE',  ( 2.898989268417691889, 20.19932627889173915, 2.190770615898228968 ) ) ;
#10971=CARTESIAN_POINT ( 'NONE',  ( 10.99108388080240850, 11.53754468935924216, 5.084071353150248385 ) ) ;
#10976=CARTESIAN_POINT ( 'NONE',  ( 5.387739448560934896, 14.30193700830310277, -1.760619005860999398 ) ) ;
#10984=CARTESIAN_POINT ( 'NONE',  ( 11.23558539073912499, 16.27078549497860394, -3.718151546694987708 ) ) ;
#10986=CARTESIAN_POINT ( 'NONE',  ( 11.33660541269852295, 21.35754284105190237, 1.979928130275292020 ) ) ;
#10992=CARTESIAN_POINT ( 'NONE',  ( 4.104248940463866013, 21.17924991814257396, 5.336610038632097819 ) ) ;
#10999=CARTESIAN_POINT ( 'NONE',  ( 10.66809636617878532, 20.98977402726757902, 0.2570665557559146386 ) ) ;
#11002=CARTESIAN_POINT ( 'NONE',  ( 1.191453932260699400, 15.64505045901557345, 9.398635499751998523 ) ) ;
#11031=AXIS2_PLACEMENT_3D ( 'NONE', #9435, #3133, #1032 ) ;
#11032=CARTESIAN_POINT ( 'NONE',  ( 3.559759918315169358, 13.11356558266398231, 8.212977649209914688 ) ) ;
#11035=CARTESIAN_POINT ( 'NONE',  ( 3.568439739289405388, 16.69396391803602953, -1.421120065001460153 ) ) ;
#11040=CARTESIAN_POINT ( 'NONE',  ( 3.133115509155857570, 12.68908857082841735, 6.468163464435182419 ) ) ;
#11047=CARTESIAN_POINT ( 'NONE',  ( 3.649632197277235424, 15.51727318038290626, 9.145577215261649684 ) ) ;
#11057=CARTESIAN_POINT ( 'NONE',  ( 6.326270045413027177, 11.43880029099476126, 4.501843889239982133 ) ) ;
#11060=CARTESIAN_POINT ( 'NONE',  ( 13.34474349389573966, 13.82947554229071585, 6.637995438756325584 ) ) ;
#11064=CARTESIAN_POINT ( 'NONE',  ( 7.899748338964175609, 11.10891229026089988, 0.6199817720100504470 ) ) ;
#11066=CARTESIAN_POINT ( 'NONE',  ( 1.994785678335496026, 13.53119643653954363, 0.9820674903561780189 ) ) ;
#11067=CARTESIAN_POINT ( 'NONE',  ( 7.505597285291182530, 20.91029632882624156, 3.112204859505360410 ) ) ;
#11068=CARTESIAN_POINT ( 'NONE',  ( 7.235830445973447489, 13.61491138090174680, 6.770065179283416334 ) ) ;
#11069=CARTESIAN_POINT ( 'NONE',  ( 2.011838081192605987, 20.33402069578789551, 5.352005239497477085 ) ) ;
#11073=CARTESIAN_POINT ( 'NONE',  ( 8.251602663485694933, 10.68384337266676276, 1.704364278152144196 ) ) ;
#11076=CARTESIAN_POINT ( 'NONE',  ( 0.1889641725767322034, 19.02238102577908307, 0.6697343601325994600 ) ) ;
#11077=CARTESIAN_POINT ( 'NONE',  ( 1.640147784336999592, 16.65909851697077571, 9.606380118624771924 ) ) ;
#11080=CARTESIAN_POINT ( 'NONE',  ( 5.376211239829841837, 15.73786965665290793, 8.095709214974558421 ) ) ;
#11087=CARTESIAN_POINT ( 'NONE',  ( 10.81776401011329547, 11.10301140953592203, 4.334198581180471521 ) ) ;
#11091=CARTESIAN_POINT ( 'NONE',  ( 12.16036747447985711, 20.61529458018329564, -1.409506725801037419 ) ) ;
#11092=CARTESIAN_POINT ( 'NONE',  ( 5.483538033079329743, 13.23206236587151707, -1.192467485947962036 ) ) ;
#11094=CARTESIAN_POINT ( 'NONE',  ( 1.113804815293770289, 18.49964734577863368, 8.330481410010762033 ) ) ;
#11098=CARTESIAN_POINT ( 'NONE',  ( 7.134758565295798327, 11.94621801824261986, 4.715951947576552783 ) ) ;
#11103=CARTESIAN_POINT ( 'NONE',  ( 3.697979674205963185, 21.37068642827637888, 4.236069647309165020 ) ) ;
#11112=CARTESIAN_POINT ( 'NONE',  ( 11.36271039377850300, 21.23937884529802389, 2.129853413371744164 ) ) ;
#11113=CARTESIAN_POINT ( 'NONE',  ( 1.467157081727171297, 15.86225324810530068, 8.827709964917746177 ) ) ;
#11115=CARTESIAN_POINT ( 'NONE',  ( 1.328448286825129943, 14.75527451915623267, -0.007290130677178787572 ) ) ;
#11125=CARTESIAN_POINT ( 'NONE',  ( 10.09152440736383483, 20.26472116815758184, -1.194358939805918896 ) ) ;
#11128=CARTESIAN_POINT ( 'NONE',  ( 7.185023862866797728, 14.38088390058819144, -2.647084244243658624 ) ) ;
#11140=CARTESIAN_POINT ( 'NONE',  ( 5.642613892620969018, 15.64107961637180289, 8.855653260751193301 ) ) ;
#11143=CARTESIAN_POINT ( 'NONE',  ( 4.143869576618084416, 19.77995523304069181, -0.2166999831453354231 ) ) ;
#11162=CARTESIAN_POINT ( 'NONE',  ( 5.810800753368915217, 11.79079236785502260, 1.673948637325690880 ) ) ;
#11165=CARTESIAN_POINT ( 'NONE',  ( 11.92791153145151739, 21.07569174392700262, -2.114904552164332152 ) ) ;
#11169=CARTESIAN_POINT ( 'NONE',  ( 8.438110056274945592, 21.24481177138277133, -0.1056387872616715573 ) ) ;
#11170=CARTESIAN_POINT ( 'NONE',  ( 7.534092756634481525, 20.90493591499421200, 3.188157648738980221 ) ) ;
#11171=CARTESIAN_POINT ( 'NONE',  ( 2.836490765739545061, 19.10541491058949148, 7.422640015091157117 ) ) ;
#11175=CARTESIAN_POINT ( 'NONE',  ( 5.422126241162127158, 15.44426253303012508, -2.220568121751542279 ) ) ;
#11176=CARTESIAN_POINT ( 'NONE',  ( 13.75503787843007153, 21.87849604123467628, 1.799798963432884813 ) ) ;
#11178=CARTESIAN_POINT ( 'NONE',  ( 5.614158541085368270, 21.64188095357850372, 3.793657251346655990 ) ) ;
#11179=CARTESIAN_POINT ( 'NONE',  ( 1.652283335345338333, 13.93189131863066166, 9.000229686725790046 ) ) ;
#11182=CARTESIAN_POINT ( 'NONE',  ( 0.2271524594679337483, 17.19594618500607908, 0.7656857658610515260 ) ) ;
#11188=CARTESIAN_POINT ( 'NONE',  ( 10.05023619051239692, 20.92035919996038018, -1.465514317523238352 ) ) ;
#11191=CARTESIAN_POINT ( 'NONE',  ( 11.95168768794008152, 20.18527580681268319, -1.951704133241007444 ) ) ;
#11192=CARTESIAN_POINT ( 'NONE',  ( 5.788809795094107535, 19.11881477019754172, -1.442269818482195154 ) ) ;
#11194=CARTESIAN_POINT ( 'NONE',  ( 3.667426890329681832, 14.05442396375879710, -0.1080398768186726643 ) ) ;
#11197=CARTESIAN_POINT ( 'NONE',  ( 5.926337056667366099, 20.60626622430410038, 4.527039204987015175 ) ) ;
#11201=CARTESIAN_POINT ( 'NONE',  ( 11.39119446960197912, 12.85296284657052190, -2.409457258905069121 ) ) ;
#11202=CARTESIAN_POINT ( 'NONE',  ( 5.036654803598190178, 18.32506955479991007, 7.572670103872398251 ) ) ;
#11205=CARTESIAN_POINT ( 'NONE',  ( 1.687914040314732800, 17.33792227738861058, 9.588941613383601847 ) ) ;
#11216=CARTESIAN_POINT ( 'NONE',  ( 9.451771490251472230, 17.56608234664911450, -2.722081582746955775 ) ) ;
#11217=CARTESIAN_POINT ( 'NONE',  ( 1.482573138264764223, 15.39360603941805294, 8.749273869541234205 ) ) ;
#11229=CARTESIAN_POINT ( 'NONE',  ( 7.509149799818086279, 21.00645437613600208, 3.202027800742528463 ) ) ;
#11231=CARTESIAN_POINT ( 'NONE',  ( 9.115559652288139247, 13.32446407270766287, -2.907578128373548232 ) ) ;
#11241=CARTESIAN_POINT ( 'NONE',  ( 1.696449191584781024, 13.01816804744978207, 0.4119424741136656354 ) ) ;
#11244=CARTESIAN_POINT ( 'NONE',  ( 4.268923416216722444, 20.13345205411175343, 0.09844701181663598200 ) ) ;
#11257=CARTESIAN_POINT ( 'NONE',  ( 2.692116518274998427, 11.24804587133957234, 4.411506177232483061 ) ) ;
#11267=CARTESIAN_POINT ( 'NONE',  ( 5.240066203759783825, 15.55272378482423079, -1.415503761420363160 ) ) ;
#11270=CARTESIAN_POINT ( 'NONE',  ( 12.27216867080381313, 21.66113888363950224, -1.179511693193084465 ) ) ;
#11276=CARTESIAN_POINT ( 'NONE',  ( 7.448527747198094850, 20.91460427354139995, 2.960036828183352231 ) ) ;
#11279=CARTESIAN_POINT ( 'NONE',  ( 3.045314960206396471, 18.44351948381887141, 7.897937509798712341 ) ) ;
#11281=CARTESIAN_POINT ( 'NONE',  ( 13.51968262288867884, 21.40970857061781274, 1.801479536130566661 ) ) ;
#11284=CARTESIAN_POINT ( 'NONE',  ( 0.3903923183617534765, 11.71055314899741084, 3.226328323983417068 ) ) ;
#11287=CARTESIAN_POINT ( 'NONE',  ( 4.511335975532223763, 19.89702943876222108, 0.8677524747804959970 ) ) ;
#11293=CARTESIAN_POINT ( 'NONE',  ( 8.965882632090805160, 11.49625537507852080, 5.536508760620900027 ) ) ;
#11295=CARTESIAN_POINT ( 'NONE',  ( 9.140884278813414809, 13.60098928899521198, -2.935439693214477508 ) ) ;
#11301=CARTESIAN_POINT ( 'NONE',  ( 12.26775042526260151, 20.79412849038763156, -1.126120126505927299 ) ) ;
#11303=CARTESIAN_POINT ( 'NONE',  ( 8.380958430407533299, 20.95884412385370155, 5.503815002083814356 ) ) ;
#11305=CARTESIAN_POINT ( 'NONE',  ( 1.864539181856161409, 20.48283743933590273, 4.919364602564411548 ) ) ;
#11308=CARTESIAN_POINT ( 'NONE',  ( 13.60833742269821833, 21.40794255445344163, 2.232467632860299478 ) ) ;
#11313=CARTESIAN_POINT ( 'NONE',  ( -0.001888554328890318379, 17.37763432658893947, 0.0008523805038631974973 ) ) ;
#11316=CARTESIAN_POINT ( 'NONE',  ( 6.668852574927204735, 11.59258977312087069, 2.757060124530255951 ) ) ;
#11326=CARTESIAN_POINT ( 'NONE',  ( 11.20042708533316933, 21.25597787441990860, 1.691039092023997492 ) ) ;
#11331=CARTESIAN_POINT ( 'NONE',  ( 0.4158508765940340801, 19.61962022855508181, 7.543245219194639972 ) ) ;
#11342=CARTESIAN_POINT ( 'NONE',  ( 11.58160216568870737, 11.69841282151974227, -0.9529902506022120967 ) ) ;
#11345=CARTESIAN_POINT ( 'NONE',  ( 9.957248104110922426, 20.90214019755116226, -1.675082132773985322 ) ) ;
#11352=ORIENTED_EDGE ( 'NONE', *, *, #20441, .F. ) ;
#11357=CARTESIAN_POINT ( 'NONE',  ( 7.186428980350254569, 18.51696245222963455, 8.092093519166050797 ) ) ;
#11360=CARTESIAN_POINT ( 'NONE',  ( 3.724362862741987357, 12.69003629999320282, 0.02154335185942457889 ) ) ;
#11366=CARTESIAN_POINT ( 'NONE',  ( 2.657223057284000767, 12.04510335958863720, 4.259266508287976372 ) ) ;
#11375=CARTESIAN_POINT ( 'NONE',  ( 3.642152772319685372, 15.74777456311460888, 9.171823029728713550 ) ) ;
#11381=CARTESIAN_POINT ( 'NONE',  ( 13.36585934105912976, 21.37707621349031228, 1.842755075219712380 ) ) ;
#11386=CARTESIAN_POINT ( 'NONE',  ( 6.092259989090710093, 20.11689778289562014, 0.2466081011508972631 ) ) ;
#11388=CARTESIAN_POINT ( 'NONE',  ( 10.97968894901760528, 16.77770024244917835, -4.337930532459063571 ) ) ;
#11393=CARTESIAN_POINT ( 'NONE',  ( 9.192923877405071664, 13.65536061100259069, 6.430361030589125448 ) ) ;
#11394=CARTESIAN_POINT ( 'NONE',  ( 6.685429349468995142, 11.82209191741327636, 4.133463687248298157 ) ) ;
#11401=CARTESIAN_POINT ( 'NONE',  ( 3.527643555736371450, 13.65542567351872272, -0.8065990906974750407 ) ) ;
#11402=CARTESIAN_POINT ( 'NONE',  ( 0.3865264268659200919, 11.71693424989172172, 3.209193188785584905 ) ) ;
#11405=CARTESIAN_POINT ( 'NONE',  ( 3.738939841724334467, 14.05232170482083198, -0.1333566731639757863 ) ) ;
#11411=CARTESIAN_POINT ( 'NONE',  ( 6.174367295332582550, 20.69792818844234361, -0.2343385128640179116 ) ) ;
#11416=CARTESIAN_POINT ( 'NONE',  ( 9.084851576897378322, 16.05738436158114979, -3.614958053632072232 ) ) ;
#11418=CARTESIAN_POINT ( 'NONE',  ( 8.826715567800096807, 19.94865183135063091, 6.668355704914617377 ) ) ;
#11420=CARTESIAN_POINT ( 'NONE',  ( 0.4722054179714940680, 12.38306287928572047, 3.426248810200787531 ) ) ;
#11426=CARTESIAN_POINT ( 'NONE',  ( 13.20757484442835406, 18.50160361240584095, 6.057113864572380102 ) ) ;
#11429=CARTESIAN_POINT ( 'NONE',  ( 7.417648194976016462, 11.73277151300288246, 5.873043469613717704 ) ) ;
#11434=CARTESIAN_POINT ( 'NONE',  ( 6.609959801914604860, 11.00164467546537317, 2.731537079386237021 ) ) ;
#11443=CARTESIAN_POINT ( 'NONE',  ( 11.14641082499276337, 21.24872442236535264, 1.545007152345080792 ) ) ;
#11446=CARTESIAN_POINT ( 'NONE',  ( 1.224586904570614365, 15.68905071955487962, 9.060239213458530116 ) ) ;
#11453=AXIS2_PLACEMENT_3D ( 'NONE', #19976, #15550, #18323 ) ;
#11456=CARTESIAN_POINT ( 'NONE',  ( 9.535371066084531222, 12.37377145998696193, -1.078836062975678578 ) ) ;
#11460=CARTESIAN_POINT ( 'NONE',  ( 11.29892349159651133, 17.71700346048863395, 7.539582004218902789 ) ) ;
#11464=CARTESIAN_POINT ( 'NONE',  ( 6.906198364295903502, 21.59098349863498001, 1.388813212125012964 ) ) ;
#11470=CARTESIAN_POINT ( 'NONE',  ( 2.375739369545591284, 11.20929286741210085, 3.469357574953835677 ) ) ;
#11473=CARTESIAN_POINT ( 'NONE',  ( 4.920739062717439438, 21.24493168367124341, 1.822501541549086612 ) ) ;
#11483=CARTESIAN_POINT ( 'NONE',  ( 1.916346363066841585, 18.21153642991714960, -0.3663088864718270221 ) ) ;
#11491=CARTESIAN_POINT ( 'NONE',  ( 9.014641633456207614, 13.68826078499848187, -2.225326884858752408 ) ) ;
#11497=CARTESIAN_POINT ( 'NONE',  ( 8.137292697265277042, 11.64158411620971201, 1.582907052082125343 ) ) ;
#11501=CARTESIAN_POINT ( 'NONE',  ( 0.07126017807656831460, 18.21124384202859048, 0.3721193727441556298 ) ) ;
#11504=CARTESIAN_POINT ( 'NONE',  ( 7.332923656907011534, 14.94905092387569745, 7.528091012762189393 ) ) ;
#11510=CARTESIAN_POINT ( 'NONE',  ( 11.22752914188877504, 17.71807980195418608, 7.565294845482125830 ) ) ;
#11512=CARTESIAN_POINT ( 'NONE',  ( 10.02357155247649168, 20.86356153117090173, -1.536494726392103383 ) ) ;
#11514=CARTESIAN_POINT ( 'NONE',  ( 8.766965087934416090, 20.11665486425001603, 6.515999777456958242 ) ) ;
#11516=CARTESIAN_POINT ( 'NONE',  ( 0.7167346981205086065, 19.54923001721996201, 7.399086397029480011 ) ) ;
#11519=CARTESIAN_POINT ( 'NONE',  ( 6.191040577287384217, 20.33851390902405143, 5.218217981261350502 ) ) ;
#11525=CARTESIAN_POINT ( 'NONE',  ( 10.17692691125095905, 21.44638057025442279, 3.378588906132224956 ) ) ;
#11528=CARTESIAN_POINT ( 'NONE',  ( 3.722652848722313834, 16.52290265193734342, 9.281875825074834552 ) ) ;
#11537=CARTESIAN_POINT ( 'NONE',  ( 11.03331691027467620, 12.88648500492797844, 5.466329197351654123 ) ) ;
#11541=CARTESIAN_POINT ( 'NONE',  ( 12.80846360209676682, 12.10654534839631147, 4.257358460916016440 ) ) ;
#11544=CARTESIAN_POINT ( 'NONE',  ( 6.160630842786900097, 11.06731641207071171, 1.862947408479730615 ) ) ;
#11546=CARTESIAN_POINT ( 'NONE',  ( -0.1868151138448943538, 17.21628798890151302, 0.7963446044912158017 ) ) ;
#11556=CARTESIAN_POINT ( 'NONE',  ( 8.501533767468714586, 20.63193666139594029, 0.2033124972060851021 ) ) ;
#11558=CARTESIAN_POINT ( 'NONE',  ( 2.275221076386582997, 18.57027319413175803, 0.6409314954482938642 ) ) ;
#11560=CARTESIAN_POINT ( 'NONE',  ( 9.207550040625500642, 18.56570064461385527, 7.657528539673981172 ) ) ;
#11565=CARTESIAN_POINT ( 'NONE',  ( 10.44409366562669383, 19.92218912599375003, 5.282434299519857213 ) ) ;
#11566=CARTESIAN_POINT ( 'NONE',  ( 9.061749118141319670, 15.28249587578532065, -3.643789211875564149 ) ) ;
#11571=CARTESIAN_POINT ( 'NONE',  ( 2.722583763829597547, 20.92902966678202148, 1.865821207828856743 ) ) ;
#11574=CARTESIAN_POINT ( 'NONE',  ( 7.495216218794918284, 16.57436198711859632, 8.387193370074408350 ) ) ;
#11583=CARTESIAN_POINT ( 'NONE',  ( 2.181769368323757785, 12.69882926080645547, 2.054496759014617702 ) ) ;
#11584=CARTESIAN_POINT ( 'NONE',  ( 10.92073974459310115, 21.80709644552430149, -0.001139687782708651703 ) ) ;
#11585=CARTESIAN_POINT ( 'NONE',  ( 3.965678348075499127, 12.88004042469166244, 0.9588226284739858052 ) ) ;
#11589=CARTESIAN_POINT ( 'NONE',  ( 2.287589871148618226, 19.69045419824025345, 0.4926734596364841234 ) ) ;
#11598=CARTESIAN_POINT ( 'NONE',  ( 5.651664637997457774, 18.85032048260596227, -0.8301301036730029947 ) ) ;
#11605=CARTESIAN_POINT ( 'NONE',  ( 9.224670804798329016, 13.97085982373057789, 6.622973666382621971 ) ) ;
#11606=CARTESIAN_POINT ( 'NONE',  ( 7.017598957091650824, 12.50116773309939155, 5.654779006795910057 ) ) ;
#11611=CARTESIAN_POINT ( 'NONE',  ( 2.254006964870530982, 19.81104553907935895, 0.4638622323098755551 ) ) ;
#11612=CARTESIAN_POINT ( 'NONE',  ( -0.1927777004839320296, 15.08680665703588097, 0.2075260073429413266 ) ) ;
#11615=CARTESIAN_POINT ( 'NONE',  ( 1.095975960959599149, 19.74033803598106118, 2.122738190115129431 ) ) ;
#11620=CARTESIAN_POINT ( 'NONE',  ( 12.38698366852240440, 10.42448595387692301, 2.757262531655723770 ) ) ;
#11623=CARTESIAN_POINT ( 'NONE',  ( 9.863601304476318887, 20.48082896158547683, -1.957850357342349357 ) ) ;
#11626=CARTESIAN_POINT ( 'NONE',  ( 9.187132663661900622, 18.55511614605454795, 7.533150477718545623 ) ) ;
#11629=CARTESIAN_POINT ( 'NONE',  ( 6.302243142281915844, 11.75769050285926198, 2.431337456366345240 ) ) ;
#11630=CARTESIAN_POINT ( 'NONE',  ( 6.357652142832493247, 20.10075509776510572, 5.647861525684289674 ) ) ;
#11633=CARTESIAN_POINT ( 'NONE',  ( 11.62556940365261759, 17.61531206902142799, 7.032413415529686240 ) ) ;
#11634=CARTESIAN_POINT ( 'NONE',  ( 1.773193521281420049, 13.91834099111223111, 9.084643052167260535 ) ) ;
#11648=CARTESIAN_POINT ( 'NONE',  ( 12.71963864430030533, 19.02334098581724575, 5.664408184932725021 ) ) ;
#11656=CARTESIAN_POINT ( 'NONE',  ( -0.2842592608159666967, 21.03045532464439304, 5.180682183037808031 ) ) ;
#11657=CARTESIAN_POINT ( 'NONE',  ( 3.885799590448840046, 17.39673999151104056, -0.5543496090295351175 ) ) ;
#11660=CARTESIAN_POINT ( 'NONE',  ( 6.081787118896238020, 11.54994109032966065, 2.929746488810360816 ) ) ;
#11663=CARTESIAN_POINT ( 'NONE',  ( 12.22544842876060400, 20.89247853322200044, -1.170216963302677549 ) ) ;
#11665=CARTESIAN_POINT ( 'NONE',  ( 11.39060897379513371, 13.68327412096624229, 7.089011163150622075 ) ) ;
#11672=CARTESIAN_POINT ( 'NONE',  ( 9.338416706065666872, 21.08959124998475332, 2.363483124878559938 ) ) ;
#11673=CARTESIAN_POINT ( 'NONE',  ( 13.29031052474874919, 12.74100552075486270, 6.136694359698553924 ) ) ;
#11679=CARTESIAN_POINT ( 'NONE',  ( 5.268927068550723014, 12.34694125381258267, 7.212504574052345241 ) ) ;
#11683=CARTESIAN_POINT ( 'NONE',  ( 6.259225472249761779, 21.09377974628283070, 5.464090393452734951 ) ) ;
#11685=EDGE_LOOP ( 'NONE', ( #14250, #20396, #6068, #7156 ) ) ;
#11687=CARTESIAN_POINT ( 'NONE',  ( 0.1316005820730320741, 13.64832906318255645, 1.788781926648060239 ) ) ;
#11690=STYLED_ITEM ( 'NONE', ( #16939 ), #13947 ) ;
#11691=CARTESIAN_POINT ( 'NONE',  ( 13.14098188209254836, 22.19922814609550343, 0.3112431406973831249 ) ) ;
#11692=CARTESIAN_POINT ( 'NONE',  ( 4.296840172830673765, 12.04396863174460997, 2.515640464070328708 ) ) ;
#11697=CARTESIAN_POINT ( 'NONE',  ( 1.893982906205322392, 12.64452536331596733, 0.8755402015730822107 ) ) ;
#11710=CARTESIAN_POINT ( 'NONE',  ( 13.82296214138276014, 20.66289627653780059, 3.967640175402189051 ) ) ;
#11711=CARTESIAN_POINT ( 'NONE',  ( 0.8632392633340351118, 20.20131944153736114, 7.855970746976047359 ) ) ;
#11717=CARTESIAN_POINT ( 'NONE',  ( 9.228806684017154538, 16.38677358761131586, 7.225591685826160848 ) ) ;
#11721=CARTESIAN_POINT ( 'NONE',  ( 2.845659021318093007, 19.08034105350286325, 7.444203947204882432 ) ) ;
#11726=CARTESIAN_POINT ( 'NONE',  ( -0.1105414598945317628, 13.63446969317437762, 0.8406885842557084709 ) ) ;
#11730=CARTESIAN_POINT ( 'NONE',  ( -0.3546834805565413640, 20.13283946025274318, 3.854164455137035095 ) ) ;
#11738=CARTESIAN_POINT ( 'NONE',  ( 8.857113657072135382, 13.36844392990906272, -2.751357805998382311 ) ) ;
#11740=CARTESIAN_POINT ( 'NONE',  ( 12.04010895967688732, 21.53301061183326226, 4.011024392964848140 ) ) ;
#11743=CARTESIAN_POINT ( 'NONE',  ( 6.923392622719085843, 21.50917362703793145, 1.522476032831644233 ) ) ;
#11748=CARTESIAN_POINT ( 'NONE',  ( 6.204561899348269627, 20.32115355487759700, 5.253253164602614156 ) ) ;
#11751=CARTESIAN_POINT ( 'NONE',  ( 10.46803433819026097, 20.58315642183951866, -1.567353574707110120 ) ) ;
#11752=CARTESIAN_POINT ( 'NONE',  ( 5.367955360089083250, 14.66436098424711787, 7.720591347676860394 ) ) ;
#11753=CARTESIAN_POINT ( 'NONE',  ( 1.663896921981091070, 13.92038700339129242, 9.113439979769390575 ) ) ;
#11758=CARTESIAN_POINT ( 'NONE',  ( 1.281390429963812361, 20.33449649584820307, 3.528586641614371633 ) ) ;
#11765=CARTESIAN_POINT ( 'NONE',  ( 10.69728709731364802, 11.77315711255725184, 3.903429647405576297 ) ) ;
#11769=CARTESIAN_POINT ( 'NONE',  ( 13.05013046055113257, 13.27867918978523143, 5.430472891953736614 ) ) ;
#11772=CARTESIAN_POINT ( 'NONE',  ( 1.277855706708208139, 17.15958586172077460, 8.877528151527451783 ) ) ;
#11777=CARTESIAN_POINT ( 'NONE',  ( 6.153511036807811863, 11.00164291183192233, 2.868232663458314402 ) ) ;
#11779=CARTESIAN_POINT ( 'NONE',  ( 6.387440882495097227, 20.04707047619034199, 0.2130560995154684445 ) ) ;
#11780=CARTESIAN_POINT ( 'NONE',  ( 11.32770823999889842, 21.35684717879324168, 1.982554180330467153 ) ) ;
#11782=CARTESIAN_POINT ( 'NONE',  ( 7.825123033775229331, 20.10277937464278253, -1.660880645940871592 ) ) ;
#11788=CARTESIAN_POINT ( 'NONE',  ( 8.542329699723902436, 20.53907793869597853, 0.2423800136953121742 ) ) ;
#11789=CARTESIAN_POINT ( 'NONE',  ( 11.52456251676331078, 10.98707485392928085, -1.337784965846495089 ) ) ;
#11794=CARTESIAN_POINT ( 'NONE',  ( 11.29480541571663110, 19.06662053919708555, -3.732521424140298638 ) ) ;
#11795=CARTESIAN_POINT ( 'NONE',  ( -0.02599706384783656565, 20.87305502788824185, 6.462324260655689656 ) ) ;
#11798=CARTESIAN_POINT ( 'NONE',  ( 7.379864355900540573, 17.67279214094323692, 8.233010488899299872 ) ) ;
#11804=CARTESIAN_POINT ( 'NONE',  ( 1.948622324866731370, 13.89757314177814074, 0.8249782737054650594 ) ) ;
#11807=CARTESIAN_POINT ( 'NONE',  ( 3.798072540083225590, 13.90936388833114634, 0.05465243366213276555 ) ) ;
#11813=CARTESIAN_POINT ( 'NONE',  ( 1.660370454735925483, 15.04581296003263446, -0.5192195669560754068 ) ) ;
#11823=CARTESIAN_POINT ( 'NONE',  ( 5.522956963460583957, 13.98659666219624675, -0.8314415007726022599 ) ) ;
#11831=CARTESIAN_POINT ( 'NONE',  ( 8.448334465459019782, 11.54763819966888150, 2.948056682048101340 ) ) ;
#11836=CARTESIAN_POINT ( 'NONE',  ( -0.07141578697956746380, 17.27597877604544863, 0.1156807881660063680 ) ) ;
#11839=CARTESIAN_POINT ( 'NONE',  ( 4.036164809125949660, 12.82285234092424098, 0.8599284710103052287 ) ) ;
#11846=CARTESIAN_POINT ( 'NONE',  ( 5.497918191286784939, 19.19176664446208136, -1.343533416796099944 ) ) ;
#11847=CARTESIAN_POINT ( 'NONE',  ( 12.82008979290802309, 19.79331256264924832, 6.077639648942910533 ) ) ;
#11849=CARTESIAN_POINT ( 'NONE',  ( 9.359056336617545213, 17.47150019132489263, 7.876253759257760834 ) ) ;
#11850=CARTESIAN_POINT ( 'NONE',  ( 2.863177793647310843, 19.21875272216368202, 7.432696887173809053 ) ) ;
#11854=CARTESIAN_POINT ( 'NONE',  ( 7.320120958300368130, 15.63209079431325144, 7.583971929050274063 ) ) ;
#11858=CARTESIAN_POINT ( 'NONE',  ( 14.23150068160818726, 21.00494883119180045, 3.295237727640887293 ) ) ;
#11859=CARTESIAN_POINT ( 'NONE',  ( 5.099963284237507111, 11.34514690749418087, 5.595862192416997338 ) ) ;
#11866=SURFACE_SIDE_STYLE ('',( #2123 ) ) ;
#11869=B_SPLINE_CURVE_WITH_KNOTS ( 'NONE', 3,
 ( #10729, #2317, #7519, #19331, #880, #2207, #4196, #14175, #9051, #7401, #12714, #14490, #12277, #20880, #5750, #10615, #7948, #14823, #8272, #8052, #3192, #14718, #2755, #21652, #12837, #11381 ),
 .UNSPECIFIED., .F., .F.,
 ( 4, 2, 2, 1, 2, 2, 2, 2, 1, 2, 2, 2, 2, 4 ),
 ( 0.000000000000000000, 0.06249999999999777955, 0.1249999999999955591, 0.1874999999999933387, 0.2187499999999900913, 0.2499999999999868439, 0.5000000000000003331, 0.6250000000000033307, 0.6875000000000076605, 0.7187500000000097700, 0.7500000000000117684, 0.8125000000000098810, 0.8750000000000079936, 1.000000000000000000 ),
 .UNSPECIFIED. ) ;
#11870=CARTESIAN_POINT ( 'NONE',  ( 8.610469691664995651, 21.47961674228977103, 0.3618051172526235981 ) ) ;
#11873=CARTESIAN_POINT ( 'NONE',  ( 13.04877617004700951, 13.26865620857769201, 5.423244249217728630 ) ) ;
#11875=CARTESIAN_POINT ( 'NONE',  ( 2.607742312338097168, 20.27761254839711924, 2.237459158246773328 ) ) ;
#11883=CARTESIAN_POINT ( 'NONE',  ( 9.167756006212099962, 13.35056178516542325, 6.341038218456379383 ) ) ;
#11885=CARTESIAN_POINT ( 'NONE',  ( 11.15100426632415420, 14.44107328295670634, -3.341937556964096334 ) ) ;
#11886=CARTESIAN_POINT ( 'NONE',  ( 4.017631021903100397, 15.51072843360936204, -1.195195369806848262 ) ) ;
#11887=CARTESIAN_POINT ( 'NONE',  ( 9.448052803682784884, 16.63233464712778087, 8.098436675483521086 ) ) ;
#11892=CARTESIAN_POINT ( 'NONE',  ( 8.946817783206428842, 20.96102289200085167, 1.313562465597416740 ) ) ;
#11893=CARTESIAN_POINT ( 'NONE',  ( 12.16871400957597515, 21.60439101236092085, -1.553992429234034800 ) ) ;
#11897=CARTESIAN_POINT ( 'NONE',  ( 10.94956279435578139, 14.20305175510790185, -3.949782705418857454 ) ) ;
#11898=CARTESIAN_POINT ( 'NONE',  ( 2.526745181667069406, 20.84690199368946040, 1.966986596898897544 ) ) ;
#11901=CARTESIAN_POINT ( 'NONE',  ( 7.175445692564514921, 18.81307093152634735, 7.806506937020126102 ) ) ;
#11910=CARTESIAN_POINT ( 'NONE',  ( 2.035270604800319738, 12.09972725174282182, 1.536988627584183309 ) ) ;
#11921=CARTESIAN_POINT ( 'NONE',  ( 10.82096220742486281, 16.27085401118791452, -3.689681977176763716 ) ) ;
#11923=CARTESIAN_POINT ( 'NONE',  ( 0.07032913840789803417, 12.52705325500010325, 1.657397282339138078 ) ) ;
#11930=CARTESIAN_POINT ( 'NONE',  ( 7.447672119940222935, 15.77891879107950324, -2.094525022072177833 ) ) ;
#11935=CARTESIAN_POINT ( 'NONE',  ( -0.1907120674000438720, 14.86661835102559159, 0.2656455004388350027 ) ) ;
#11939=CARTESIAN_POINT ( 'NONE',  ( 0.4090325377308574040, 17.21628798890151302, 0.6179089441262706206 ) ) ;
#11946=CARTESIAN_POINT ( 'NONE',  ( 9.052467241478945326, 12.91190710784102080, 6.975301435476066736 ) ) ;
#11948=CARTESIAN_POINT ( 'NONE',  ( 13.37137086141695619, 16.12366711453539736, 7.173766633443349860 ) ) ;
#11951=CARTESIAN_POINT ( 'NONE',  ( 13.11605872809629858, 21.42344080416877006, 1.163243345628418357 ) ) ;
#11952=CARTESIAN_POINT ( 'NONE',  ( 9.491314998020746074, 14.79089830327174937, 7.774602169083346226 ) ) ;
#11953=CARTESIAN_POINT ( 'NONE',  ( 4.255350674082147400, 12.02975038249582163, 2.250507228818958705 ) ) ;
#11957=CARTESIAN_POINT ( 'NONE',  ( 1.414909354815941267, 18.54739417496245579, 8.316710155238244084 ) ) ;
#11958=CARTESIAN_POINT ( 'NONE',  ( 1.026903634312197333, 19.93157197858078788, 2.808439018299325074 ) ) ;
#11962=CARTESIAN_POINT ( 'NONE',  ( 11.73734890072733172, 21.76139788190002022, 1.882179297186191036 ) ) ;
#11963=CARTESIAN_POINT ( 'NONE',  ( 4.677500656696262915, 10.96673477554678122, 3.790603218585762324 ) ) ;
#11967=CARTESIAN_POINT ( 'NONE',  ( 6.416266621286034422, 10.92343542074206120, 2.783831947462576561 ) ) ;
#11976=CARTESIAN_POINT ( 'NONE',  ( 11.28778781650649776, 17.64863795527461576, 7.430186115869990893 ) ) ;
#11979=CARTESIAN_POINT ( 'NONE',  ( 13.16590010066154015, 14.90344756276430616, 6.212949255494740974 ) ) ;
#11981=CARTESIAN_POINT ( 'NONE',  ( 0.5001283093862811668, 19.74033803598106118, 2.301173850479345528 ) ) ;
#11991=CARTESIAN_POINT ( 'NONE',  ( 9.709978852237810543, 21.05303134726939973, 3.417248539804212282 ) ) ;
#11992=CARTESIAN_POINT ( 'NONE',  ( 3.930841689390241811, 20.49042122551175638, 4.838430134900644219 ) ) ;
#11994=CARTESIAN_POINT ( 'NONE',  ( 7.553652573848785856, 21.00575954651474220, 3.188648499624214150 ) ) ;
#11995=CARTESIAN_POINT ( 'NONE',  ( 9.442279758265636147, 19.32856220366442201, -2.967836764750759304 ) ) ;
#12000=CARTESIAN_POINT ( 'NONE',  ( 9.180768457294835372, 21.06661498530921151, 1.940146591543385979 ) ) ;
#12001=CARTESIAN_POINT ( 'NONE',  ( 12.94877351110852715, 11.26870765665696084, 4.634005384042424680 ) ) ;
#12006=CARTESIAN_POINT ( 'NONE',  ( 2.950312850434896106, 11.97425653754774189, 6.932220074007259036 ) ) ;
#12009=CARTESIAN_POINT ( 'NONE',  ( 7.406607808117615654, 13.05076105357039573, 7.314782732399700116 ) ) ;
#12012=CARTESIAN_POINT ( 'NONE',  ( 0.2665283650859920916, 12.98379964877340775, 2.505562667629908535 ) ) ;
#12015=CARTESIAN_POINT ( 'NONE',  ( 1.991330241149480873, 13.57173140902838782, 1.074079535782173300 ) ) ;
#12020=CARTESIAN_POINT ( 'NONE',  ( 4.690729861326075500, 20.36709625471669938, 6.894995340168590836 ) ) ;
#12031=CARTESIAN_POINT ( 'NONE',  ( 10.20687392145870653, 20.34020649082646059, 4.946106562410360397 ) ) ;
#12033=CARTESIAN_POINT ( 'NONE',  ( 2.107350683505484490, 11.83412605131448103, 1.752489760913824579 ) ) ;
#12041=CARTESIAN_POINT ( 'NONE',  ( 7.584943636950675305, 13.21535262572377611, -0.9819277678746927140 ) ) ;
#12050=CARTESIAN_POINT ( 'NONE',  ( 2.190455368389823576, 21.01608119939916364, 5.860843236296549463 ) ) ;
#12055=CARTESIAN_POINT ( 'NONE',  ( 2.483346228476034590, 12.45711053362852283, 2.021137222503261555 ) ) ;
#12061=CARTESIAN_POINT ( 'NONE',  ( 11.45962687667246804, 20.25175440475918265, -3.101195653451903400 ) ) ;
#12063=CARTESIAN_POINT ( 'NONE',  ( 13.38710885774181314, 15.59940030760539820, 7.127019235770691630 ) ) ;
#12069=CARTESIAN_POINT ( 'NONE',  ( 9.327916374733275617, 17.71149373539732252, 7.821919058577349482 ) ) ;
#12070=CARTESIAN_POINT ( 'NONE',  ( 4.550724514086687655, 19.87742190051230295, 6.393129328018801516 ) ) ;
#12072=CARTESIAN_POINT ( 'NONE',  ( 5.710684426658359847, 17.22355540511336258, -1.322581421157464909 ) ) ;
#12073=CARTESIAN_POINT ( 'NONE',  ( 7.068676109993910828, 17.98782383223260695, 7.330006056139382942 ) ) ;
#12077=CARTESIAN_POINT ( 'NONE',  ( 7.701365284815051560, 12.68409469243044363, -1.677233022421109832 ) ) ;
#12080=CARTESIAN_POINT ( 'NONE',  ( 5.716420248627351874, 15.64056738454816120, 8.837994797662030777 ) ) ;
#12087=CARTESIAN_POINT ( 'NONE',  ( 0.1697664307767892677, 13.13563057234646081, 2.183769842644804005 ) ) ;
#12092=B_SPLINE_CURVE_WITH_KNOTS ( 'NONE', 3,
 ( #6438, #4787, #11629, #6644, #3781, #12291, #8964, #1888, #13742, #17490, #5648, #5766, #15628, #20785, #2225, #19016, #19134, #12407, #2105, #5307, #20560, #10515, #20898, #15741, #12186, #4002, #10846, #3892, #19246, #569, #12522, #344, #13858, #15842, #7418, #7089, #15411, #4107, #6974, #5421, #10745, #18910, #5532, #8847, #17261, #14077, #8635, #14190, #233, #20438, #10414, #12072, #10630, #18800, #2333, #9067, #465, #3668, #7213, #13975, #20672, #17382, #671, #7313, #17156, #1995, #8737, #15514, #4536, #12623, #14506, #12731, #4328, #19345, #7534, #1106, #4213, #4440, #21221, #9289, #5964, #12961, #7743, #14298, #2557, #5864, #9613, #6080, #21334, #7850, #11276, #17705, #11067, #11170, #14731, #14626, #10951, #16064, #19453, #9398, #21438, #12854, #897, #4649, #9505, #1218, #7962, #17594, #6291, #19668, #7638, #14400, #18026, #21113, #17823, #2882, #2667, #13067, #9174, #2447, #786, #993, #16166, #19573, #17922, #2768, #16276, #21017, #6194, #19774, #16380, #15955, #20209, #8381, #4761, #13492, #9723, #11717, #20310, #16902, #6734, #19992, #3324, #4864, #9823, #18240, #3204, #21876, #98, #19889, #14949, #6848, #11605, #4963, #11393, #20096, #15271, #1750, #1429, #13608, #9938, #6621, #21549, #5080, #15155, #10156, #21667, #18341, #18139, #2997, #10055, #16487, #6527, #16701, #18452, #1542, #1320, #8287, #16805, #8491, #1642, #21769, #11831, #18560, #3423, #8063, #14834, #15057, #6408, #13180, #13385, #11497, #3099, #16591, #8172, #13287, #5505, #18885, #17131, #20530, #10601, #12376, #3755, #20758, #8816, #7288, #5278, #18771, #2196, #15713, #12041, #18659, #540, #3528, #3641, #12266, #5397, #10265, #13713, #8608, #8936, #5615, #14052, #5179, #11930, #10387, #15383, #15594, #17011, #1866, #207, #429, #1971, #10490, #7182, #13946, #8711, #6950, #20413, #15489, #315, #12160, #7060, #13826, #17232, #18988, #17348, #2074, #3863, #20643, #1387, #18620, #16553, #8350, #6911, #15121, #1500, #5037, #16768, #20054, #9892, #11788, #8129, #16657, #10015, #6692, #5239, #11892, #18302, #13564, #6485, #3160, #9784, #12000, #13249, #11672, #16865, #18411, #8246, #15018, #1607, #20160, #14908, #13452, #1710, #13674, #21838, #20374, #3282, #19958, #21736, #18520, #4830, #3487, #21624, #3386, #11565, #20268, #50, #1820, #13350, #10223, #6589, #10119, #4924, #8449, #15222, #3061, #6804, #5140, #16970, #8563, #15339, #168, #7252, #3820, #8774, #9004, #5806, #2378, #15886, #18843, #18947, #10675, #711, #606, #12119, #7014, #20715, #4039, #18732, #10785, #1929, #15447, #386, #274, #20487, #7139, #6457, #10198, #1792, #1474, #6774, #11537, #3253, #16941, #1584, #8535, #4698, #6337, #18277, #8328, #6662, #13423, #5011, #11765, #8777, #9109, #15783, #12122, #13910, #10681, #9222, #15891, #390, #17534, #10455, #7144, #13785, #16005, #17193, #15676, #20827, #506, #5466, #20608, #20720, #2382, #17637, #15558, #10558, #10889, #19060, #2490, #7257, #2033, #12228, #14016, #18951, #7466, #20490, #2269, #3824, #716, #4045, #5811, #17304, #5575, #7017, #5361, #5696, #17427, #14122, #18847, #3714, #14237, #10789, #2152, #12334, #20954, #7355, #9008, #12567, #19289, #3935, #8897, #610, #4151, #12456, #19179, #6128, #19712, #9764, #11216, #18187, #7897, #4702, #21159, #12786, #14775, #6340, #6014, #14340, #19827, #9442, #2603, #12668, #6234, #17756, #9551, #19613, #5906, #19509, #18077, #12898, #19391, #7683, #10999, #21484, #17967, #4585, #13008, #16430, #936, #16214, #16320, #11443, #11326, #16106, #14442, #17863, #11112, #4479, #2817, #4373, #832, #14673, #13114, #3040, #7578, #21055, #2937, #2709, #1041, #1262, #7787, #14555, #8003, #21273, #4260, #1158, #21380, #9663, #21813, #14998, #18495, #8330, #11648, #1477, #6462, #8224, #13651, #3141, #16945, #3468, #13542, #9865, #18600, #14882, #16844, #3577, #16530, #19936, #3256, #8424, #9992, #21714, #6568, #15098, #5123, #5221, #16634, #20032, #11979, #16747, #10098, #1361, #3367, #20351, #6890, #13329, #1797, #8104, #11769, #4809, #11873, #20248, #15320, #4900, #1588, #21600, #13226, #15200, #11541, #18384, #6666, #1685, #13427, #18708, #20137, #28, #10202, #6779, #5014, #8540, #143, #18281, #13763, #7114, #14099, #20694, #20581, #15654, #4023, #19037, #19157, #5331, #7236, #5441, #20802, #5551, #10653, #12205, #7333, #19269, #12309, #5786, #17406, #14212, #8752, #363, #2355, #15863, #15533, #1906, #7436, #15426, #13883, #5669, #483, #252, #17281, #18928, #588, #12545, #692, #20926, #10316, #18821, #8652, #3910, #17061, #12429, #10767, #2126, #12097, #3798, #13994, #2246, #3688, #6992, #8983, #15761, #10431, #20462, #9085, #17171, #10534, #2011, #8870, #17510, #10867, #12981, #15979, #19689, #810, #16190, #7982, #1017, #2579, #19593, #17731, #7659, #6210, #11191, #14318, #14420, #11091, #7764, #21037, #11301, #5988, #21353, #12758, #19480, #2690, #21249, #9527, #1129, #2906, #14753, #21458, #15509, #17256, #8844, #11951, #2098, #5528, #17486 ),
 .UNSPECIFIED., .F., .F.,
 ( 4, 3, 3, 3, 3, 3, 3, 3, 3, 3, 3, 3, 3, 3, 3, 3, 3, 3, 3, 3, 3, 3, 3, 3, 3, 3, 3, 3, 3, 3, 3, 3, 3, 3, 3, 3, 3, 3, 3, 3, 3, 3, 3, 3, 3, 3, 3, 3, 3, 3, 3, 3, 3, 3, 3, 3, 3, 3, 3, 3, 3, 3, 3, 3, 3, 3, 3, 3, 3, 3, 3, 3, 3, 3, 3, 3, 3, 3, 3, 3, 3, 3, 3, 3, 3, 3, 3, 3, 3, 3, 3, 3, 3, 3, 3, 3, 3, 3, 3, 3, 3, 3, 3, 3, 3, 3, 3, 3, 3, 3, 3, 3, 3, 3, 3, 3, 3, 3, 3, 3, 3, 3, 3, 3, 3, 3, 3, 3, 3, 3, 3, 3, 3, 3, 3, 3, 3, 3, 3, 3, 3, 3, 3, 3, 3, 3, 3, 3, 3, 3, 3, 3, 3, 3, 3, 3, 3, 3, 3, 3, 3, 3, 3, 3, 3, 3, 3, 3, 3, 3, 3, 3, 3, 3, 3, 3, 3, 3, 3, 3, 3, 3, 3, 3, 3, 3, 3, 3, 3, 3, 3, 3, 3, 3, 3, 3, 3, 3, 3, 3, 3, 3, 3, 3, 3, 3, 3, 3, 3, 3, 3, 3, 3, 3, 3, 3, 4 ),
 ( 3.913411576274749967E-10, 0.006369427103560140052, 0.01249999939102700020, 0.01273885381577509988, 0.01910828052800209870, 0.02547770724021910030, 0.02875000254734080135, 0.03184713395243609496, 0.03821656066465310003, 0.04458598737687999997, 0.04500000225596059722, 0.05095541408909699810, 0.05732484080131399623, 0.06124999398789569838, 0.06369426751353099436, 0.07006369422575800532, 0.07643312093797499651, 0.07750000840243019551, 0.08280254765019190444, 0.08917197436240889563, 0.09374998978646680026, 0.09554140107463589271, 0.1019108277868729928, 0.1082802544991000038, 0.1100000129344189947, 0.1146496812113270009, 0.1210191079235540118, 0.1262499915749089874, 0.1273885346356810055, 0.1337579613479080165, 0.1401273880601349997, 0.1425000117241630171, 0.1464968147723620107, 0.1528662414845889939, 0.1587499967440479942, 0.1592356681968160048, 0.1656050949090429880, 0.1719745216212700267, 0.1750000048165079869, 0.1783439483334970099, 0.1847133750457240209, 0.1910828017579510041, 0.1912499997860669931, 0.1974522284701780150, 0.2038216551824049982, 0.2074999958526209942, 0.2101910818945320059, 0.2165605086067590168, 0.2229299353189860000, 0.2237500049592059947, 0.2292993620312130110, 0.2356687887434399942, 0.2399999896536270105, 0.2420382154556670051, 0.2484076421678940161, 0.2547770688801209715, 0.2562500107525759740, 0.2611464955923479825, 0.2675159223045749934, 0.2724999892630159959, 0.2738853490168020044, 0.2802547757290280162, 0.2866242024412549716, 0.2887500119236349749, 0.2929936291533819515, 0.2993630558656089624, 0.3049999937500470493, 0.3057324825778360289, 0.3121019092900629843, 0.3184713360022899953, 0.3212500068789819752, 0.3248407627145170062, 0.3312101894267439617, 0.3375796161389710281, 0.3439490428511979836, 0.3503184695634249946, 0.3537499981227409940, 0.3566878962756520055, 0.3630573229878790165, 0.3694267497001059719, 0.3700000016114870505, 0.3757961764122330073, 0.3821656031244600182, 0.3862499903775790111, 0.3885350298366869737, 0.3949044565489140401, 0.4012738832611409956, 0.4025000078859060082, 0.4076433099733680065, 0.4140127366855950175, 0.4187499876790780062, 0.4203821633978219729, 0.4267515901100490394, 0.4331210168222760504, 0.4350000112083169945, 0.4394904435345030058, 0.4458598702467300168, 0.4512499907420399747, 0.4522292969589570277, 0.4585987236710840076, 0.4649681503833110185, 0.4675000083970360376, 0.4713375770955380295, 0.4777070038077650405, 0.4837499959041640096, 0.4840764305199919959, 0.4904458572322190069, 0.4968152839444460178, 0.5000000005418490101, 0.5031847106566730288, 0.5095541373688999842, 0.5159235640811269397, 0.5162499986996510470, 0.5222929907933540061, 0.5286624175055810726, 0.5324999918453350300, 0.5350318442178080280, 0.5414012709300350945, 0.5477706976421620189, 0.5487500045795760117, 0.5541401243543889743, 0.5605095510666160408, 0.5649999869507580375, 0.5668789777788429962, 0.5732484044910699517, 0.5796178312032970181, 0.5812500095876119710, 0.5859872579155239736, 0.5923566846277509290, 0.5974999880555230680, 0.5987261113399779955, 0.6050955380522050620, 0.6114649647644320174, 0.6137500091740419883, 0.6178343914766590839, 0.6242038181888860393, 0.6299999931106780027, 0.6305732449010130747, 0.6369426716132400301, 0.6433120983254669856, 0.6462500028379470907, 0.6496815250376939410, 0.6560509517499210075, 0.6624203784621479629, 0.6687898051743739192, 0.6751592318866019848, 0.6787499938729660842, 0.6815286585988289403, 0.6878980853110550076, 0.6942675120232830732, 0.6950000011427179825, 0.7006369387355090295, 0.7070063654477359849, 0.7112499871106169325, 0.7133757921598630203, 0.7197452188720899757, 0.7261146455843170422, 0.7275000071637089949, 0.7324840722965439976, 0.7388534990087709531, 0.7437499859629570498, 0.7452229257209980195, 0.7515923524332249750, 0.7579617791454519304, 0.7600000090789329477, 0.7643312058576789969, 0.7707006325699060634, 0.7762499900630959182, 0.7770700592821330188, 0.7834394859943600853, 0.7898089127065870407, 0.7925000047482080312, 0.7961783394187139651, 0.8025477661309410315, 0.8087499948081490198, 0.8089171928431679870, 0.8152866195553949424, 0.8216560462676220089, 0.8249999962251529650, 0.8280254729798489643, 0.8343948996920759198, 0.8407643264043029863, 0.8412499979177490150, 0.8471337531165300527, 0.8535031798287568972, 0.8574999881000170410, 0.8598726065409840746, 0.8662420332532110301, 0.8726114599654379855, 0.8737500041287140640, 0.8789808866775650209, 0.8853503133897919763, 0.8899999846533520609, 0.8917197401020189318, 0.8980891668142459983, 0.9044585935264729537, 0.9062500080622120091, 0.9108280202386999092, 0.9171974469509269756, 0.9224999871212090641, 0.9235668736631539311, 0.9299363003753809975, 0.9363057270876080640, 0.9387500060427089732, 0.9426751537998350194, 0.9490445805120619749, 0.9549999923723109241, 0.9554140072242890414, 0.9617834339364159657, 0.9681528606486430322, 0.9712499985339340114, 0.9745222873608699876, 0.9808917140730969431, 0.9872611407853240095, 0.9874999952026149996, 0.9936305674975509650, 0.9999999942097779204 ),
 .UNSPECIFIED. ) ;
#12094=CARTESIAN_POINT ( 'NONE',  ( 11.22444918248842072, 18.10120891158497258, 7.310595827509144051 ) ) ;
#12097=CARTESIAN_POINT ( 'NONE',  ( 11.15612707441398044, 15.87324431098740085, -3.568713840340196786 ) ) ;
#12099=CARTESIAN_POINT ( 'NONE',  ( 2.913591648697507974, 17.99578554531247576, 8.387739717085498370 ) ) ;
#12104=CARTESIAN_POINT ( 'NONE',  ( 6.013049556678311092, 11.37554327182399305, 2.937595415487594064 ) ) ;
#12109=CARTESIAN_POINT ( 'NONE',  ( 8.607975884807220979, 19.62966740229102314, 6.049914683357609846 ) ) ;
#12110=CARTESIAN_POINT ( 'NONE',  ( 10.70304827739237652, 21.11777521280046344, 0.2911716477774642930 ) ) ;
#12111=CARTESIAN_POINT ( 'NONE',  ( 4.431163241856458157, 18.91035477026892409, -0.6033642490446163853 ) ) ;
#12112=CARTESIAN_POINT ( 'NONE',  ( 11.29543655879299102, 22.16525292274814163, 2.036776594994900158 ) ) ;
#12119=CARTESIAN_POINT ( 'NONE',  ( 11.21722422336513958, 15.53347034410194638, 6.755855952064321102 ) ) ;
#12120=CARTESIAN_POINT ( 'NONE',  ( 9.486626320258515932, 19.32892518063468046, -2.981737702492698094 ) ) ;
#12122=CARTESIAN_POINT ( 'NONE',  ( 10.60309855497350995, 11.60677215276931307, 3.485811182180083012 ) ) ;
#12124=CARTESIAN_POINT ( 'NONE',  ( 12.84499073484238529, 22.15877926570874479, 0.4069147557942170979 ) ) ;
#12126=CARTESIAN_POINT ( 'NONE',  ( -0.4924320145162884854, 15.60814665309257343, 0.1703380108912158075 ) ) ;
#12129=CARTESIAN_POINT ( 'NONE',  ( 6.608070263590670734, 10.94537441895658247, 3.759284071021552265 ) ) ;
#12133=CARTESIAN_POINT ( 'NONE',  ( 0.1546840198724105664, 13.50064022236746197, 1.919107787120799546 ) ) ;
#12138=CARTESIAN_POINT ( 'NONE',  ( 13.36585934105912976, 21.37707621349031228, 1.842755075219712380 ) ) ;
#12141=CARTESIAN_POINT ( 'NONE',  ( 5.396977437131427635, 17.85491577864669210, 8.577743016638430973 ) ) ;
#12153=CARTESIAN_POINT ( 'NONE',  ( 5.580593771912873535, 15.56575848494070868, -1.427280786813629021 ) ) ;
#12154=CARTESIAN_POINT ( 'NONE',  ( 1.272552473378664173, 21.11368951514764092, 3.304751149015114464 ) ) ;
#12156=CARTESIAN_POINT ( 'NONE',  ( 5.336823734216668669, 12.43211864545296130, 7.110286411329449052 ) ) ;
#12160=CARTESIAN_POINT ( 'NONE',  ( 7.714989009133786269, 18.22557723514703909, -1.778184321832799064 ) ) ;
#12163=CARTESIAN_POINT ( 'NONE',  ( 3.429843259907740638, 15.08894331730447824, 8.264066473586211714 ) ) ;
#12167=CARTESIAN_POINT ( 'NONE',  ( 2.774532003195825158, 20.20761322045536801, 7.401467972215330704 ) ) ;
#12170=CARTESIAN_POINT ( 'NONE',  ( 6.497001381719418767, 20.52421269917602231, 5.165954059377466656 ) ) ;
#12176=CARTESIAN_POINT ( 'NONE',  ( 10.99454862271408118, 17.69506805168922980, 7.542432694877700072 ) ) ;
#12178=CARTESIAN_POINT ( 'NONE',  ( 11.15535515337743355, 22.04911995710877193, 1.564565634628638291 ) ) ;
#12183=CARTESIAN_POINT ( 'NONE',  ( 8.466430781601271605, 10.75601055456078292, 3.008801692261342531 ) ) ;
#12184=CARTESIAN_POINT ( 'NONE',  ( 4.941667063029573370, 12.10288835339510172, 5.331384855635830533 ) ) ;
#12186=CARTESIAN_POINT ( 'NONE',  ( 5.701223588767351025, 13.46368314359502172, -0.4004066624196506718 ) ) ;
#12187=CARTESIAN_POINT ( 'NONE',  ( 7.259060271705660483, 16.62791818454387638, 7.622863755745528991 ) ) ;
#12190=CARTESIAN_POINT ( 'NONE',  ( 8.731341498189751249, 21.27400681123072346, -0.2105259513614896327 ) ) ;
#12191=CARTESIAN_POINT ( 'NONE',  ( 4.991580028654951207, 12.36007056541882676, 5.665111606981183101 ) ) ;
#12193=CARTESIAN_POINT ( 'NONE',  ( 13.40968688455454405, 21.37908828663751848, 1.829925544955474104 ) ) ;
#12194=CARTESIAN_POINT ( 'NONE',  ( 0.02568036181144206509, 12.52652910124526109, 1.670289039172707657 ) ) ;
#12195=CARTESIAN_POINT ( 'NONE',  ( 1.145631384210077153, 19.30514743024435731, 8.620931369668081601 ) ) ;
#12197=CARTESIAN_POINT ( 'NONE',  ( 3.332789469297661622, 13.61441523003558274, 7.617045249923235950 ) ) ;
#12202=CARTESIAN_POINT ( 'NONE',  ( 10.12849651354907188, 21.37172880332488134, 4.537220786037014619 ) ) ;
#12205=CARTESIAN_POINT ( 'NONE',  ( 11.74400045100115442, 11.53932207960275313, -0.3771188630170393963 ) ) ;
#12217=CARTESIAN_POINT ( 'NONE',  ( 10.78489084012707444, 11.65180524149912245, 3.851168386773756946 ) ) ;
#12218=CARTESIAN_POINT ( 'NONE',  ( 4.732537519185278541, 19.32618335802288456, 6.876597588250359827 ) ) ;
#12219=CARTESIAN_POINT ( 'NONE',  ( 6.423071385528279720, 20.04707047619034199, 0.2023860023504502892 ) ) ;
#12220=CARTESIAN_POINT ( 'NONE',  ( 0.1034156370570294553, 15.60814665309257343, -0.008097649473000866072 ) ) ;
#12225=CARTESIAN_POINT ( 'NONE',  ( 10.44704334393187040, 21.01241846032922211, 5.354331383626338869 ) ) ;
#12228=CARTESIAN_POINT ( 'NONE',  ( 9.611418352984147262, 12.34090135786862064, -0.8804288050913021690 ) ) ;
#12231=CARTESIAN_POINT ( 'NONE',  ( 7.200333630658113826, 16.63782405840064982, 8.499115931225610154 ) ) ;
#12237=CARTESIAN_POINT ( 'NONE',  ( 0.09157794466913266040, 16.58397131323004459, 0.8032362651113809093 ) ) ;
#12257=CARTESIAN_POINT ( 'NONE',  ( 11.04394092023493279, 14.44257473674272241, -3.305683158826597356 ) ) ;
#12258=CARTESIAN_POINT ( 'NONE',  ( 3.822081440817369558, 12.20035416735056266, 0.3768256591275319645 ) ) ;
#12261=CARTESIAN_POINT ( 'NONE',  ( 5.600389116865858163, 15.22982981733899166, 8.688047065010637837 ) ) ;
#12266=CARTESIAN_POINT ( 'NONE',  ( 7.499759535020694479, 13.88337118655590707, -1.456658198050375663 ) ) ;
#12271=CARTESIAN_POINT ( 'NONE',  ( 3.541706160064697961, 17.13097328727698354, 9.143733616943571008 ) ) ;
#12275=CARTESIAN_POINT ( 'NONE',  ( 2.845328762890635854, 20.46094657096126213, 6.331683592853763365 ) ) ;
#12277=CARTESIAN_POINT ( 'NONE',  ( 12.99934549847542975, 21.71373124764409468, 2.001921367698964893 ) ) ;
#12282=CARTESIAN_POINT ( 'NONE',  ( 9.942270574732733124, 20.67808185030680335, 5.266683502927268279 ) ) ;
#12284=CARTESIAN_POINT ( 'NONE',  ( 11.95009173601784269, 10.47212404987846135, 0.5522848250625118638 ) ) ;
#12288=CARTESIAN_POINT ( 'NONE',  ( 9.446499639003540949, 13.84869720761932577, 7.423493914728108933 ) ) ;
#12289=CARTESIAN_POINT ( 'NONE',  ( 0.06378921647583885024, 14.29169281587572371, 1.241023057593835466 ) ) ;
#12291=CARTESIAN_POINT ( 'NONE',  ( 6.168663171305069248, 11.89819385903220095, 1.834497862875971164 ) ) ;
#12292=CARTESIAN_POINT ( 'NONE',  ( 1.844819993078286480, 20.39307813490978560, 4.918341983821658658 ) ) ;
#12294=CARTESIAN_POINT ( 'NONE',  ( 11.44565647860347823, 14.29921781272587289, -3.826291723331187722 ) ) ;
#12296=CARTESIAN_POINT ( 'NONE',  ( -0.1939951092443372993, 13.90873432424026213, 0.5745305717807484003 ) ) ;
#12299=CARTESIAN_POINT ( 'NONE',  ( 2.432517352912638486, 19.25811192615784151, 1.027623169201872688 ) ) ;
#12306=CARTESIAN_POINT ( 'NONE',  ( 10.32709312739783059, 21.06472931975369889, 5.073596581982923404 ) ) ;
#12309=CARTESIAN_POINT ( 'NONE',  ( 11.63972793865917943, 11.75705524565226057, -0.8376248640525733036 ) ) ;
#12319=CARTESIAN_POINT ( 'NONE',  ( 12.56063288857526494, 19.93927778675710272, 5.046451759067746679 ) ) ;
#12320=CARTESIAN_POINT ( 'NONE',  ( 7.562553572936893787, 21.00645437613600208, 3.186035226974327728 ) ) ;
#12321=CARTESIAN_POINT ( 'NONE',  ( 2.907540519534558943, 11.61267145053902006, 3.383141968181686110 ) ) ;
#12326=UNCERTAINTY_MEASURE_WITH_UNIT (LENGTH_MEASURE( 1.000000000000000082E-05 ), #3461, 'distance_accuracy_value', 'NONE');
#12331=CARTESIAN_POINT ( 'NONE',  ( 6.500793124041273074, 10.79737175431668206, 3.223669991492981168 ) ) ;
#12334=CARTESIAN_POINT ( 'NONE',  ( 9.294261281082977888, 15.43778034884425843, -2.770203070420261149 ) ) ;
#12338=CARTESIAN_POINT ( 'NONE',  ( -0.4864308613666389891, 14.10021357005799025, 1.033949880137899680 ) ) ;
#12341=CARTESIAN_POINT ( 'NONE',  ( 6.717861222798634735, 11.03073353602231066, 4.225789866886649371 ) ) ;
#12346=CARTESIAN_POINT ( 'NONE',  ( 0.03937504533965078407, 14.66358865000540668, 1.157625443383156760 ) ) ;
#12351=CARTESIAN_POINT ( 'NONE',  ( 2.043921479127090102, 17.43725209588588143, 0.1880180425226697094 ) ) ;
#12366=CARTESIAN_POINT ( 'NONE',  ( 5.630097896594783435, 13.98451010310800768, -0.8674368136027429399 ) ) ;
#12367=CARTESIAN_POINT ( 'NONE',  ( 1.914114187929045308, 18.25211889560055667, -0.4709243356944546322 ) ) ;
#12370=CARTESIAN_POINT ( 'NONE',  ( 5.510631153008393568, 13.48046023248279113, 7.984051925542015482 ) ) ;
#12376=CARTESIAN_POINT ( 'NONE',  ( 7.837419745790809245, 12.17652530823029622, 0.2379137956085111139 ) ) ;
#12379=CARTESIAN_POINT ( 'NONE',  ( 2.997723901089916154, 12.34803938479561758, 5.822245433047846142 ) ) ;
#12387=CARTESIAN_POINT ( 'NONE',  ( 1.476429774960471342, 21.14820369255740218, 3.937503551924574019 ) ) ;
#12390=CARTESIAN_POINT ( 'NONE',  ( 0.6684363650904089349, 20.56733048332889879, 6.164057930869264013 ) ) ;
#12396=CARTESIAN_POINT ( 'NONE',  ( 9.067351539292140217, 12.06055924076114216, -1.205741145043526030 ) ) ;
#12399=CARTESIAN_POINT ( 'NONE',  ( 13.35919779853531075, 14.07369424383953671, 6.735913025832823031 ) ) ;
#12404=CARTESIAN_POINT ( 'NONE',  ( 7.818102070580549068, 19.84329907872170651, -1.733884698244102518 ) ) ;
#12405=CARTESIAN_POINT ( 'NONE',  ( 3.971545295231272643, 12.81903963674880131, 0.8759281729739175626 ) ) ;
#12407=CARTESIAN_POINT ( 'NONE',  ( 5.845438114022948994, 12.70542626881843695, 0.3374892689872108220 ) ) ;
#12413=CARTESIAN_POINT ( 'NONE',  ( 9.648314893053726138, 12.91190710784102080, 6.796865775111411878 ) ) ;
#12415=CARTESIAN_POINT ( 'NONE',  ( 5.606983389587787414, 15.64107961637180289, 8.866323357916209957 ) ) ;
#12416=CARTESIAN_POINT ( 'NONE',  ( -0.1849527129589544072, 21.03045532914853055, 5.150944214860931680 ) ) ;
#12418=CARTESIAN_POINT ( 'NONE',  ( 5.025537597986745375, 20.64340025166658421, 2.222619301790576429 ) ) ;
#12425=CARTESIAN_POINT ( 'NONE',  ( 11.08308940409050081, 11.83732144666078590, 5.490605150716255878 ) ) ;
#12429=CARTESIAN_POINT ( 'NONE',  ( 11.14440184571222048, 15.20245592030993542, -3.461858056394771399 ) ) ;
#12430=CARTESIAN_POINT ( 'NONE',  ( 5.366014621799982010, 15.47125256599008480, -2.080610254137109649 ) ) ;
#12432=CARTESIAN_POINT ( 'NONE',  ( 1.756216822573207104, 20.47856574081302128, 4.951414795929986568 ) ) ;
#12442=CARTESIAN_POINT ( 'NONE',  ( 8.205998663303592622, 20.59028652745482191, 4.708363946724399618 ) ) ;
#12443=CARTESIAN_POINT ( 'NONE',  ( 5.638809941220587874, 13.98417111045325001, -0.8706810591892518714 ) ) ;
#12452=CARTESIAN_POINT ( 'NONE',  ( 11.14549571141843032, 18.39193805972417550, -4.149403309388357997 ) ) ;
#12456=CARTESIAN_POINT ( 'NONE',  ( 9.381874342791970633, 16.98982907235301454, -2.824620680285168994 ) ) ;
#12459=CARTESIAN_POINT ( 'NONE',  ( 4.947262131256387363, 17.41457342482845405, 8.526143230933524109 ) ) ;
#12471=CARTESIAN_POINT ( 'NONE',  ( 2.126660353523132319, 17.90725987158581134, 0.3359893863204973519 ) ) ;
#12473=CARTESIAN_POINT ( 'NONE',  ( 13.18855152120810459, 18.81300736124048001, 6.748715921887202818 ) ) ;
#12484=CARTESIAN_POINT ( 'NONE',  ( 0.7810342319177687731, 11.31615121391088152, 4.852052013636332539 ) ) ;
#12486=CARTESIAN_POINT ( 'NONE',  ( 5.458294004585774850, 13.09016006394465670, 7.706839728735500827 ) ) ;
#12501=CARTESIAN_POINT ( 'NONE',  ( 2.418915203433949834, 20.78401357429190099, 6.470070638013244668 ) ) ;
#12504=CARTESIAN_POINT ( 'NONE',  ( 4.881460237509400280, 11.69375961036644362, 3.716556164300745646 ) ) ;
#12510=CARTESIAN_POINT ( 'NONE',  ( 6.891132270267191551, 14.51543401643281150, -2.160190151449621787 ) ) ;
#12514=CARTESIAN_POINT ( 'NONE',  ( 12.83058271130599692, 11.15713451920434096, 4.225958205527430067 ) ) ;
#12519=CARTESIAN_POINT ( 'NONE',  ( 7.300797866228468713, 13.50249100423538096, -2.124842999382142494 ) ) ;
#12520=CARTESIAN_POINT ( 'NONE',  ( 2.532743019807210505, 12.01113885212942201, 3.567531869357724261 ) ) ;
#12522=CARTESIAN_POINT ( 'NONE',  ( 5.637115699025978088, 14.03407875391135207, -0.7791771547164595413 ) ) ;
#12525=CARTESIAN_POINT ( 'NONE',  ( 7.184449520472315776, 21.50782955549438213, 1.331064232565272398 ) ) ;
#12526=CARTESIAN_POINT ( 'NONE',  ( 4.940276686280794749, 12.24160006483127106, 5.425643334560562359 ) ) ;
#12529=CARTESIAN_POINT ( 'NONE',  ( 7.115319024147658489, 11.65893940570930276, 6.012375857502059162 ) ) ;
#12530=CARTESIAN_POINT ( 'NONE',  ( 1.585245561862221653, 17.17248089324893101, 9.542008508283084112 ) ) ;
#12532=CARTESIAN_POINT ( 'NONE',  ( 1.351641340660706847, 17.16051976808181578, 8.859800491581550475 ) ) ;
#12540=CARTESIAN_POINT ( 'NONE',  ( 9.585720859379199155, 11.37056570364833163, -0.8501006578359496801 ) ) ;
#12545=CARTESIAN_POINT ( 'NONE',  ( 11.18523345132915736, 14.07407650860021775, -3.067769628887059064 ) ) ;
#12546=CARTESIAN_POINT ( 'NONE',  ( 5.878563872623911557, 19.46939843988503682, -1.227892073574268217 ) ) ;
#12548=CARTESIAN_POINT ( 'NONE',  ( 2.108322636598648714, 12.53619568343860102, 2.181841141998187350 ) ) ;
#12554=CARTESIAN_POINT ( 'NONE',  ( 9.212431987401760836, 13.35013903698374094, 6.328237305530491241 ) ) ;
#12558=CARTESIAN_POINT ( 'NONE',  ( 4.490329389414642769, 20.73221372401878071, 6.369734200962422044 ) ) ;
#12562=CARTESIAN_POINT ( 'NONE',  ( 5.683261704384478641, 19.24102485395664175, -1.479744840059466826 ) ) ;
#12567=CARTESIAN_POINT ( 'NONE',  ( 9.298577761259569030, 15.72771140787512856, -2.821255160405396811 ) ) ;
#12568=CARTESIAN_POINT ( 'NONE',  ( -0.04547524747676359030, 20.22526626403869088, 5.510211994146467340 ) ) ;
#12569=CARTESIAN_POINT ( 'NONE',  ( 0.3230198289976083381, 19.99706093811970220, 2.158794779438429234 ) ) ;
#12576=CARTESIAN_POINT ( 'NONE',  ( 0.06040298848788722835, 14.32294367124328538, 1.330604002369546013 ) ) ;
#12590=CARTESIAN_POINT ( 'NONE',  ( 5.376318597655482812, 12.35012481907357973, 7.177346072766759733 ) ) ;
#12592=CARTESIAN_POINT ( 'NONE',  ( 4.758059951364139728, 11.14941623714734220, 4.549010102586493964 ) ) ;
#12601=CARTESIAN_POINT ( 'NONE',  ( 3.546339648969794922, 13.37831192441575645, 8.288436347218903322 ) ) ;
#12603=CARTESIAN_POINT ( 'NONE',  ( 2.000905577855156992, 14.11369167694475202, 8.640875553472284309 ) ) ;
#12610=CARTESIAN_POINT ( 'NONE',  ( 6.490961022597671715, 21.20305659848830260, 1.632485957150709321 ) ) ;
#12615=CARTESIAN_POINT ( 'NONE',  ( 12.24639129257385761, 10.40896227699137100, 1.778670804891760771 ) ) ;
#12619=CARTESIAN_POINT ( 'NONE',  ( 7.847767795464331897, 11.20922263031854094, 0.3967533504084792551 ) ) ;
#12623=CARTESIAN_POINT ( 'NONE',  ( 6.371911847424065911, 19.85835382792685877, 0.1381288362860780827 ) ) ;
#12624=CARTESIAN_POINT ( 'NONE',  ( 7.275815797620375669, 13.98176671473206056, 7.010075019451711853 ) ) ;
#12628=CARTESIAN_POINT ( 'NONE',  ( 9.179736842370099126, 21.96122921384184323, 1.647385027738300201 ) ) ;
#12633=CARTESIAN_POINT ( 'NONE',  ( 5.849665999842254216, 11.58475123937168050, 0.6023921236097111720 ) ) ;
#12636=CARTESIAN_POINT ( 'NONE',  ( -0.006835114654918546251, 15.70524387060945948, 0.7726394593941875444 ) ) ;
#12643=CARTESIAN_POINT ( 'NONE',  ( 9.882996518030738642, 10.80489496159325213, 0.4162864141824605402 ) ) ;
#12653=CARTESIAN_POINT ( 'NONE',  ( 10.38767455379903737, 20.34020649082646059, 4.891963057538385229 ) ) ;
#12655=CARTESIAN_POINT ( 'NONE',  ( 10.32478362973197861, 20.34432016293438039, 4.913735014817459223 ) ) ;
#12656=CARTESIAN_POINT ( 'NONE',  ( 2.391149987034691282, 11.90891113418242142, 1.713267630547372855 ) ) ;
#12661=CARTESIAN_POINT ( 'NONE',  ( 5.477890856393674568, 17.26865818392792562, 8.717832788898684626 ) ) ;
#12664=PRODUCT_DEFINITION_FORMATION_WITH_SPECIFIED_SOURCE ( 'ANY', '', #9124, .NOT_KNOWN. ) ;
#12668=CARTESIAN_POINT ( 'NONE',  ( 10.06365592863438962, 20.01297154863687311, -1.326460872188967022 ) ) ;
#12671=CARTESIAN_POINT ( 'NONE',  ( -0.3012801303904104055, 12.83134191367328292, 2.046756627941362261 ) ) ;
#12685=CARTESIAN_POINT ( 'NONE',  ( 11.21692919964015545, 18.39344551543875284, -4.174985455970938730 ) ) ;
#12694=CARTESIAN_POINT ( 'NONE',  ( 7.591324994831230022, 14.71783044265311702, 8.261316382108162770 ) ) ;
#12697=CARTESIAN_POINT ( 'NONE',  ( 4.013474518967609761, 11.67735946699760241, 1.345522051684508336 ) ) ;
#12702=CARTESIAN_POINT ( 'NONE',  ( 3.036164854790453393, 12.43340785568576301, 6.003854425968038200 ) ) ;
#12710=CARTESIAN_POINT ( 'NONE',  ( 2.181336132775622438, 11.71815103926796198, 2.193647000044615325 ) ) ;
#12714=CARTESIAN_POINT ( 'NONE',  ( 13.05797387958584821, 21.99054487380438871, 2.024989902501916905 ) ) ;
#12718=CARTESIAN_POINT ( 'NONE',  ( 8.988283004004445687, 14.76305577989238138, 7.604544232459095277 ) ) ;
#12723=CARTESIAN_POINT ( 'NONE',  ( 13.37108644572652771, 14.27456381540390673, 6.816450116726900710 ) ) ;
#12727=CARTESIAN_POINT ( 'NONE',  ( 7.447520878388439236, 12.50167464702338194, -1.386640270854869961 ) ) ;
#12728=CARTESIAN_POINT ( 'NONE',  ( 5.229630846777064690, 12.95116610613770369, 6.655177510049234968 ) ) ;
#12731=CARTESIAN_POINT ( 'NONE',  ( 6.405688018049387367, 19.93193575971154274, 0.2230809831250722963 ) ) ;
#12732=CARTESIAN_POINT ( 'NONE',  ( 7.232330221986995156, 13.58629969230393186, 6.749857871587612301 ) ) ;
#12734=CARTESIAN_POINT ( 'NONE',  ( 2.314778814167119059, 20.07314846742249514, 6.131468401820635350 ) ) ;
#12738=CARTESIAN_POINT ( 'NONE',  ( 5.864062336726267866, 19.24102485395664175, -1.533888344931878311 ) ) ;
#12740=CARTESIAN_POINT ( 'NONE',  ( 13.54865253201757724, 22.13033908681270390, 1.898565167770253970 ) ) ;
#12743=CARTESIAN_POINT ( 'NONE',  ( -0.2458537890374220825, 15.59650202059448354, 0.006824066329813496118 ) ) ;
#12744=CARTESIAN_POINT ( 'NONE',  ( 1.649085185276372156, 13.89508689931360763, 8.979946004438978946 ) ) ;
#12747=CARTESIAN_POINT ( 'NONE',  ( 4.556409632327232728, 11.78043576488526156, 3.812351442791019451 ) ) ;
#12754=CARTESIAN_POINT ( 'NONE',  ( 10.44642686154466382, 10.62307989687129961, 2.768800612658094629 ) ) ;
#12758=CARTESIAN_POINT ( 'NONE',  ( 12.38484231126942703, 20.96008087765395089, -0.8145651279088295116 ) ) ;
#12760=CARTESIAN_POINT ( 'NONE',  ( 5.365919581558607376, 15.46343705278112779, -2.079313974049490810 ) ) ;
#12766=CARTESIAN_POINT ( 'NONE',  ( 5.315554667604303951, 20.70596588439894603, 2.913411620298497873 ) ) ;
#12770=CARTESIAN_POINT ( 'NONE',  ( 10.19446762859863753, 11.43307009487834058, 0.3353791086218075312 ) ) ;
#12773=CARTESIAN_POINT ( 'NONE',  ( 9.325258829846921671, 14.88009260821627500, 7.099533925557936165 ) ) ;
#12778=CARTESIAN_POINT ( 'NONE',  ( 5.128092007265404817, 19.14636313803755385, 7.990005468057869820 ) ) ;
#12786=CARTESIAN_POINT ( 'NONE',  ( 9.643460259527261158, 18.64508862159060598, -2.339718049086865204 ) ) ;
#12788=CARTESIAN_POINT ( 'NONE',  ( 1.395580270598014927, 16.74552131709351954, 8.831485484237404648 ) ) ;
#12790=CARTESIAN_POINT ( 'NONE',  ( 1.158249747892080794, 14.11369167694475202, 8.893221684370338664 ) ) ;
#12793=ADVANCED_FACE ( 'NONE', ( #4641 ), #17612, .T. ) ;
#12804=CARTESIAN_POINT ( 'NONE',  ( 11.21434600409958549, 15.74974973885002250, 6.894954303353790337 ) ) ;
#12815=CARTESIAN_POINT ( 'NONE',  ( 6.867032585371679154, 20.09449018309318191, 7.026303756821641322 ) ) ;
#12818=CARTESIAN_POINT ( 'NONE',  ( 3.961642205674128281, 19.15682536790682633, -0.6604031723089509587 ) ) ;
#12823=CARTESIAN_POINT ( 'NONE',  ( 0.7634208374692786903, 12.21449189027183202, 4.858061345911853124 ) ) ;
#12826=CARTESIAN_POINT ( 'NONE',  ( 2.861593723304581616, 12.14881861375367755, 5.191963922796355213 ) ) ;
#12833=CARTESIAN_POINT ( 'NONE',  ( 3.650877847608121840, 15.06301662852333578, 9.047293290129529097 ) ) ;
#12837=CARTESIAN_POINT ( 'NONE',  ( 13.32162806899934893, 21.37707596500918683, 1.856000767176475552 ) ) ;
#12842=CARTESIAN_POINT ( 'NONE',  ( 12.03032088244432707, 10.82393886236346248, 2.770426701479023812 ) ) ;
#12845=CARTESIAN_POINT ( 'NONE',  ( 11.53638331813690954, 20.03120816360499745, -3.140810468174559222 ) ) ;
#12850=CARTESIAN_POINT ( 'NONE',  ( 7.216176021458938550, 15.38174918897333221, -2.804623791465954863 ) ) ;
#12854=CARTESIAN_POINT ( 'NONE',  ( 8.038529297171338683, 20.58475548577969150, 4.525697635533767027 ) ) ;
#12855=CARTESIAN_POINT ( 'NONE',  ( 2.817889642889978674, 19.15467982449370510, 7.378628536716077768 ) ) ;
#12857=CARTESIAN_POINT ( 'NONE',  ( 10.40160824207624124, 10.44972119249194087, 2.176742725712211612 ) ) ;
#12860=CARTESIAN_POINT ( 'NONE',  ( 4.982336563036975363, 11.34978398626420137, 5.629178714701890129 ) ) ;
#12861=CARTESIAN_POINT ( 'NONE',  ( 1.696998172421366080, 15.65649341095878455, 9.566233938423973626 ) ) ;
#12864=CARTESIAN_POINT ( 'NONE',  ( 1.586865396680246620, 15.70174598044015291, 8.856975764382001515 ) ) ;
#12870=CARTESIAN_POINT ( 'NONE',  ( 9.155526609938167582, 17.09045796635639647, -3.577556058969439956 ) ) ;
#12875=CARTESIAN_POINT ( 'NONE',  ( 5.708262345184669684, 12.06421266500533385, -0.1129897529190057592 ) ) ;
#12877=CARTESIAN_POINT ( 'NONE',  ( 4.018752164006647476, 18.69182423982057273, -0.1184710799488992716 ) ) ;
#12882=CARTESIAN_POINT ( 'NONE',  ( 9.503420364428157185, 13.29753225131360139, 6.313021545593930028 ) ) ;
#12898=CARTESIAN_POINT ( 'NONE',  ( 10.44085112785771940, 20.71911837938399970, -0.3471262034279907205 ) ) ;
#12900=CARTESIAN_POINT ( 'NONE',  ( 1.037299993275809129, 18.58659267166814999, 8.184560022580539496 ) ) ;
#12912=CARTESIAN_POINT ( 'NONE',  ( 0.4797181036071520022, 18.70046581331961377, 1.488109832587226400 ) ) ;
#12914=CARTESIAN_POINT ( 'NONE',  ( 13.04981212868784546, 13.21942167511952171, 5.527924531863672719 ) ) ;
#12916=CARTESIAN_POINT ( 'NONE',  ( 10.76563475082845045, 10.89862672135422095, 4.180636303131555209 ) ) ;
#12921=CARTESIAN_POINT ( 'NONE',  ( 6.937125200865347452, 11.28756208157694019, 5.042906767430812565 ) ) ;
#12927=CARTESIAN_POINT ( 'NONE',  ( 3.693057765962900696, 14.72322116853433194, 9.052632804461167026 ) ) ;
#12930=CARTESIAN_POINT ( 'NONE',  ( 3.966093002749460972, 11.78989785928834166, 1.136079879895026457 ) ) ;
#12934=CARTESIAN_POINT ( 'NONE',  ( 1.031545730800382143, 12.42199107967254612, 6.104814753628482471 ) ) ;
#12936=CARTESIAN_POINT ( 'NONE',  ( 4.271378093513435559, 12.07963554767070491, 2.399734011776157860 ) ) ;
#12942=CARTESIAN_POINT ( 'NONE',  ( 2.952410920574639164, 11.41616042669180153, 5.536812326145255980 ) ) ;
#12953=CARTESIAN_POINT ( 'NONE',  ( 11.13175442624480027, 11.34274383772578254, -1.019214542774232291 ) ) ;
#12956=CARTESIAN_POINT ( 'NONE',  ( 12.15966635475609436, 21.49276353786485316, -1.487043894966438629 ) ) ;
#12960=CARTESIAN_POINT ( 'NONE',  ( 8.530860809380452991, 21.37506940292296065, 0.1456188494152097501 ) ) ;
#12961=CARTESIAN_POINT ( 'NONE',  ( 6.953635458187449103, 20.71811460043715414, 1.644380932150268482 ) ) ;
#12962=CARTESIAN_POINT ( 'NONE',  ( 2.950444939269316613, 18.77528755091357482, 7.687626738347391075 ) ) ;
#12966=CARTESIAN_POINT ( 'NONE',  ( 0.4897477519866756390, 11.56708685249278190, 3.664773833674189518 ) ) ;
#12971=CARTESIAN_POINT ( 'NONE',  ( 3.277779626878584818, 17.95937840445101230, 8.190852587568969057 ) ) ;
#12977=CARTESIAN_POINT ( 'NONE',  ( 8.123211010957181344, 21.33440546750962241, 5.089800795509036746 ) ) ;
#12978=CARTESIAN_POINT ( 'NONE',  ( 10.47045210838663465, 21.61076908352683290, -0.3286064108336465561 ) ) ;
#12981=CARTESIAN_POINT ( 'NONE',  ( 11.45073599112340190, 18.47806154431882675, -3.160592916386676610 ) ) ;
#12982=CARTESIAN_POINT ( 'NONE',  ( 7.324935168321892398, 21.70618499363874321, 2.622908559674388407 ) ) ;
#12984=CARTESIAN_POINT ( 'NONE',  ( 4.869080998300100660, 18.75692939610809162, 7.455446531200784044 ) ) ;
#12986=CARTESIAN_POINT ( 'NONE',  ( 6.424002077374439068, 19.97927104947973476, 5.816179246968293803 ) ) ;
#12992=CARTESIAN_POINT ( 'NONE',  ( 8.941503686131628825, 19.69124030533750158, 6.014763436590002676 ) ) ;
#12993=CARTESIAN_POINT ( 'NONE',  ( 4.701704227727827146, 20.47280481670116359, 0.3545505907435208548 ) ) ;
#12997=CARTESIAN_POINT ( 'NONE',  ( 6.766171957887571864, 11.28156526743874188, 2.705201495196027039 ) ) ;
#13008=CARTESIAN_POINT ( 'NONE',  ( 10.76378183054590920, 21.07819761844824313, 0.5131835306795289320 ) ) ;
#13010=CARTESIAN_POINT ( 'NONE',  ( -0.1152391821539391209, 20.23795519954344613, 5.330493952060566976 ) ) ;
#13019=CARTESIAN_POINT ( 'NONE',  ( 11.11705324017706786, 16.27078922038442599, -3.687858511736137768 ) ) ;
#13021=CARTESIAN_POINT ( 'NONE',  ( 10.59745498212427073, 21.89042938493124169, 0.06821599229823353816 ) ) ;
#13034=CARTESIAN_POINT ( 'NONE',  ( 5.550556903167823464, 21.64685404058683815, 3.813055932019618677 ) ) ;
#13036=CARTESIAN_POINT ( 'NONE',  ( 3.815750765661552357, 12.28651131542703112, 0.4528471948513508871 ) ) ;
#13049=CARTESIAN_POINT ( 'NONE',  ( 2.278003711904815987, 11.54516833574618317, 2.618891172102409293 ) ) ;
#13060=CARTESIAN_POINT ( 'NONE',  ( 7.125560052436228808, 16.36585256730476701, -2.220941111682218416 ) ) ;
#13067=CARTESIAN_POINT ( 'NONE',  ( 8.695075460036933990, 19.30551093097031412, 6.194751677661820111 ) ) ;
#13071=CARTESIAN_POINT ( 'NONE',  ( 3.376984682214053013, 16.43012674869273582, 8.444289425429094109 ) ) ;
#13076=CARTESIAN_POINT ( 'NONE',  ( 0.6892992815739681367, 11.43080006335364374, 4.536020415443320353 ) ) ;
#13079=CARTESIAN_POINT ( 'NONE',  ( 1.458656339048537420, 17.15958586172077460, 8.823384646655476615 ) ) ;
#13086=CARTESIAN_POINT ( 'NONE',  ( 11.92979004589613190, 21.69514399574918073, 3.992311296994946801 ) ) ;
#13088=CARTESIAN_POINT ( 'NONE',  ( 9.121940360070944109, 13.82260832479536816, -3.046301295306517165 ) ) ;
#13090=CARTESIAN_POINT ( 'NONE',  ( 8.453759634856433891, 20.82441444446472190, 5.697268492166688958 ) ) ;
#13092=CARTESIAN_POINT ( 'NONE',  ( 2.854147253460158851, 19.21826933052950181, 7.434877585083132345 ) ) ;
#13098=CARTESIAN_POINT ( 'NONE',  ( 9.334231404058437320, 18.26872045576617865, 6.931657937804551750 ) ) ;
#13101=CARTESIAN_POINT ( 'NONE',  ( 3.873944326939889216, 13.69792732696330262, -0.8314339933664549598 ) ) ;
#13114=CARTESIAN_POINT ( 'NONE',  ( 11.78825387765158972, 20.99241592478037077, 3.275920435853647561 ) ) ;
#13125=CARTESIAN_POINT ( 'NONE',  ( 0.8312686293824771422, 19.60397523007529230, 2.320213228409029327 ) ) ;
#13129=CARTESIAN_POINT ( 'NONE',  ( 9.640329918106763429, 18.90712183571880090, -2.306490695281333547 ) ) ;
#13130=CARTESIAN_POINT ( 'NONE',  ( 2.873684328219870743, 20.03727096405572539, 2.085104636573927195 ) ) ;
#13133=CARTESIAN_POINT ( 'NONE',  ( 11.15539492206983319, 12.02330533696836135, 5.876692431811527229 ) ) ;
#13143=CARTESIAN_POINT ( 'NONE',  ( 1.155066700459650875, 21.11849136136308047, 3.338538337880277762 ) ) ;
#13147=CARTESIAN_POINT ( 'NONE',  ( 4.060856035186504620, 11.56482107470509213, 1.554964223477295127 ) ) ;
#13159=CARTESIAN_POINT ( 'NONE',  ( 1.966330561627286810, 12.33255769116432177, 1.219573196129033477 ) ) ;
#13170=CARTESIAN_POINT ( 'NONE',  ( 6.427231207988340245, 11.74208123617664157, 4.389945309724444300 ) ) ;
#13180=CARTESIAN_POINT ( 'NONE',  ( 8.201956413317519790, 11.59017961620675052, 1.867525178087086291 ) ) ;
#13181=CARTESIAN_POINT ( 'NONE',  ( 6.585538771758304932, 11.73707508029471214, 3.688088777089395087 ) ) ;
#13186=CARTESIAN_POINT ( 'NONE',  ( 1.702168628018286167, 14.88652389531085163, 9.403711407008401579 ) ) ;
#13189=CARTESIAN_POINT ( 'NONE',  ( 6.170897731235724493, 20.44464562225766358, 5.225896666988528949 ) ) ;
#13197=CARTESIAN_POINT ( 'NONE',  ( 11.32818978341159877, 13.68104675248728164, 7.112358373980030457 ) ) ;
#13199=CARTESIAN_POINT ( 'NONE',  ( 9.731254064506467572, 20.11182769301898077, -2.300494539041386677 ) ) ;
#13201=CARTESIAN_POINT ( 'NONE',  ( 8.972590385489363385, 19.47977362735880291, 7.032588333189179863 ) ) ;
#13203=CARTESIAN_POINT ( 'NONE',  ( 4.439494607601830012, 19.89361395305066083, 0.8919725944796629280 ) ) ;
#13209=CARTESIAN_POINT ( 'NONE',  ( 7.841140811635576746, 13.09203250846072208, -1.210482602502612970 ) ) ;
#13211=CARTESIAN_POINT ( 'NONE',  ( 5.639633595010457690, 12.41500460647656112, 7.037384739680620171 ) ) ;
#13214=CARTESIAN_POINT ( 'NONE',  ( 6.631720943421993475, 11.01939120177532239, 2.726317316095465682 ) ) ;
#13226=CARTESIAN_POINT ( 'NONE',  ( 12.85077078482076551, 12.25509064126621617, 4.452759652903010235 ) ) ;
#13228=CARTESIAN_POINT ( 'NONE',  ( 6.324617228969283467, 10.93918168731720186, 2.559496390996669923 ) ) ;
#13230=CARTESIAN_POINT ( 'NONE',  ( 1.042931226275107592, 13.09009564387116065, 7.664567888277438179 ) ) ;
#13235=CARTESIAN_POINT ( 'NONE',  ( 4.047143398541026116, 18.29642203768929676, -0.2535756372466432818 ) ) ;
#13241=CARTESIAN_POINT ( 'NONE',  ( 11.90016014395877342, 20.94917700551698303, 3.661585867165440433 ) ) ;
#13243=CARTESIAN_POINT ( 'NONE',  ( 6.758398147623775110, 11.05210752777782091, 4.476560998182233853 ) ) ;
#13249=CARTESIAN_POINT ( 'NONE',  ( 9.259384945965678071, 21.08603154913874178, 2.151121503098819332 ) ) ;
#13250=CARTESIAN_POINT ( 'NONE',  ( 6.065245546251053277, 11.11134465255707937, 1.342380378476411007 ) ) ;
#13256=CARTESIAN_POINT ( 'NONE',  ( -0.8081381244975988087, 20.81272068207762516, 3.752964682919363693 ) ) ;
#13259=CARTESIAN_POINT ( 'NONE',  ( 7.071627640836038786, 19.23017274739645899, 7.562272307646363600 ) ) ;
#13263=CARTESIAN_POINT ( 'NONE',  ( 1.069380478968006809, 12.49147184623710238, 6.284399451820561033 ) ) ;
#13267=CARTESIAN_POINT ( 'NONE',  ( 8.511781261342891369, 21.35551480289056059, -0.1885739448980535138 ) ) ;
#13269=PLANE ( 'NONE',  #11453 ) ;
#13271=CARTESIAN_POINT ( 'NONE',  ( 1.700472889415836741, 16.44472669448222746, -0.6926365997233963068 ) ) ;
#13280=CARTESIAN_POINT ( 'NONE',  ( 6.182380192748544445, 11.52015345895104126, 3.309294107830659470 ) ) ;
#13287=CARTESIAN_POINT ( 'NONE',  ( 7.966544624650091500, 11.88367076829663205, 0.8237426769557719686 ) ) ;
#13289=CARTESIAN_POINT ( 'NONE',  ( 3.153395120602799917, 17.97939181118854179, 8.120414267292568766 ) ) ;
#13294=CARTESIAN_POINT ( 'NONE',  ( -0.1894246789259524388, 15.61174044977811803, 0.09809569534440258642 ) ) ;
#13299=CARTESIAN_POINT ( 'NONE',  ( 0.7885908350430151925, 19.54577606275120161, 7.374915595215576047 ) ) ;
#13304=CARTESIAN_POINT ( 'NONE',  ( 11.03321510994558352, 12.31537751810604320, -2.946964147034912163 ) ) ;
#13306=CARTESIAN_POINT ( 'NONE',  ( 9.091854592231021215, 14.28828935598729011, -3.244019243948331521 ) ) ;
#13308=CARTESIAN_POINT ( 'NONE',  ( 9.171773708691890903, 18.63249697686906714, 7.499116223077195720 ) ) ;
#13310=CARTESIAN_POINT ( 'NONE',  ( 7.199757042754272973, 16.58762552368920851, 7.742064170688478519 ) ) ;
#13315=CARTESIAN_POINT ( 'NONE',  ( 6.756709577111620568, 20.37078616557504063, -0.1517828402666514531 ) ) ;
#13320=CARTESIAN_POINT ( 'NONE',  ( 6.487363973528258221, 10.93980350523859180, 2.763734740000318268 ) ) ;
#13329=CARTESIAN_POINT ( 'NONE',  ( 13.09702908948960598, 13.66552469702472017, 5.688823683958623256 ) ) ;
#13333=CARTESIAN_POINT ( 'NONE',  ( 6.748626741718993571, 18.34719479834194189, 7.834309874210196867 ) ) ;
#13336=CARTESIAN_POINT ( 'NONE',  ( -0.2842591080265123304, 20.23672349150513483, 5.180682693245175940 ) ) ;
#13344=CARTESIAN_POINT ( 'NONE',  ( 7.430732595839587340, 16.36411096495813311, -2.221128139217481756 ) ) ;
#13346=CARTESIAN_POINT ( 'NONE',  ( 10.94051986474393523, 19.57796819772926256, 6.737305449978185479 ) ) ;
#13350=CARTESIAN_POINT ( 'NONE',  ( 10.68002764719964937, 19.26684220934778935, 5.864093243101673458 ) ) ;
#13351=CARTESIAN_POINT ( 'NONE',  ( 10.64203227393771201, 21.88976505986162024, 0.05508552734995522671 ) ) ;
#13356=CARTESIAN_POINT ( 'NONE',  ( 4.496700024354473690, 10.96673477554678122, 3.844746723458174031 ) ) ;
#13359=CARTESIAN_POINT ( 'NONE',  ( 4.500494465692399082, 20.64052229378682313, 0.7001359311331863955 ) ) ;
#13363=CARTESIAN_POINT ( 'NONE',  ( 0.4297214030689984199, 12.52539863399390541, 3.302885710598653990 ) ) ;
#13367=CARTESIAN_POINT ( 'NONE',  ( 7.643032390518417429, 21.81816933872264030, 3.222994271250708032 ) ) ;
#13368=CARTESIAN_POINT ( 'NONE',  ( 4.228318371191494229, 12.14970637543461152, 2.202701631799199866 ) ) ;
#13371=CARTESIAN_POINT ( 'NONE',  ( 2.533239475727145695, 20.31455609140651219, 1.114995646245765748 ) ) ;
#13379=CARTESIAN_POINT ( 'NONE',  ( 9.244890676200823165, 13.73439867555944716, -2.211585914485044047 ) ) ;
#13380=CARTESIAN_POINT ( 'NONE',  ( -0.2988811684143778957, 21.11360319320700185, 4.764389704680555226 ) ) ;
#13385=CARTESIAN_POINT ( 'NONE',  ( 8.169479316132337132, 11.61242145201585352, 1.724731120145178043 ) ) ;
#13388=CARTESIAN_POINT ( 'NONE',  ( 3.164782767117006124, 17.92400674599301880, 8.142467647448141221 ) ) ;
#13392=CARTESIAN_POINT ( 'NONE',  ( 0.5982744427495542139, 20.03176192076531947, 1.619753041731076815 ) ) ;
#13399=CARTESIAN_POINT ( 'NONE',  ( 8.135493846614000546, 21.27400681123072346, -0.03209029099654438222 ) ) ;
#13401=CARTESIAN_POINT ( 'NONE',  ( 12.97983257214918851, 19.16628937045455316, 6.468072931972185913 ) ) ;
#13404=CARTESIAN_POINT ( 'NONE',  ( 6.159189550780465261, 20.31477451228112230, -0.5216155623760124760 ) ) ;
#13412=CARTESIAN_POINT ( 'NONE',  ( 9.830938833968739132, 14.76305577989238138, 7.352198101560677657 ) ) ;
#13417=CARTESIAN_POINT ( 'NONE',  ( 4.506322691401866365, 19.87799086262558035, 6.406845734523337832 ) ) ;
#13421=FILL_AREA_STYLE_COLOUR ( '', #7463 ) ;
#13423=CARTESIAN_POINT ( 'NONE',  ( 10.75023146982646516, 11.88040354724858538, 4.139699607910164225 ) ) ;
#13427=CARTESIAN_POINT ( 'NONE',  ( 12.72388782238154192, 11.86124722755734240, 3.874417171192698017 ) ) ;
#13431=CARTESIAN_POINT ( 'NONE',  ( 2.086806850236180733, 20.17421804741920255, 6.415940164516433342 ) ) ;
#13444=CARTESIAN_POINT ( 'NONE',  ( 13.05853762340243307, 13.21983372403380130, 5.524725199965593525 ) ) ;
#13445=CARTESIAN_POINT ( 'NONE',  ( 12.02314496290491874, 11.13213648998272198, 0.7539960825612619377 ) ) ;
#13447=CARTESIAN_POINT ( 'NONE',  ( 7.357671466288501883, 12.62844402333576177, -1.643692759918340851 ) ) ;
#13452=CARTESIAN_POINT ( 'NONE',  ( 9.775342085382558110, 20.91378398451936960, 3.534348224629963564 ) ) ;
#13453=CARTESIAN_POINT ( 'NONE',  ( 8.448737300149691265, 21.35108299968154455, -0.1673130223080695478 ) ) ;
#13459=CARTESIAN_POINT ( 'NONE',  ( 11.15182637456070580, 12.40253908811542161, -2.879831532321843302 ) ) ;
#13460=CARTESIAN_POINT ( 'NONE',  ( 3.820117857399456973, 19.12888530071778348, -0.7817677823692853467 ) ) ;
#13463=CARTESIAN_POINT ( 'NONE',  ( 7.281532115049993870, 18.28463547046064974, 8.039107993424838838 ) ) ;
#13473=CARTESIAN_POINT ( 'NONE',  ( 2.673620212570479104, 20.58160544162635119, 1.481323531626213663 ) ) ;
#13486=CARTESIAN_POINT ( 'NONE',  ( 8.438489806275660143, 20.62750485818692070, 0.2245734197965573720 ) ) ;
#13491=ORIENTED_EDGE ( 'NONE', *, *, #6432, .T. ) ;
#13492=CARTESIAN_POINT ( 'NONE',  ( 9.213875215811913932, 16.57205411493795211, 7.219289365333760422 ) ) ;
#13497=CARTESIAN_POINT ( 'NONE',  ( 3.428797585246498691, 14.99582101891923180, 8.235017481150693541 ) ) ;
#13503=CARTESIAN_POINT ( 'NONE',  ( 0.6940729559828254791, 20.23939374610027997, 1.864739730547348096 ) ) ;
#13506=CARTESIAN_POINT ( 'NONE',  ( 0.6866223815748832005, 18.62527059298248489, 1.150325187240316405 ) ) ;
#13515=CARTESIAN_POINT ( 'NONE',  ( 11.67896625218249618, 10.41612365926042116, 0.7535808997328219405 ) ) ;
#13517=CARTESIAN_POINT ( 'NONE',  ( 12.66021206568372115, 20.29409823522225054, 5.669750305148447467 ) ) ;
#13520=CARTESIAN_POINT ( 'NONE',  ( 9.447553535191925533, 16.53591467142064175, 7.981982076782735192 ) ) ;
#13522=CARTESIAN_POINT ( 'NONE',  ( 1.877778717054381152, 14.88408257588732653, 0.2291485109617275584 ) ) ;
#13527=CARTESIAN_POINT ( 'NONE',  ( 10.28864454875730594, 11.13211821786026157, 0.2008260053232651388 ) ) ;
#13528=CARTESIAN_POINT ( 'NONE',  ( 1.976491907247917013, 18.25402966388874049, -0.4944100302576455719 ) ) ;
#13532=CARTESIAN_POINT ( 'NONE',  ( 0.1888168487964103914, 20.17819236544972128, 6.192740200012695873 ) ) ;
#13539=CARTESIAN_POINT ( 'NONE',  ( 11.14979281629860353, 18.53988176718878478, 7.153212395691411096 ) ) ;
#13542=CARTESIAN_POINT ( 'NONE',  ( 12.94132309758686716, 17.97498947781735268, 6.146935883453322980 ) ) ;
#13544=CARTESIAN_POINT ( 'NONE',  ( 1.406064764339918005, 15.70174598044015291, 8.911119269253976682 ) ) ;
#13552=CARTESIAN_POINT ( 'NONE',  ( 11.98751445987246456, 11.13213648998272198, 0.7646661797260611015 ) ) ;
#13553=CARTESIAN_POINT ( 'NONE',  ( 3.329379522287787108, 20.49949451679308154, 3.262314715822274724 ) ) ;
#13556=CARTESIAN_POINT ( 'NONE',  ( 11.31768156113191814, 12.85014763714888097, -2.390818890651747353 ) ) ;
#13557=CARTESIAN_POINT ( 'NONE',  ( 4.619952123971384772, 11.64801722256006045, 1.999733552329578501 ) ) ;
#13558=CARTESIAN_POINT ( 'NONE',  ( 6.456273409070454328, 10.79806832651256165, 3.236992721971956311 ) ) ;
#13564=CARTESIAN_POINT ( 'NONE',  ( 9.062145815712636221, 21.02807274652383995, 1.621998221968902865 ) ) ;
#13565=CARTESIAN_POINT ( 'NONE',  ( 10.94235719458289502, 14.15760627606356081, -4.071005994705733322 ) ) ;
#13570=CARTESIAN_POINT ( 'NONE',  ( 11.15697610284867380, 12.37466090015357167, -2.855684010099386771 ) ) ;
#13571=CARTESIAN_POINT ( 'NONE',  ( -0.2379154757676318899, 12.59227895038538136, 1.809312566514052145 ) ) ;
#13574=CARTESIAN_POINT ( 'NONE',  ( 5.725800361066888833, 21.50854493894243191, 4.016541230030424181 ) ) ;
#13578=CARTESIAN_POINT ( 'NONE',  ( 0.2018155601342993544, 13.25506815275162253, 2.172332146088685079 ) ) ;
#13583=CARTESIAN_POINT ( 'NONE',  ( 3.903363043724838555, 13.16387888568485209, 0.6442466956650357846 ) ) ;
#13588=CARTESIAN_POINT ( 'NONE',  ( 1.788345386425812533, 17.37974145227866885, -0.6040922398381389780 ) ) ;
#13600=CARTESIAN_POINT ( 'NONE',  ( 6.737092676267780078, 12.02983150285682079, 4.801046767657766168 ) ) ;
#13601=CARTESIAN_POINT ( 'NONE',  ( 5.035740336155781982, 11.34978398626420137, 5.613186140933690282 ) ) ;
#13608=CARTESIAN_POINT ( 'NONE',  ( 9.137988923863366253, 13.24564614376286187, 6.127326076054989912 ) ) ;
#13610=CARTESIAN_POINT ( 'NONE',  ( 3.366847080470771747, 13.90270457291361161, 7.709217921812351548 ) ) ;
#13616=CARTESIAN_POINT ( 'NONE',  ( -0.1883589726742697090, 15.66015328560438391, 0.09064164159222751205 ) ) ;
#13619=CARTESIAN_POINT ( 'NONE',  ( 5.049881630641887220, 18.75692939610809162, 7.401303026328372781 ) ) ;
#13624=CARTESIAN_POINT ( 'NONE',  ( 14.14253296582467634, 21.25787525723532312, 4.279652095381059063 ) ) ;
#13626=CARTESIAN_POINT ( 'NONE',  ( 10.81036398341225713, 21.91646156000656021, 0.6078543174893448198 ) ) ;
#13630=CARTESIAN_POINT ( 'NONE',  ( 8.177763578858511906, 10.79888309947691205, 1.796606758151653604 ) ) ;
#13631=CARTESIAN_POINT ( 'NONE',  ( 2.400718128888100544, 20.09598732912352403, 6.282947492075177998 ) ) ;
#13638=CARTESIAN_POINT ( 'NONE',  ( 6.902807237671314766, 11.20245161629656039, 3.097827888567519228 ) ) ;
#13639=CARTESIAN_POINT ( 'NONE',  ( 5.318830492975814117, 13.90914350924470000, 7.343574724398199471 ) ) ;
#13640=CARTESIAN_POINT ( 'NONE',  ( 4.000918489741002837, 19.12888530071778348, -0.8359112872416241125 ) ) ;
#13643=CARTESIAN_POINT ( 'NONE',  ( 5.229160492742135347, 17.31893540436420764, 8.031536564559639046 ) ) ;
#13648=CARTESIAN_POINT ( 'NONE',  ( 9.093866485257809273, 21.83689553850923204, 1.689583340911293030 ) ) ;
#13651=CARTESIAN_POINT ( 'NONE',  ( 12.84502056709592033, 18.48422115218343009, 5.947007296923204400 ) ) ;
#13657=CARTESIAN_POINT ( 'NONE',  ( 4.584455248502485425, 19.89944416103447367, 1.015146957114681614 ) ) ;
#13663=CARTESIAN_POINT ( 'NONE',  ( 6.701167270133946197, 11.82549305421424179, 4.285450746564428037 ) ) ;
#13664=CARTESIAN_POINT ( 'NONE',  ( 3.783379877289300364, 20.55809296471286629, 4.452500340783561938 ) ) ;
#13665=CARTESIAN_POINT ( 'NONE',  ( 10.71277408803009124, 11.64784025693482228, 3.874468920058604215 ) ) ;
#13666=CARTESIAN_POINT ( 'NONE',  ( 7.591282571684015323, 18.34719479834194189, 7.581963743311560755 ) ) ;
#13667=CARTESIAN_POINT ( 'NONE',  ( 11.28984340714546697, 17.71682859275886557, 7.541597259675597797 ) ) ;
#13674=CARTESIAN_POINT ( 'NONE',  ( 9.882382622271025596, 20.81632985100941013, 3.819104690091920329 ) ) ;
#13675=CARTESIAN_POINT ( 'NONE',  ( 10.33786395622847820, 10.45470314796870248, 2.195665064187855897 ) ) ;
#13679=CARTESIAN_POINT ( 'NONE',  ( 3.278096675365355317, 13.69792732696330262, -0.6529983330018749310 ) ) ;
#13682=CARTESIAN_POINT ( 'NONE',  ( 7.136194838460433232, 11.81701620255667606, 6.040694753304580722 ) ) ;
#13690=CARTESIAN_POINT ( 'NONE',  ( 3.773036282072748993, 14.18962759126609186, -0.1098811704971767444 ) ) ;
#13694=CARTESIAN_POINT ( 'NONE',  ( 3.049180314527587310, 21.09804464240151134, 2.479317242939253596 ) ) ;
#13704=CARTESIAN_POINT ( 'NONE',  ( 11.14922546541893489, 15.75027095350177397, 6.909280940405325033 ) ) ;
#13706=CARTESIAN_POINT ( 'NONE',  ( 7.600020092372349545, 14.71802924512825683, 8.258015545363242893 ) ) ;
#13713=CARTESIAN_POINT ( 'NONE',  ( 7.457035429875517707, 14.48312770791961235, -1.753970211364317633 ) ) ;
#13718=CARTESIAN_POINT ( 'NONE',  ( 3.422385042412149136, 14.70423030993896774, 8.132674026271640599 ) ) ;
#13722=CARTESIAN_POINT ( 'NONE',  ( -0.1410424437649658302, 13.95926234754164597, 0.6541928679012153358 ) ) ;
#13730=CARTESIAN_POINT ( 'NONE',  ( 10.01244073014268920, 10.54134736952624252, 2.290216055019587138 ) ) ;
#13732=CARTESIAN_POINT ( 'NONE',  ( 12.07419610447281144, 21.48700711848800182, 4.104121981384611040 ) ) ;
#13740=CARTESIAN_POINT ( 'NONE',  ( 9.493382606263734758, 14.90386241890908181, 7.804904356304905200 ) ) ;
#13741=CARTESIAN_POINT ( 'NONE',  ( 0.2231702038951091094, 13.13563057234646081, 2.167777268876749819 ) ) ;
#13742=CARTESIAN_POINT ( 'NONE',  ( 6.123273286415696681, 11.97223630154925722, 1.629447004418834055 ) ) ;
#13743=CARTESIAN_POINT ( 'NONE',  ( 1.256988000113886894, 20.19907556228512391, 3.394663028293312568 ) ) ;
#13746=CARTESIAN_POINT ( 'NONE',  ( 9.794783782024321539, 14.67110634242510159, 7.680502800501443517 ) ) ;
#13747=CARTESIAN_POINT ( 'NONE',  ( 5.342884009753714025, 14.20367987736782034, 7.509086329562091322 ) ) ;
#13749=CARTESIAN_POINT ( 'NONE',  ( 4.478280779456667027, 20.54582653591270258, 0.3636022304821014961 ) ) ;
#13753=CARTESIAN_POINT ( 'NONE',  ( 0.7860029000012983547, 19.67029402086490109, 2.268881696640435042 ) ) ;
#13758=CARTESIAN_POINT ( 'NONE',  ( 8.775219136977288059, 21.64129978188946168, 0.8126495212682610658 ) ) ;
#13763=CARTESIAN_POINT ( 'NONE',  ( 12.37075837638908915, 11.27712503541973277, 2.326519893733080657 ) ) ;
#13765=CARTESIAN_POINT ( 'NONE',  ( 3.125990652992958641, 16.48662853297853914, 8.702465120992709302 ) ) ;
#13770=CARTESIAN_POINT ( 'NONE',  ( 6.118335074779962746, 11.59259103338027153, 2.921910985984132125 ) ) ;
#13772=CARTESIAN_POINT ( 'NONE',  ( 8.005991736905883727, 19.55876953988840228, -1.089244621163904192 ) ) ;
#13774=CARTESIAN_POINT ( 'NONE',  ( 8.949934402927555155, 12.18626401121546188, 5.089483566546638471 ) ) ;
#13775=CARTESIAN_POINT ( 'NONE',  ( 3.985841724706598921, 14.84625823140281753, 8.562040005760753303 ) ) ;
#13776=CARTESIAN_POINT ( 'NONE',  ( 12.90414695137542367, 11.26929059074382167, 4.646971329330398248 ) ) ;
#13782=CARTESIAN_POINT ( 'NONE',  ( 12.49492969781971397, 10.42866963796318025, 2.723955664945219013 ) ) ;
#13785=CARTESIAN_POINT ( 'NONE',  ( 10.27191476923467839, 11.36650105605588124, 2.042190157982642695 ) ) ;
#13789=CARTESIAN_POINT ( 'NONE',  ( 4.105856576153292359, 20.47280481670116359, 0.5329862511081018273 ) ) ;
#13792=CARTESIAN_POINT ( 'NONE',  ( 7.511152631442144845, 14.04345836577225093, 7.903093247502026131 ) ) ;
#13804=CARTESIAN_POINT ( 'NONE',  ( 5.183650323967657236, 18.93835688769866010, 8.121491601508173730 ) ) ;
#13816=CARTESIAN_POINT ( 'NONE',  ( 8.534517951019410020, 19.62664610146546096, 6.068736627783791526 ) ) ;
#13818=CARTESIAN_POINT ( 'NONE',  ( 5.894278812470819418, 11.58534598419692152, 0.5893802728092781829 ) ) ;
#13821=CARTESIAN_POINT ( 'NONE',  ( 5.398353993155480701, 12.72011693706338242, 7.404239398001607242 ) ) ;
#13826=CARTESIAN_POINT ( 'NONE',  ( 7.793721086304733703, 18.58975311028322963, -1.609092735773066440 ) ) ;
#13834=CARTESIAN_POINT ( 'NONE',  ( 2.981856859474616872, 19.70546197453703030, 7.926161949011188312 ) ) ;
#13837=CARTESIAN_POINT ( 'NONE',  ( 5.143049725565362884, 20.63862493749866189, 2.188920118661080938 ) ) ;
#13844=CARTESIAN_POINT ( 'NONE',  ( 9.540165638950465876, 10.83116634084218077, 0.3186190329235050744 ) ) ;
#13848=CARTESIAN_POINT ( 'NONE',  ( 12.26704403196416848, 21.18870809390503140, 4.628066114304389522 ) ) ;
#13855=CARTESIAN_POINT ( 'NONE',  ( 9.425811793576164277, 16.82642761605352888, 7.967843750810155612 ) ) ;
#13856=CARTESIAN_POINT ( 'NONE',  ( 2.468147855947524505, 19.25811192615784151, 1.016953072036343997 ) ) ;
#13858=CARTESIAN_POINT ( 'NONE',  ( 5.610206909946246157, 14.39083947916401662, -0.9654280252086245850 ) ) ;
#13861=CARTESIAN_POINT ( 'NONE',  ( 6.780578452629304920, 10.88474977364208129, 3.138707800202942710 ) ) ;
#13862=CARTESIAN_POINT ( 'NONE',  ( 5.103210221467147534, 12.69041179827479127, 6.197607713142090802 ) ) ;
#13866=CARTESIAN_POINT ( 'NONE',  ( 1.578497903329783236, 17.33698837102782520, 9.617339370494299544 ) ) ;
#13867=CARTESIAN_POINT ( 'NONE',  ( 0.9078720132265757359, 19.93072420684222124, 8.031871908601623034 ) ) ;
#13881=CARTESIAN_POINT ( 'NONE',  ( 9.071911524784843195, 21.82902542499374476, 1.628992493446408396 ) ) ;
#13883=CARTESIAN_POINT ( 'NONE',  ( 11.31520137981316410, 12.97204149252575611, -2.348193457568243492 ) ) ;
#13885=CARTESIAN_POINT ( 'NONE',  ( 6.724285126367631094, 12.26967076330688222, 5.725847290954301450 ) ) ;
#13890=CARTESIAN_POINT ( 'NONE',  ( 4.730636513238291485, 20.15959900865225762, 1.386152104603439073 ) ) ;
#13895=CARTESIAN_POINT ( 'NONE',  ( 11.32746420189878656, 18.10709300986449222, -3.412108001743339170 ) ) ;
#13896=CARTESIAN_POINT ( 'NONE',  ( 4.675198410806061133, 19.47349363154792812, 6.738369589952927896 ) ) ;
#13898=CARTESIAN_POINT ( 'NONE',  ( 7.466363098872039750, 16.36411096495813311, -2.231798236382281697 ) ) ;
#13899=CARTESIAN_POINT ( 'NONE',  ( 7.761792451437417029, 13.22675071421554094, 6.967738278329483670 ) ) ;
#13901=CARTESIAN_POINT ( 'NONE',  ( 5.306437989180502690, 15.44500604033330404, -2.180778496895487528 ) ) ;
#13908=CARTESIAN_POINT ( 'NONE',  ( 8.179209644894292808, 10.68807868122940263, 1.726742278678839337 ) ) ;
#13910=CARTESIAN_POINT ( 'NONE',  ( 10.56155824565360923, 11.55374880816059324, 3.303473780892424827 ) ) ;
#13914=CARTESIAN_POINT ( 'NONE',  ( 3.080897780363576643, 18.24815116393151015, 8.946422692470362037 ) ) ;
#13919=CARTESIAN_POINT ( 'NONE',  ( 0.03026019913916072612, 15.50729429995752007, 0.8891892028274968052 ) ) ;
#13938=CARTESIAN_POINT ( 'NONE',  ( 11.05478475839636232, 16.27078549497850091, -3.664008041822284678 ) ) ;
#13939=CARTESIAN_POINT ( 'NONE',  ( 3.030261223045108476, 19.78000251358870187, 7.990636196055694640 ) ) ;
#13942=CARTESIAN_POINT ( 'NONE',  ( 4.170163828269353168, 11.37233773221519151, 2.030869314271058101 ) ) ;
#13946=CARTESIAN_POINT ( 'NONE',  ( 7.601397047067438351, 17.55424594826779128, -1.993577623704449575 ) ) ;
#13947=MANIFOLD_SOLID_BREP ( 'Stock-MAS-676-1', #3239 ) ;
#13954=CARTESIAN_POINT ( 'NONE',  ( 2.706655912361267458, 20.34229411180381675, 7.226032060704281612 ) ) ;
#13957=CARTESIAN_POINT ( 'NONE',  ( 0.3171430137197577270, 15.65082615746288219, 0.2565623787687694723 ) ) ;
#13964=CARTESIAN_POINT ( 'NONE',  ( 7.123635696461563249, 18.22263143684711650, -2.172865895562870353 ) ) ;
#13966=CARTESIAN_POINT ( 'NONE',  ( 13.28239733708039338, 13.17358900937307098, 6.289479045720847594 ) ) ;
#13972=CARTESIAN_POINT ( 'NONE',  ( 9.026437793025710477, 11.56923703291080230, 5.398293960222889432 ) ) ;
#13973=CARTESIAN_POINT ( 'NONE',  ( 1.351254500901492683, 13.15556036664986195, 7.512915273831200835 ) ) ;
#13975=CARTESIAN_POINT ( 'NONE',  ( 5.961261165759633940, 18.61877392896656147, -0.8433191557062420518 ) ) ;
#13976=CARTESIAN_POINT ( 'NONE',  ( 7.107506517079237973, 17.78663461815678204, 7.406428215689759398 ) ) ;
#13979=CARTESIAN_POINT ( 'NONE',  ( 13.67197232725310130, 16.73453105516203721, 6.764297440454364541 ) ) ;
#13983=CARTESIAN_POINT ( 'NONE',  ( 2.795715374130701480, 20.92518826319738068, 1.845909576047056522 ) ) ;
#13984=CARTESIAN_POINT ( 'NONE',  ( 1.503723558945946115, 17.75019041696929278, 9.406929423142640800 ) ) ;
#13986=CARTESIAN_POINT ( 'NONE',  ( 1.306606356420245030, 13.15608644122636228, 7.525809141478054798 ) ) ;
#13991=CARTESIAN_POINT ( 'NONE',  ( 8.858306312843332364, 21.71400761653233147, 1.040450809158882661 ) ) ;
#13994=CARTESIAN_POINT ( 'NONE',  ( 11.17581378589971308, 16.27188659041726737, -3.588801592582428146 ) ) ;
#14000=CARTESIAN_POINT ( 'NONE',  ( 4.141737580667239627, 18.68175291836243090, -0.04791304144243380830 ) ) ;
#14004=CARTESIAN_POINT ( 'NONE',  ( 10.77600359882631764, 21.11368617580202312, 0.2706713370999587198 ) ) ;
#14006=CARTESIAN_POINT ( 'NONE',  ( 10.79498092501055950, 19.11273924176536099, 6.089322568971846650 ) ) ;
#14007=CARTESIAN_POINT ( 'NONE',  ( 4.076791092353339252, 13.85370291750471772, -0.6031074348338666402 ) ) ;
#14008=CARTESIAN_POINT ( 'NONE',  ( 12.45036876921160029, 10.42934933986260049, 2.737140771311291410 ) ) ;
#14013=CARTESIAN_POINT ( 'NONE',  ( 5.472929299800822101, 17.41108386104152572, -2.181338777335867452 ) ) ;
#14016=CARTESIAN_POINT ( 'NONE',  ( 9.581330595514776505, 12.45782188202256258, -1.022525368604570772 ) ) ;
#14019=CARTESIAN_POINT ( 'NONE',  ( 0.3421348966474949682, 11.72126458219154266, 4.984374349806848237 ) ) ;
#14022=CARTESIAN_POINT ( 'NONE',  ( 0.000000000000000000, 0.000000000000000000, 0.000000000000000000 ) ) ;
#14025=VERTEX_POINT ( 'NONE', #2241 ) ;
#14042=CARTESIAN_POINT ( 'NONE',  ( 6.135032277701231607, 11.87301092205614061, 1.607754465602344141 ) ) ;
#14043=CARTESIAN_POINT ( 'NONE',  ( 4.186481793393173056, 11.26694048801452119, 1.988198107626873101 ) ) ;
#14046=CARTESIAN_POINT ( 'NONE',  ( 4.268749360096856016, 11.23597362958910217, 2.456883663558785180 ) ) ;
#14052=CARTESIAN_POINT ( 'NONE',  ( 7.440635613041443719, 15.33804443884177893, -2.014925911322226426 ) ) ;
#14053=CARTESIAN_POINT ( 'NONE',  ( 1.446457749880594168, 14.21890420874361638, 8.282590212535712482 ) ) ;
#14058=CARTESIAN_POINT ( 'NONE',  ( 3.346841482731536921, 18.37601729971541786, 8.783708127353060391 ) ) ;
#14061=CARTESIAN_POINT ( 'NONE',  ( 3.984298728599178219, 15.55943979790526122, -0.8574646732594534138 ) ) ;
#14067=CARTESIAN_POINT ( 'NONE',  ( 10.89219221246175273, 13.86399106732309328, 6.860601030035128112 ) ) ;
#14069=CARTESIAN_POINT ( 'NONE',  ( 11.51479575839695180, 11.09863041152549279, -1.273237637403870526 ) ) ;
#14074=CARTESIAN_POINT ( 'NONE',  ( 7.336019681823533922, 17.38139003493714796, -2.801635840538051259 ) ) ;
#14075=CARTESIAN_POINT ( 'NONE',  ( 2.476888523641526341, 19.25858774544496299, 1.013804407051679402 ) ) ;
#14077=CARTESIAN_POINT ( 'NONE',  ( 5.634997990689105229, 16.47394368154384381, -1.394772957107783151 ) ) ;
#14080=CARTESIAN_POINT ( 'NONE',  ( 7.524408825705059201, 14.40990712224419745, -2.662676755242683324 ) ) ;
#14081=CARTESIAN_POINT ( 'NONE',  ( 4.735151946278128854, 11.94990942969003633, 4.489362985911736104 ) ) ;
#14084=CARTESIAN_POINT ( 'NONE',  ( 5.623058703637103584, 21.64257598718208442, 3.791041185262803204 ) ) ;
#14087=CARTESIAN_POINT ( 'NONE',  ( 0.4365749149366086046, 12.38306287928572047, 3.436918907366315334 ) ) ;
#14094=CARTESIAN_POINT ( 'NONE',  ( 10.67791946166693151, 10.86254514955002115, 3.740422676341600194 ) ) ;
#14099=CARTESIAN_POINT ( 'NONE',  ( 12.27210225253973341, 11.22090649283593145, 1.901844011543860624 ) ) ;
#14100=CARTESIAN_POINT ( 'NONE',  ( 6.053300999215300848, 11.21400605080730095, 1.403379422147501998 ) ) ;
#14109=CARTESIAN_POINT ( 'NONE',  ( 13.22401121011497871, 16.70014932840746980, 6.472590397630748171 ) ) ;
#14110=CARTESIAN_POINT ( 'NONE',  ( 8.050360878220200078, 19.55923767994525875, -1.103070160109182796 ) ) ;
#14118=CARTESIAN_POINT ( 'NONE',  ( 13.28158503003489521, 12.74059347184058133, 6.139893691599064951 ) ) ;
#14122=CARTESIAN_POINT ( 'NONE',  ( 9.328167723008592205, 14.17953533357325213, -2.361609774951227703 ) ) ;
#14128=CARTESIAN_POINT ( 'NONE',  ( 3.234135262388317056, 13.85370291750471772, -0.3507613039352304729 ) ) ;
#14131=CARTESIAN_POINT ( 'NONE',  ( 6.722042540637936270, 11.03467657806808155, 4.243594125539606132 ) ) ;
#14154=CARTESIAN_POINT ( 'NONE',  ( 3.571986513017807230, 13.65508413018860168, -0.8205120656026146930 ) ) ;
#14157=CARTESIAN_POINT ( 'NONE',  ( 5.560588701018165381, 14.03900692732092637, 8.286612247724049141 ) ) ;
#14161=CARTESIAN_POINT ( 'NONE',  ( 1.307674456180993205, 13.22153521441935631, 7.464550839006347083 ) ) ;
#14169=CARTESIAN_POINT ( 'NONE',  ( 1.241553966568222478, 21.00182112902565024, 3.306851382610512147 ) ) ;
#14173=CARTESIAN_POINT ( 'NONE',  ( 5.279151643709653285, 18.80848272075206040, 7.411774736893618432 ) ) ;
#14175=CARTESIAN_POINT ( 'NONE',  ( 13.17913432789424455, 22.09378701703648318, 2.003858574039297125 ) ) ;
#14179=CARTESIAN_POINT ( 'NONE',  ( 8.053807618826375858, 20.99150983053873887, 0.1441728028981547893 ) ) ;
#14183=CARTESIAN_POINT ( 'NONE',  ( 13.32555521554802347, 13.59179201149856731, 6.524269766134250581 ) ) ;
#14187=CARTESIAN_POINT ( 'NONE',  ( 7.217504064768158756, 15.13630231636019907, -2.750538542655735164 ) ) ;
#14188=CARTESIAN_POINT ( 'NONE',  ( 6.711813954139214111, 19.52167825130506174, 6.475648147207831329 ) ) ;
#14190=CARTESIAN_POINT ( 'NONE',  ( 5.672450816875850066, 16.90457802579262392, -1.372803282523601842 ) ) ;
#14194=CARTESIAN_POINT ( 'NONE',  ( 11.44906460655527347, 16.27109148020024776, -4.209446567205482381 ) ) ;
#14196=CARTESIAN_POINT ( 'NONE',  ( 1.449957865217590181, 12.54475284465800300, 8.036837038674857325 ) ) ;
#14200=CARTESIAN_POINT ( 'NONE',  ( 2.821159705543409668, 12.03350028468612010, 5.087159923345644152 ) ) ;
#14208=CARTESIAN_POINT ( 'NONE',  ( 11.23769815086176038, 12.55470729765644577, 6.205490070020298177 ) ) ;
#14212=CARTESIAN_POINT ( 'NONE',  ( 11.58533050013644861, 11.88887413582774499, -1.080035739352499746 ) ) ;
#14213=CARTESIAN_POINT ( 'NONE',  ( 5.440803762682732803, 16.93165822604456494, -2.129577970569525913 ) ) ;
#14215=CARTESIAN_POINT ( 'NONE',  ( 3.362212792910313830, 14.97059756667285058, 8.341616412569205607 ) ) ;
#14221=CARTESIAN_POINT ( 'NONE',  ( 12.51631392633175821, 11.22339177084746176, 2.531244740403540749 ) ) ;
#14222=CARTESIAN_POINT ( 'NONE',  ( 10.14492818048215383, 20.26472116815758184, -1.210351513573973081 ) ) ;
#14223=CARTESIAN_POINT ( 'NONE',  ( 2.768558239392996612, 11.29961739780916119, 3.368077172965935784 ) ) ;
#14229=CARTESIAN_POINT ( 'NONE',  ( 3.780217353292837590, 21.35532275365758892, 4.459463005498162325 ) ) ;
#14233=CARTESIAN_POINT ( 'NONE',  ( 9.847866323654898224, 10.74839508995118109, 0.1972236645847412484 ) ) ;
#14237=CARTESIAN_POINT ( 'NONE',  ( 9.298361730296520022, 14.82474458426707287, -2.615784524909192221 ) ) ;
#14239=CARTESIAN_POINT ( 'NONE',  ( 0.9969110339907100160, 18.71640230995546617, 8.094414359749949384 ) ) ;
#14240=CARTESIAN_POINT ( 'NONE',  ( 1.573239863039354036, 18.09708922108623241, 0.02106776903118079761 ) ) ;
#14250=ORIENTED_EDGE ( 'NONE', *, *, #6255, .T. ) ;
#14262=CARTESIAN_POINT ( 'NONE',  ( 0.3901958476314392743, 11.62494085263212185, 3.152395423529554819 ) ) ;
#14265=CARTESIAN_POINT ( 'NONE',  ( 5.037610691315365763, 11.52515137269489287, 5.758083063193782714 ) ) ;
#14270=CARTESIAN_POINT ( 'NONE',  ( 1.463311253929418410, 14.47771670469544247, 8.418734608934853370 ) ) ;
#14273=CARTESIAN_POINT ( 'NONE',  ( 2.788510799092093428, 12.08762853899515655, 4.857404785327848806 ) ) ;
#14280=CARTESIAN_POINT ( 'NONE',  ( 3.373764802772109661, 18.23923658461143660, 8.840318433877319748 ) ) ;
#14282=CARTESIAN_POINT ( 'NONE',  ( 1.184790726613003997, 11.72126458219154266, 4.732028218908065575 ) ) ;
#14287=CARTESIAN_POINT ( 'NONE',  ( 13.92088304628949835, 21.18286304486736427, 4.294626054287162376 ) ) ;
#14290=CARTESIAN_POINT ( 'NONE',  ( 12.49114903281414435, 10.57457003121523265, 2.794588968605982160 ) ) ;
#14294=CARTESIAN_POINT ( 'NONE',  ( 8.060400974142371666, 10.89137254501747165, 1.302109054530725452 ) ) ;
#14295=CARTESIAN_POINT ( 'NONE',  ( 4.134645168753052324, 18.69448487464559250, -0.1575769768225616096 ) ) ;
#14298=CARTESIAN_POINT ( 'NONE',  ( 6.980081620662553554, 20.74003334725626857, 1.714263682474118200 ) ) ;
#14303=CARTESIAN_POINT ( 'NONE',  ( 7.941166293774544194, 20.10612899863186342, -1.699484797600306685 ) ) ;
#14306=CARTESIAN_POINT ( 'NONE',  ( 7.257894689705208791, 18.51518438473548045, 8.066618968152379665 ) ) ;
#14307=CARTESIAN_POINT ( 'NONE',  ( 0.4987414016220624857, 20.62897293350240346, 6.972998423300798443 ) ) ;
#14309=CARTESIAN_POINT ( 'NONE',  ( -0.6625952780925900010, 20.05113242023052322, 3.974854857413083309 ) ) ;
#14315=CARTESIAN_POINT ( 'NONE',  ( 10.20092691626072501, 10.57410012085601281, 1.745687182084074029 ) ) ;
#14318=CARTESIAN_POINT ( 'NONE',  ( 12.01826200721117921, 20.34182557837260674, -1.780941468847173637 ) ) ;
#14319=CARTESIAN_POINT ( 'NONE',  ( 6.055248116062193375, 11.21101810703654245, 1.411743302974689307 ) ) ;
#14321=CARTESIAN_POINT ( 'NONE',  ( 1.812277707583389574, 16.41892220718292705, 0.009655869164628197443 ) ) ;
#14327=CARTESIAN_POINT ( 'NONE',  ( 9.021865827675320304, 12.18989644830414321, 5.065564172291198375 ) ) ;
#14328=CARTESIAN_POINT ( 'NONE',  ( 4.895015545045986904, 18.85334257715032891, 7.259427143975731411 ) ) ;
#14329=CARTESIAN_POINT ( 'NONE',  ( 6.431837864969753404, 20.04762713518370276, 0.1993235301662593661 ) ) ;
#14332=CARTESIAN_POINT ( 'NONE',  ( 5.321178521759295066, 18.30337503607197647, 8.427072287543769136 ) ) ;
#14335=CARTESIAN_POINT ( 'NONE',  ( 12.85747229756767318, 22.28580575005450370, 0.3837689773447273134 ) ) ;
#14340=CARTESIAN_POINT ( 'NONE',  ( 9.849116944258051731, 19.41443847587203564, -1.859163645420073285 ) ) ;
#14343=CARTESIAN_POINT ( 'NONE',  ( 1.435485551437910345, 20.88642215721691997, 5.084564560294345448 ) ) ;
#14355=CARTESIAN_POINT ( 'NONE',  ( 11.00471620700651698, 14.15586088870902515, -4.094554156936994538 ) ) ;
#14364=CARTESIAN_POINT ( 'NONE',  ( 0.06131086484389459967, 12.52652910124526109, 1.659618942007908604 ) ) ;
#14367=CARTESIAN_POINT ( 'NONE',  ( 3.782569706950912991, 18.34578091050401838, -1.064631198517248967 ) ) ;
#14373=CARTESIAN_POINT ( 'NONE',  ( 3.098003633530906686, 12.58238514230527194, 6.297671215640997744 ) ) ;
#14378=CARTESIAN_POINT ( 'NONE',  ( 2.429351595637148975, 11.35538272796713244, 3.277950258183725207 ) ) ;
#14388=CARTESIAN_POINT ( 'NONE',  ( 12.13064228076788176, 20.23326750546686270, 5.472641854910515136 ) ) ;
#14392=CARTESIAN_POINT ( 'NONE',  ( 11.45377137136283530, 11.24886065122903211, -1.534485868486173521 ) ) ;
#14397=CARTESIAN_POINT ( 'NONE',  ( 7.227849133945657201, 15.88119260777969366, -2.864944999438480799 ) ) ;
#14398=CARTESIAN_POINT ( 'NONE',  ( 5.282564265860938413, 17.31893540436420764, 8.015543990791440976 ) ) ;
#14400=CARTESIAN_POINT ( 'NONE',  ( 8.519789844685428548, 19.76956797718314007, 5.764066944484178556 ) ) ;
#14403=CARTESIAN_POINT ( 'NONE',  ( 9.146683264432596161, 11.49625537507852080, 5.482365255748488764 ) ) ;
#14406=CARTESIAN_POINT ( 'NONE',  ( 0.3457492210648637210, 11.62559268301756177, 3.165962217078898799 ) ) ;
#14407=CARTESIAN_POINT ( 'NONE',  ( 1.703304774440397296, 15.10408740295005714, 9.458727078297481938 ) ) ;
#14409=CARTESIAN_POINT ( 'NONE',  ( 5.951959548518082954, 12.27588422369934129, 0.9763157611141449754 ) ) ;
#14417=CARTESIAN_POINT ( 'NONE',  ( 11.14903082554621605, 12.11221548192478004, 5.790615822781773225 ) ) ;
#14420=CARTESIAN_POINT ( 'NONE',  ( 12.08799520445995945, 20.48566632575741764, -1.599630408105054746 ) ) ;
#14422=CARTESIAN_POINT ( 'NONE',  ( 5.856409722658628247, 11.60590070312898092, 0.5491629594515322621 ) ) ;
#14426=CARTESIAN_POINT ( 'NONE',  ( 6.000401609189997210, 20.54164716138263813, 4.721118242335392345 ) ) ;
#14429=CARTESIAN_POINT ( 'NONE',  ( 9.844264539218293919, 12.30663295771102383, -1.228584621700786306 ) ) ;
#14430=CARTESIAN_POINT ( 'NONE',  ( 6.971783283983191026, 20.81512969834162163, 1.607819997509327692 ) ) ;
#14431=CARTESIAN_POINT ( 'NONE',  ( 3.283575605484034821, 19.71984925633132235, 7.849616204200203562 ) ) ;
#14442=CARTESIAN_POINT ( 'NONE',  ( 11.30859256852448347, 21.24860540534560016, 1.983546970420978939 ) ) ;
#14444=CARTESIAN_POINT ( 'NONE',  ( 0.08608646803520518531, 20.17500070246044075, 5.848371221736313075 ) ) ;
#14446=CARTESIAN_POINT ( 'NONE',  ( -0.7373233266190051260, 20.71056957386564079, 4.930574937443840788 ) ) ;
#14454=CARTESIAN_POINT ( 'NONE',  ( 0.5053304282907709055, 18.78275443002634759, 1.545950046922383025 ) ) ;
#14457=CARTESIAN_POINT ( 'NONE',  ( 12.86047607407836324, 18.46447794879854243, 6.079284020093307817 ) ) ;
#14458=CARTESIAN_POINT ( 'NONE',  ( 2.418392266879479724, 19.05216738376148911, 0.9656792871569455095 ) ) ;
#14459=CARTESIAN_POINT ( 'NONE',  ( 11.21401574228518427, 12.31537751810604320, -3.001107651909319607 ) ) ;
#14469=CARTESIAN_POINT ( 'NONE',  ( 3.929373626785105600, 19.12659651351990320, -0.8107010527169089542 ) ) ;
#14473=CARTESIAN_POINT ( 'NONE',  ( 3.950319039265778986, 19.11221838521101546, -0.6870736532921090101 ) ) ;
#14478=CARTESIAN_POINT ( 'NONE',  ( 0.8869166634311153041, 12.25464994366603122, 5.429115086724404016 ) ) ;
#14485=CARTESIAN_POINT ( 'NONE',  ( 2.832812540163568649, 11.30610737436141200, 5.018348456016711090 ) ) ;
#14490=CARTESIAN_POINT ( 'NONE',  ( 13.00571045122730851, 21.87905377962147213, 2.024278336491688535 ) ) ;
#14494=CARTESIAN_POINT ( 'NONE',  ( 7.707318447941210238, 19.61749303057682070, -1.067354726136881427 ) ) ;
#14498=CARTESIAN_POINT ( 'NONE',  ( 11.08491485109335351, 17.82867876252078432, -4.185153311738524451 ) ) ;
#14502=CARTESIAN_POINT ( 'NONE',  ( 7.261604238741163897, 13.94690558326506746, -2.355022785685753739 ) ) ;
#14506=CARTESIAN_POINT ( 'NONE',  ( 6.388697458777018667, 19.89557336115347397, 0.1802627198813876175 ) ) ;
#14510=CARTESIAN_POINT ( 'NONE',  ( 5.544310973761614747, 17.41197255053186055, -2.207093946540664042 ) ) ;
#14514=CARTESIAN_POINT ( 'NONE',  ( 0.9415645308267408531, 11.48439724119077177, 5.634514928165719638 ) ) ;
#14520=CARTESIAN_POINT ( 'NONE',  ( 5.034481523711040296, 20.64273285859446361, 2.220149373443666807 ) ) ;
#14527=CARTESIAN_POINT ( 'NONE',  ( 10.79394434136722225, 11.05572186037332294, 4.232501299144526996 ) ) ;
#14532=CARTESIAN_POINT ( 'NONE',  ( 5.627668837156483583, 18.34364325301588394, -1.803485302817334546 ) ) ;
#14534=CARTESIAN_POINT ( 'NONE',  ( 6.586789902921174722, 11.71523883824356282, 4.117049529868094027 ) ) ;
#14539=CARTESIAN_POINT ( 'NONE',  ( 11.69938498582200914, 11.70279650494946289, -0.9857855139570842473 ) ) ;
#14555=CARTESIAN_POINT ( 'NONE',  ( 12.23193311121828586, 20.35868270965967852, 4.448204119538093693 ) ) ;
#14556=CARTESIAN_POINT ( 'NONE',  ( 1.459005598626311073, 16.01352310531106937, 8.842019805628964946 ) ) ;
#14558=CARTESIAN_POINT ( 'NONE',  ( -1.111594454113435715, 19.92362218466222146, 3.626275517597432607 ) ) ;
#14576=CARTESIAN_POINT ( 'NONE',  ( 11.18302750797556655, 14.04470801367943267, 6.395837339788904785 ) ) ;
#14577=CARTESIAN_POINT ( 'NONE',  ( 2.716457121344570069, 19.77266525423434729, 1.688395397584657953 ) ) ;
#14578=CARTESIAN_POINT ( 'NONE',  ( 8.772911046456378870, 20.20056482616064031, 6.600680312436005615 ) ) ;
#14591=CARTESIAN_POINT ( 'NONE',  ( 2.831345877163882196, 20.92518826319738068, 1.835239478882038977 ) ) ;
#14594=CARTESIAN_POINT ( 'NONE',  ( 3.878576562893467194, 12.05861442832895669, 0.7413939759094347881 ) ) ;
#14599=CARTESIAN_POINT ( 'NONE',  ( 2.613241785389884608, 12.04565783673474577, 4.059156808520036464 ) ) ;
#14601=CARTESIAN_POINT ( 'NONE',  ( 4.412770401086850924, 11.92270407980696589, 3.040133244938206136 ) ) ;
#14607=CARTESIAN_POINT ( 'NONE',  ( 3.146901756478003964, 11.73978298677764265, 6.391159807765457224 ) ) ;
#14617=CARTESIAN_POINT ( 'NONE',  ( 11.21717328838213135, 19.98250042233096124, -2.706654341015993115 ) ) ;
#14620=CARTESIAN_POINT ( 'NONE',  ( 12.10902647966340417, 21.41074805268790371, -1.624989011717251186 ) ) ;
#14624=CARTESIAN_POINT ( 'NONE',  ( 8.344319702060484900, 21.09743033546479296, -0.3585062597797421535 ) ) ;
#14626=CARTESIAN_POINT ( 'NONE',  ( 7.629991675630842352, 20.88079669329302135, 3.443698988702693864 ) ) ;
#14627=CARTESIAN_POINT ( 'NONE',  ( 6.993352728955766651, 12.42634065549329314, 5.540270479366993683 ) ) ;
#14634=CARTESIAN_POINT ( 'NONE',  ( 2.976857449924355858, 19.78000251358870187, 8.006628769824478908 ) ) ;
#14635=CARTESIAN_POINT ( 'NONE',  ( 1.673502052647580118, 16.21230766891936170, 9.615316047918000208 ) ) ;
#14638=CARTESIAN_POINT ( 'NONE',  ( 4.104074918077325052, 20.52844081774288298, 5.032055296311012782 ) ) ;
#14644=CARTESIAN_POINT ( 'NONE',  ( 9.075928832518638245, 15.79855474736653598, -3.595103111437136345 ) ) ;
#14648=CARTESIAN_POINT ( 'NONE',  ( 8.218573335227386423, 21.19769852377196173, 5.067010135336594168 ) ) ;
#14650=CARTESIAN_POINT ( 'NONE',  ( 1.515498579774128496, 15.70115217790233508, 8.882780545536347105 ) ) ;
#14657=CARTESIAN_POINT ( 'NONE',  ( 6.778227844323079232, 11.52015345895104126, 3.130858447466078331 ) ) ;
#14660=CARTESIAN_POINT ( 'NONE',  ( 3.633311392490445879, 13.11091270743887982, 8.194468062865079006 ) ) ;
#14663=CARTESIAN_POINT ( 'NONE',  ( 6.570055536094496773, 11.67239202316484104, 2.792470343458694604 ) ) ;
#14673=CARTESIAN_POINT ( 'NONE',  ( 11.70990690266660295, 21.06271108513744394, 3.065845505830564477 ) ) ;
#14675=CARTESIAN_POINT ( 'NONE',  ( 0.1479864323037562990, 20.14003584071202013, 6.007153626829540904 ) ) ;
#14687=CARTESIAN_POINT ( 'NONE',  ( 10.27137985661365960, 20.34432016293438039, 4.929727588585513409 ) ) ;
#14690=CARTESIAN_POINT ( 'NONE',  ( 11.95563672222081841, 10.32956393789710070, 0.6582173057821769646 ) ) ;
#14703=CARTESIAN_POINT ( 'NONE',  ( 3.541852216381984331, 16.52290265193734342, 9.336019329946809719 ) ) ;
#14706=CARTESIAN_POINT ( 'NONE',  ( 3.742561817426398374, 18.11868962831785268, -1.147007223846213897 ) ) ;
#14715=CARTESIAN_POINT ( 'NONE',  ( 3.002670853353920588, 11.48192359107278193, 5.755866358288438178 ) ) ;
#14718=CARTESIAN_POINT ( 'NONE',  ( 13.19325985535186874, 21.42039298163480154, 1.900799873352047475 ) ) ;
#14725=CARTESIAN_POINT ( 'NONE',  ( 13.74851850464161807, 20.92287966070258065, 4.168088350112811646 ) ) ;
#14727=CARTESIAN_POINT ( 'NONE',  ( 10.92875438672132127, 14.66671681640350222, -4.110811315144232481 ) ) ;
#14731=CARTESIAN_POINT ( 'NONE',  ( 7.582094801143906437, 20.89590603020118209, 3.316103915199458463 ) ) ;
#14732=CARTESIAN_POINT ( 'NONE',  ( 2.997879949738217142, 18.60940351736496012, 7.792782124073855066 ) ) ;
#14737=CARTESIAN_POINT ( 'NONE',  ( 6.247365411986783634, 10.85645724975988102, 2.357295897773714177 ) ) ;
#14738=CARTESIAN_POINT ( 'NONE',  ( 1.526806735031254192, 12.95316680106106588, 8.305910411264434856 ) ) ;
#14742=CARTESIAN_POINT ( 'NONE',  ( 1.993078339923719078, 16.41892220718292705, -0.04448763570734674822 ) ) ;
#14749=CARTESIAN_POINT ( 'NONE',  ( 10.52449966068789600, 21.89451842192714182, 0.08871630297646766750 ) ) ;
#14750=CARTESIAN_POINT ( 'NONE',  ( 9.098771279194568962, 16.31622443234601505, -3.618126721927819478 ) ) ;
#14753=CARTESIAN_POINT ( 'NONE',  ( 12.86968119689294276, 21.36979473703610211, 0.4932293370143083777 ) ) ;
#14754=CARTESIAN_POINT ( 'NONE',  ( 7.409109770802898787, 21.71406919359216303, 2.854341070393255464 ) ) ;
#14756=CARTESIAN_POINT ( 'NONE',  ( 6.972679700711061024, 18.17742714445450858, 7.378323603228086114 ) ) ;
#14758=CARTESIAN_POINT ( 'NONE',  ( 6.842142561927330391, 18.93559280865479622, 6.839764141372675965 ) ) ;
#14761=CARTESIAN_POINT ( 'NONE',  ( 12.23472727335246546, 21.02863807409008245, 3.597568982022594231 ) ) ;
#14762=CARTESIAN_POINT ( 'NONE',  ( 5.365249781777944982, 15.79612960646276143, 8.006526335470118383 ) ) ;
#14764=CARTESIAN_POINT ( 'NONE',  ( 5.755077836978824024, 17.48971098885959918, 8.606492718269242559 ) ) ;
#14767=CARTESIAN_POINT ( 'NONE',  ( 6.730216886430935297, 11.15497028527178180, 2.706720253529151687 ) ) ;
#14775=CARTESIAN_POINT ( 'NONE',  ( 9.691931056481777773, 18.84418690367108695, -2.229408216028554435 ) ) ;
#14779=CARTESIAN_POINT ( 'NONE',  ( 6.919136621472420146, 13.22675071421554094, 7.220084409228111788 ) ) ;
#14785=CARTESIAN_POINT ( 'NONE',  ( 0.8343063516506451505, 19.60987250044867380, 2.327694854359185772 ) ) ;
#14788=CARTESIAN_POINT ( 'NONE',  ( 7.996957105099447460, 19.55923767994525875, -1.087077586340398971 ) ) ;
#14789=CARTESIAN_POINT ( 'NONE',  ( 2.535383609039546737, 19.37376392382110168, 1.243470200790914637 ) ) ;
#14792=CARTESIAN_POINT ( 'NONE',  ( 11.39967439401671356, 13.68296282620402238, 7.086946939641975973 ) ) ;
#14806=CARTESIAN_POINT ( 'NONE',  ( 2.791956288251989271, 11.23314441701904087, 5.253760342499054659 ) ) ;
#14809=CARTESIAN_POINT ( 'NONE',  ( 3.516109142659268105, 15.63669090343262980, -1.372924135725262396 ) ) ;
#14818=CARTESIAN_POINT ( 'NONE',  ( 1.728940443695251572, 13.74568572289879143, 0.01708573981842225267 ) ) ;
#14823=CARTESIAN_POINT ( 'NONE',  ( 13.09961018545095790, 21.49405002474989601, 1.939654742769484574 ) ) ;
#14828=CARTESIAN_POINT ( 'NONE',  ( 13.55229689020630346, 21.28532635717934340, 3.644360168486233231 ) ) ;
#14830=CARTESIAN_POINT ( 'NONE',  ( 11.34437852127595825, 19.30251821168517878, -3.616633193649956723 ) ) ;
#14834=CARTESIAN_POINT ( 'NONE',  ( 8.250958580417858457, 11.56196078241316094, 2.082770178844938425 ) ) ;
#14835=CARTESIAN_POINT ( 'NONE',  ( 6.628825292412243719, 11.76599776795001162, 3.880554096689835308 ) ) ;
#14844=CARTESIAN_POINT ( 'NONE',  ( 2.786917533582454531, 20.92456416987101875, 1.848867324536296319 ) ) ;
#14845=CARTESIAN_POINT ( 'NONE',  ( 1.702540419714505981, 15.43467393698043111, 9.533519331230623450 ) ) ;
#14848=CARTESIAN_POINT ( 'NONE',  ( 4.906036559996388213, 12.10288835339510172, 5.342054952800848966 ) ) ;
#14853=CARTESIAN_POINT ( 'NONE',  ( 9.739256322687126044, 10.74433361426668121, 0.2283133401813704499 ) ) ;
#14855=CARTESIAN_POINT ( 'NONE',  ( 9.112690981491565978, 16.57506450310666324, -3.621295390223508548 ) ) ;
#14858=CARTESIAN_POINT ( 'NONE',  ( 7.074389910882576515, 21.61684822571231024, 1.935217957262916455 ) ) ;
#14860=CARTESIAN_POINT ( 'NONE',  ( 3.855364176784159991, 12.82285234092424098, 0.9140719758827169361 ) ) ;
#14865=CARTESIAN_POINT ( 'NONE',  ( 9.537190736074361297, 15.40389167150912009, -3.043062899500690754 ) ) ;
#14869=CARTESIAN_POINT ( 'NONE',  ( 5.429893219852483632, 19.16583807351516100, 7.915143928656239503 ) ) ;
#14882=CARTESIAN_POINT ( 'NONE',  ( 13.04011110611221191, 17.29791255147096862, 6.322173244565231442 ) ) ;
#14885=CARTESIAN_POINT ( 'NONE',  ( 5.614794017493704104, 11.64278443974904320, 1.417881410066428094 ) ) ;
#14899=CARTESIAN_POINT ( 'NONE',  ( 8.986932461157417507, 18.23310434598736052, 6.953159659984535779 ) ) ;
#14900=CARTESIAN_POINT ( 'NONE',  ( 2.969052100254564674, 20.17138864544537569, 2.328491213132350079 ) ) ;
#14903=CARTESIAN_POINT ( 'NONE',  ( 13.40212049016752083, 14.65538885420913573, 7.066582115483678095 ) ) ;
#14908=CARTESIAN_POINT ( 'NONE',  ( 9.720932288844398528, 20.95102166027618296, 3.388999603248170178 ) ) ;
#14909=CARTESIAN_POINT ( 'NONE',  ( 9.441987842462824077, 11.74734702153278043, -1.584992358009425839 ) ) ;
#14916=CARTESIAN_POINT ( 'NONE',  ( 0.6728160834238413601, 11.31186333555498180, 4.884450196609837924 ) ) ;
#14918=CARTESIAN_POINT ( 'NONE',  ( 4.548213313756960474, 20.72542134385079393, 0.8261887588110893299 ) ) ;
#14922=CARTESIAN_POINT ( 'NONE',  ( 1.156505235941993837, 12.68153838805022104, 6.702054009790849420 ) ) ;
#14928=CARTESIAN_POINT ( 'NONE',  ( 13.69372857911114671, 14.67906862019266612, 6.891448972015076002 ) ) ;
#14930=CARTESIAN_POINT ( 'NONE',  ( 4.499766462069353601, 11.88009950761181166, 3.431268433568689602 ) ) ;
#14934=CARTESIAN_POINT ( 'NONE',  ( 2.164828507489252374, 19.30256671482680275, 0.1920966893002172826 ) ) ;
#14943=CARTESIAN_POINT ( 'NONE',  ( 7.239715322470854808, 21.09291897731618093, 3.289218189963096339 ) ) ;
#14949=CARTESIAN_POINT ( 'NONE',  ( 9.250817896104313931, 14.36852381253967259, 6.813382293121613920 ) ) ;
#14953=CARTESIAN_POINT ( 'NONE',  ( 3.238746979964965078, 17.52814199671485440, 8.277643969343714048 ) ) ;
#14958=CARTESIAN_POINT ( 'NONE',  ( 0.3397968550407932109, 11.79551702397467672, 3.001928043112756406 ) ) ;
#14961=CARTESIAN_POINT ( 'NONE',  ( 4.565292852930672218, 11.78113229454884170, 3.809678802701250699 ) ) ;
#14966=CARTESIAN_POINT ( 'NONE',  ( 7.345424518500083266, 18.37388711802374530, -2.636412766723661871 ) ) ;
#14969=CARTESIAN_POINT ( 'NONE',  ( 9.360979028382789835, 12.15336758057035738, -1.848830518539319678 ) ) ;
#14974=CARTESIAN_POINT ( 'NONE',  ( 6.036247796095363327, 19.98418368318813165, -0.8363276938606165611 ) ) ;
#14976=CARTESIAN_POINT ( 'NONE',  ( 0.2144152073732452368, 13.13615472609876100, 2.170878085811235092 ) ) ;
#14983=CARTESIAN_POINT ( 'NONE',  ( 11.57888104933464746, 12.79277479448814248, -2.537844513231963361 ) ) ;
#14985=CARTESIAN_POINT ( 'NONE',  ( 7.796181282232575782, 16.63782405840064982, 8.320680270861050332 ) ) ;
#14988=CARTESIAN_POINT ( 'NONE',  ( 6.555793388040663139, 10.96622957324827219, 2.745169609115350351 ) ) ;
#14998=CARTESIAN_POINT ( 'NONE',  ( 12.55379232897500152, 19.58114513849477234, 5.265243977356697691 ) ) ;
#15005=CARTESIAN_POINT ( 'NONE',  ( 4.131751249095085399, 18.64349594346743189, -0.07007902096679233250 ) ) ;
#15012=CARTESIAN_POINT ( 'NONE',  ( 9.316412786783502042, 13.73224064219962592, -2.236872125683732282 ) ) ;
#15013=CARTESIAN_POINT ( 'NONE',  ( 5.315127011898622023, 15.44490212850582189, -2.184099619210333909 ) ) ;
#15018=CARTESIAN_POINT ( 'NONE',  ( 9.652372407212508776, 20.99368581358743313, 3.205678883041131577 ) ) ;
#15019=CARTESIAN_POINT ( 'NONE',  ( 13.12356091339558262, 18.81087267297494137, 6.763476435230526107 ) ) ;
#15025=CARTESIAN_POINT ( 'NONE',  ( 3.586014194197774785, 14.72191889613304205, 9.088953234725488883 ) ) ;
#15028=CARTESIAN_POINT ( 'NONE',  ( 5.598095257095291544, 21.53640102163099357, 3.667698324075315153 ) ) ;
#15031=CARTESIAN_POINT ( 'NONE',  ( 0.3666840790735627076, 12.67405468869563201, 2.999742210112375851 ) ) ;
#15036=CARTESIAN_POINT ( 'NONE',  ( 5.498548077612729124, 13.58815257356176076, -1.570838218170207856 ) ) ;
#15039=CARTESIAN_POINT ( 'NONE',  ( 2.355781047999157884, 19.88761438775357604, 0.6622465411279562231 ) ) ;
#15048=CARTESIAN_POINT ( 'NONE',  ( 6.027233423144887858, 11.87704527764502060, 1.641552790826397157 ) ) ;
#15057=CARTESIAN_POINT ( 'NONE',  ( 8.234567635551437448, 11.56963249381149161, 2.010831876170865229 ) ) ;
#15058=CARTESIAN_POINT ( 'NONE',  ( 6.732418519251836209, 11.87159243078942161, 4.343617615359864459 ) ) ;
#15059=CARTESIAN_POINT ( 'NONE',  ( 3.089332131768892431, 18.26930023550903925, 7.991679757977339094 ) ) ;
#15063=CARTESIAN_POINT ( 'NONE',  ( 0.4154230101138479681, 19.55300952260564173, 1.162825123489284573 ) ) ;
#15066=CARTESIAN_POINT ( 'NONE',  ( 3.676953213723906710, 13.56078169262926281, 7.585074204264090625 ) ) ;
#15073=CARTESIAN_POINT ( 'NONE',  ( 9.133094369329063156, 11.81448552380872208, -1.435243799284318111 ) ) ;
#15075=CARTESIAN_POINT ( 'NONE',  ( 9.997327980603063935, 20.80492458171390169, -1.606069075083376374 ) ) ;
#15077=CARTESIAN_POINT ( 'NONE',  ( 9.194614005794997880, 18.51609980883254991, 7.549505974447304091 ) ) ;
#15084=CARTESIAN_POINT ( 'NONE',  ( 5.990136806399605440, 17.32712159277285124, -1.922517228740736384 ) ) ;
#15085=CARTESIAN_POINT ( 'NONE',  ( 5.254588850512410758, 13.39928225704216658, 6.969322526385836269 ) ) ;
#15087=CARTESIAN_POINT ( 'NONE',  ( 1.819498930146989046, 15.58835493759099400, 9.633805599351241256 ) ) ;
#15090=CARTESIAN_POINT ( 'NONE',  ( 2.075021368115900877, 17.94205954657215685, 0.2607137428604667795 ) ) ;
#15098=CARTESIAN_POINT ( 'NONE',  ( 13.16336969972371485, 15.65847078906175049, 6.372932858607479822 ) ) ;
#15103=CARTESIAN_POINT ( 'NONE',  ( 5.772535574092870547, 11.93222000202738187, 1.495588789165622545 ) ) ;
#15108=CARTESIAN_POINT ( 'NONE',  ( 6.220337769557592544, 11.67239398284132257, 2.897195776018576918 ) ) ;
#15111=CARTESIAN_POINT ( 'NONE',  ( 12.84446185305211685, 21.48375758380098333, 0.5023101645198579934 ) ) ;
#15113=CARTESIAN_POINT ( 'NONE',  ( 11.25866438965172556, 15.74982258328167717, 6.880959276425811844 ) ) ;
#15116=CARTESIAN_POINT ( 'NONE',  ( 9.388584069342069682, 11.74734702153278043, -1.568999784240643125 ) ) ;
#15121=CARTESIAN_POINT ( 'NONE',  ( 8.296946464115761088, 20.10878641201166772, -0.3926114842361396184 ) ) ;
#15122=CARTESIAN_POINT ( 'NONE',  ( 9.251884976597745336, 18.56541443352003640, 7.643588779325639848 ) ) ;
#15126=CARTESIAN_POINT ( 'NONE',  ( -0.3109692073693477443, 15.59583246595391692, 0.02116780168869621809 ) ) ;
#15129=CARTESIAN_POINT ( 'NONE',  ( 4.995330526685626715, 21.31046569428566073, 2.024587815778703614 ) ) ;
#15132=CARTESIAN_POINT ( 'NONE',  ( 0.4679875273695434101, 12.45726290459096219, 3.483910897087822089 ) ) ;
#15135=CARTESIAN_POINT ( 'NONE',  ( 2.071751749769342510, 13.12036018483466648, 1.505555561256101127 ) ) ;
#15139=CARTESIAN_POINT ( 'NONE',  ( 2.602153466714682839, 20.45502326233802393, 1.293897402751491565 ) ) ;
#15149=CARTESIAN_POINT ( 'NONE',  ( 8.107474665427385929, 11.49260726995666104, 1.880968186788171792 ) ) ;
#15155=CARTESIAN_POINT ( 'NONE',  ( 8.981279084499066201, 12.48120098075682805, 5.346287112963081789 ) ) ;
#15162=CARTESIAN_POINT ( 'NONE',  ( 0.05081553632030246653, 12.65820550866425620, 1.671469819115525723 ) ) ;
#15165=CARTESIAN_POINT ( 'NONE',  ( 6.767590535262720586, 11.71523883824356282, 4.062906024995755594 ) ) ;
#15171=CARTESIAN_POINT ( 'NONE',  ( 13.09788092753539424, 14.67906862019266612, 7.069884632380020406 ) ) ;
#15174=CARTESIAN_POINT ( 'NONE',  ( 11.32645464201832652, 22.04042062782242084, 2.039904004311749564 ) ) ;
#15177=CARTESIAN_POINT ( 'NONE',  ( 8.523675650794778846, 10.78766231307313994, 3.249609201625923927 ) ) ;
#15178=CARTESIAN_POINT ( 'NONE',  ( 3.167498170806753777, 12.59169734781732330, 6.476231790880818018 ) ) ;
#15181=CARTESIAN_POINT ( 'NONE',  ( 7.254584665336054172, 16.67580702288875116, 7.619632138345714623 ) ) ;
#15185=CARTESIAN_POINT ( 'NONE',  ( 11.61973461185466583, 18.13781435472470349, -3.585029466117453989 ) ) ;
#15187=CARTESIAN_POINT ( 'NONE',  ( 3.613208712544091039, 16.52268874363389628, 9.310180084879426943 ) ) ;
#15191=CARTESIAN_POINT ( 'NONE',  ( 3.161989770655216248, 17.96135795615357011, 8.230302926828514387 ) ) ;
#15198=CARTESIAN_POINT ( 'NONE',  ( 9.699109564081849655, 21.77551566733012933, 3.361061402723362512 ) ) ;
#15200=CARTESIAN_POINT ( 'NONE',  ( 12.83002304812085015, 12.17901403585384656, 4.356414321884917840 ) ) ;
#15203=CARTESIAN_POINT ( 'NONE',  ( 3.505934377962688586, 17.20635281421107265, -0.6812542612677440212 ) ) ;
#15209=CARTESIAN_POINT ( 'NONE',  ( 6.206257128763711606, 10.96622738556230026, 2.849852413749992763 ) ) ;
#15212=CARTESIAN_POINT ( 'NONE',  ( 8.098296366812832048, 20.59418330540166053, 4.742484706917446502 ) ) ;
#15214=CARTESIAN_POINT ( 'NONE',  ( 9.685017632263924980, 18.90675885874853890, -2.319252428474684269 ) ) ;
#15215=CARTESIAN_POINT ( 'NONE',  ( 6.658090509130313528, 20.81351436963172219, 5.254839933866528590 ) ) ;
#15216=CARTESIAN_POINT ( 'NONE',  ( 13.55166441465202176, 22.20239475586336297, 2.436989766962892823 ) ) ;
#15222=CARTESIAN_POINT ( 'NONE',  ( 10.83319469175927985, 18.70694946134396375, 6.220917748816447990 ) ) ;
#15223=CARTESIAN_POINT ( 'NONE',  ( 12.95755072449374090, 11.26929059074382167, 4.630978755562344062 ) ) ;
#15228=CARTESIAN_POINT ( 'NONE',  ( 11.05480056376844544, 17.56817812073120422, -4.236062988348112235 ) ) ;
#15229=CARTESIAN_POINT ( 'NONE',  ( 1.361757355601472597, 13.96208391574584162, 9.123754984142934177 ) ) ;
#15232=CARTESIAN_POINT ( 'NONE',  ( 5.936085032262425010, 21.40849574231920371, 4.589919153110645134 ) ) ;
#15241=CARTESIAN_POINT ( 'NONE',  ( 0.5565784135784356268, 12.32463844299294209, 3.900071968666352973 ) ) ;
#15245=CARTESIAN_POINT ( 'NONE',  ( 3.788814298098374778, 14.00384518420827185, -0.003950202559398034718 ) ) ;
#15249=CARTESIAN_POINT ( 'NONE',  ( 2.872526310428787699, 20.88929092507290264, 2.007101110068493899 ) ) ;
#15263=CARTESIAN_POINT ( 'NONE',  ( 7.332841212239828543, 14.65140826333467139, -1.889360907835787584 ) ) ;
#15264=CARTESIAN_POINT ( 'NONE',  ( 1.622819991010447493, 17.33683664400565050, 9.603356706031211942 ) ) ;
#15270=ORIENTED_EDGE ( 'NONE', *, *, #2449, .F. ) ;
#15271=CARTESIAN_POINT ( 'NONE',  ( 9.162049469916118127, 13.41167720919363582, 6.257157424146843283 ) ) ;
#15274=CARTESIAN_POINT ( 'NONE',  ( 3.384545484207448496, 16.33714236856847535, 8.445044841043495509 ) ) ;
#15280=CARTESIAN_POINT ( 'NONE',  ( 0.5341928495527494825, 19.88375074128939346, 1.456988048183946560 ) ) ;
#15283=CARTESIAN_POINT ( 'NONE',  ( 5.292371360443332229, 12.95486688907394246, 6.632903289465746255 ) ) ;
#15289=CARTESIAN_POINT ( 'NONE',  ( 5.059806928477906141, 15.45793682862229801, -2.017440984236586576 ) ) ;
#15291=CARTESIAN_POINT ( 'NONE',  ( 13.34013785991228573, 16.63357698718011690, 7.165916878433363557 ) ) ;
#15296=CARTESIAN_POINT ( 'NONE',  ( 8.408550922056784671, 10.74106511205577164, 2.765873773487825815 ) ) ;
#15298=CARTESIAN_POINT ( 'NONE',  ( 7.026614297195842518, 12.34350287060300211, 5.586514903065737947 ) ) ;
#15300=CARTESIAN_POINT ( 'NONE',  ( 7.172396199599091027, 17.36778504101753740, 7.516626074145736247 ) ) ;
#15303=CARTESIAN_POINT ( 'NONE',  ( 11.89439084632494215, 11.62217351343478278, -1.089731598560132575 ) ) ;
#15305=CARTESIAN_POINT ( 'NONE',  ( -0.9181641814394345680, 20.56338889613970267, 3.252949121733808457 ) ) ;
#15309=CARTESIAN_POINT ( 'NONE',  ( 3.372374456746679350, 16.48230391985759979, 8.538301946733126258 ) ) ;
#15315=CARTESIAN_POINT ( 'NONE',  ( 10.97450655955806198, 19.34169052257783505, 6.746375022551643674 ) ) ;
#15320=CARTESIAN_POINT ( 'NONE',  ( 12.99318388508481092, 12.89692632477686551, 5.134509715740512625 ) ) ;
#15323=CARTESIAN_POINT ( 'NONE',  ( 3.179746087645565211, 14.94275550331619229, 8.487434319128327687 ) ) ;
#15325=CARTESIAN_POINT ( 'NONE',  ( -0.6062791574742081302, 20.63358940807441400, 5.277116226863125092 ) ) ;
#15328=CARTESIAN_POINT ( 'NONE',  ( 6.288799001572192182, 11.69884688535491080, 2.878624824896528267 ) ) ;
#15331=CARTESIAN_POINT ( 'NONE',  ( 5.664688483032882083, 17.24315932450417321, -1.411349549249473645 ) ) ;
#15332=CARTESIAN_POINT ( 'NONE',  ( 3.192747775439045199, 20.40795131746391533, 2.906160320096165428 ) ) ;
#15333=CARTESIAN_POINT ( 'NONE',  ( 11.03274821853219478, 12.61666159072338189, 5.337489519850219466 ) ) ;
#15334=CARTESIAN_POINT ( 'NONE',  ( 4.291439396447429111, 12.50969690204968288, 0.5082001374855064091 ) ) ;
#15335=CARTESIAN_POINT ( 'NONE',  ( 12.82184179453522255, 22.28580575005450370, 0.3944390745095269213 ) ) ;
#15339=CARTESIAN_POINT ( 'NONE',  ( 11.06256098204447902, 17.48602064462742334, 6.685474825520898889 ) ) ;
#15340=CARTESIAN_POINT ( 'NONE',  ( 10.81007580454433281, 10.89927089225536250, 4.167050900241501488 ) ) ;
#15346=CARTESIAN_POINT ( 'NONE',  ( 2.000949203156153544, 19.75183458472020348, 0.6057391540848391376 ) ) ;
#15349=CARTESIAN_POINT ( 'NONE',  ( 6.702764444734650162, 20.32026046638254613, 6.637863228519256253 ) ) ;
#15357=CARTESIAN_POINT ( 'NONE',  ( 3.851420698079342841, 13.47177213679970720, 0.3669712269455133735 ) ) ;
#15364=CARTESIAN_POINT ( 'NONE',  ( 3.436124513232142519, 21.34046060373059106, 3.525057534639083556 ) ) ;
#15376=CARTESIAN_POINT ( 'NONE',  ( 13.63565303003243478, 21.00494883119180045, 3.473673388005832585 ) ) ;
#15377=CARTESIAN_POINT ( 'NONE',  ( -0.1405913361260165972, 13.90873432424026213, 0.5585379980126942145 ) ) ;
#15383=CARTESIAN_POINT ( 'NONE',  ( 7.463375574167044668, 16.12223603717324849, -2.121406194095333930 ) ) ;
#15390=CARTESIAN_POINT ( 'NONE',  ( -0.1293393001420969635, 13.83032883076687725, 0.7266954706132912056 ) ) ;
#15394=CARTESIAN_POINT ( 'NONE',  ( 5.013800915383680668, 12.10687735873178283, 5.308141424993535473 ) ) ;
#15400=B_SPLINE_CURVE_WITH_KNOTS ( 'NONE', 3,
 ( #12416, #4222, #2115, #350, #3898, #5655, #10640, #4009, #10753, #17268, #10962, #15850, #14307, #21024, #2001, #5870, #17601, #3787, #7099, #9075, #2232, #13867, #2454, #5430, #9183, #12195, #17498, #7424, #10522, #470, #2342, #20912, #17392, #8856, #15639, #7223, #13984, #20681, #15963, #8971, #5774, #12530, #6302, #21122, #11077, #6416, #14635, #7646, #1327, #16491, #12861, #9512, #14845, #7752, #14407, #13186, #16388, #21560, #7859, #19783, #5971, #11179, #12744, #16177, #4448, #19466, #18148, #1225, #14738, #2890, #4657, #4337, #19581, #19895, #18033, #6091, #21444, #4768, #6198, #17715, #9622, #17932, #17832, #2679, #7968, #2566, #9300, #9408, #14514, #2777, #8069, #1003, #3003, #21340, #16281, #21234, #13076, #16075, #905, #1114, #12966, #19677, #4545, #11284, #11402, #9730, #14958, #20315, #3330, #8614, #8387, #18665, #16597, #4868, #16808, #15162, #19997, #1437, #3534, #6956, #6854, #18565, #11726, #15390, #10272, #18463, #13722, #3103, #20051, #17021, #10061, #11935, #11612, #21775, #18345, #13294, #13616, #20214, #8184, #3211, #1647, #5184, #8498, #9949, #1870, #9828, #11836, #21672, #5088, #3428, #217, #20418, #11501, #18244, #10163, #6534, #16710, #6739, #1548, #16906, #1755, #8291, #15063, #6626, #15280, #13392, #20100, #4970, #13503, #105, #2203, #18780, #10497, #15720, #10393, #20539, #2427, #14169, #15497, #20652, #7192, #15604, #18996, #12387, #3873, #761, #5625, #10825, #10610, #548, #324, #5746, #441, #2086, #7067, #12050, #20875, #3650, #12501, #7515, #17359, #15935, #3762, #7294, #8944, #13954, #12167, #17137, #18891, #9153, #13834, #19223, #4085, #2311, #5403, #7398, #1978, #19111, #8719, #20765, #14058, #17574, #14280, #5513, #3982, #5285, #17243, #8827, #12271, #10725, #17467, #9047, #15823, #650, #8045, #7829, #2981, #11375, #11047, #9705, #12833, #16255, #9267, #9593, #18004, #19756, #9378, #6061, #20997, #5844, #19651, #12601, #16146, #19554, #6176, #4421, #16471, #21315, #4628, #17902, #1085, #9484, #16362, #2862, #21202, #2536, #17801, #1201, #14607, #973, #2750, #14715, #12942, #7944, #16045, #4519, #7723, #14485, #876, #10932, #11257, #18122, #19325, #7619, #1303, #4192, #17683, #21421, #14378, #5944, #21094, #13049, #6275, #12710, #19434, #4308, #2649, #1524, #1625, #11910, #3307, #13159, #18325, #11697, #3185, #4945, #18435, #8155, #1845, #6718, #20290, #5159, #14818, #18639, #10138, #9807, #19871, #18542, #10039, #9917, #20078, #11813, #21531, #16787, #10246, #21859, #3507, #13271, #4849, #6827, #5061, #13588, #6391, #16576, #16991, #4746, #11483, #8268, #18227, #21648, #3084, #3405, #1412, #14934, #6511, #19978, #11589, #16683, #8366, #15039, #21753, #6607, #13371, #15139, #13473, #20189, #16883, #1733, #8473, #15249, #75, #17110, #13694, #931, #4365, #4254, #3735, #5378, #10365, #15364, #17749, #6931, #2595, #11103, #14229, #7571, #19501, #7035, #10881, #706, #17211, #10992, #17630, #20394, #294, #7455, #12558, #17857, #9330, #1950, #16101, #12020, #8690, #8587, #5802, #5258, #21153, #6008, #2054, #20945, #12778, #187, #19280, #13804, #2482, #15996, #14332, #20508, #12141, #8795, #18867, #4143, #5897, #12661, #10817, #1967, #5610, #20526, #20862, #7387, #9140, #7499, #19209, #5393, #3857, #12261, #20754, #17456, #10380, #310, #4076, #14157, #637, #2190, #17226, #15587, #12370, #5732, #12486, #10595, #13821, #15925, #8931, #19097, #12156, #17564, #9036, #2414, #2299, #748, #7053, #18984, #14265, #10711, #20639, #20982, #19317, #3966, #5834, #15811, #12592, #18881, #3752, #17127, #8705, #15484, #10485, #426, #17342, #2069, #8810, #7177, #14046, #15708, #13942, #5499, #536, #7284, #9693, #13147, #12697, #12930, #1294, #14594, #2848, #7606, #13036, #17891, #8033, #1073, #11360, #9254, #19421, #9473, #7816, #4295, #16033, #18110, #21517, #21410, #21189, #21083, #10922, #19741, #2525, #4615, #6374, #16243, #17992, #14809, #2637, #6165, #2737, #6047, #11035, #864, #17790, #4179, #9366, #2967, #16459, #17670, #16133, #14706, #14367, #962, #5933, #21302, #7712, #14473, #12818, #19544, #19639, #4409, #11143, #4507, #11244, #9580, #16350, #1188, #6265, #7930, #13359, #14918, #18314, #6598, #1396, #20278, #11473, #15129, #8138, #8460, #16875, #18630, #8255, #4934, #19860, #4733, #18531, #18217, #15028, #3070, #9796, #13574, #1722, #10130, #15232, #63, #3497, #21744, #11683, #16564, #21635, #3396, #6495, #20064, #18422, #5049, #3293, #15349, #20174, #10024, #4839, #3170, #8358, #6815, #5149, #16777, #13259, #16667, #11901, #21848, #1618, #6702, #10233, #13463, #16978, #19967, #11798, #1832, #8574, #9901, #177, #6919, #11574, #1510, #15455, #2388, #15898, #17540, #396, #3610, #20496, #1939, #5702, #2158, #17434, #19067, #7361, #13792, #7150, #8903, #9115, #5367, #12009, #17199, #10565, #2039, #3830, #17311, #7024, #724, #5582, #19185, #4051, #13682, #10795, #9014, #8681, #18740, #20726, #282, #20382, #616, #10350, #14131, #5249, #18958, #12341, #17094, #12129, #15683, #5472, #8784, #18853 ),
 .UNSPECIFIED., .F., .F.,
 ( 4, 3, 3, 3, 3, 3, 3, 3, 3, 3, 3, 3, 3, 3, 3, 3, 3, 3, 3, 3, 3, 3, 3, 3, 3, 3, 3, 3, 3, 3, 3, 3, 3, 3, 3, 3, 3, 3, 3, 3, 3, 3, 3, 3, 3, 3, 3, 3, 3, 3, 3, 3, 3, 3, 3, 3, 3, 3, 3, 3, 3, 3, 3, 3, 3, 3, 3, 3, 3, 3, 3, 3, 3, 3, 3, 3, 3, 3, 3, 3, 3, 3, 3, 3, 3, 3, 3, 3, 3, 3, 3, 3, 3, 3, 3, 3, 3, 3, 3, 3, 3, 3, 3, 3, 3, 3, 3, 3, 3, 3, 3, 3, 3, 3, 3, 3, 3, 3, 3, 3, 3, 3, 3, 3, 3, 3, 3, 3, 3, 3, 3, 3, 3, 3, 3, 3, 3, 3, 3, 3, 3, 3, 3, 3, 3, 3, 3, 3, 3, 3, 3, 3, 3, 3, 3, 3, 3, 3, 3, 3, 3, 3, 3, 3, 3, 3, 3, 3, 3, 3, 3, 3, 3, 3, 3, 3, 3, 3, 3, 3, 3, 3, 3, 3, 3, 3, 3, 3, 3, 3, 3, 3, 3, 3, 3, 3, 3, 3, 3, 3, 3, 3, 3, 3, 3, 3, 3, 3, 3, 3, 3, 3, 3, 3, 3, 3, 3, 3, 4 ),
 ( 0.000000000000000000, 0.006329113921512709816, 0.01249999948583089930, 0.01265822784302339868, 0.01898734176453509975, 0.02531645568604689797, 0.02874999970365120158, 0.03164556960755859905, 0.03797468352907030359, 0.04430379745058199426, 0.04500000460022859916, 0.05063291137210369774, 0.05696202529361540229, 0.06124999099804120245, 0.06329113921512709295, 0.06962025313663890158, 0.07594936705815059919, 0.07750001213348130247, 0.08227848097966231067, 0.08860759490117400827, 0.09374999174283218939, 0.09493670882268570588, 0.1012658227441869951, 0.1075949366657489997, 0.1100000114765239956, 0.1139240505872110010, 0.1202531645087729917, 0.1262499984399119979, 0.1265822784302340076, 0.1329113923517959983, 0.1392405062732580134, 0.1425000018589560047, 0.1455696201948190049, 0.1518987341162809923, 0.1582278480378430108, 0.1587500029336659790, 0.1645569619593049981, 0.1708860758808660174, 0.1749999920308009937, 0.1772151898023280048, 0.1835443037238899955, 0.1898734176453510114, 0.1912500109487239863, 0.1962025315669130021, 0.2025316454883749895, 0.2074999907470810034, 0.2088607594099370079, 0.2151898733313979961, 0.2215189872529599868, 0.2237500124104200017, 0.2278481011744220019, 0.2341772150959829935, 0.2399999971172069868, 0.2405063290174449808, 0.2468354429390069993, 0.2531645568604689589, 0.2562500040988209826, 0.2594936707820300059, 0.2658227847034919655, 0.2721518986250540117, 0.2725000015136869735, 0.2784810125465150277, 0.2848101264680770184, 0.2887499934460570072, 0.2911392403895390335, 0.2974683543111009687, 0.3037974682325620401, 0.3050000094647010163, 0.3101265821541239753, 0.3164556960755859905, 0.3212499901042359940, 0.3227848099971469820, 0.3291139239186089971, 0.3354430378401709878, 0.3375000129078500333, 0.3417721517616330029, 0.3481012656831939944, 0.3537499956223240094, 0.3544303796046560096, 0.3607594935262180003, 0.3670886074476790162, 0.3700000062353510089, 0.3734177213692410069, 0.3797468352907030220, 0.3860759492122649572, 0.3862500004432609657, 0.3924050631337259731, 0.3987341770552880194, 0.4024999951885679939, 0.4050632909767500345, 0.4113924048983109705, 0.4177215188197730411, 0.4187500077716679869, 0.4240506327413349763, 0.4303797466627969914, 0.4349999898663099995, 0.4367088605843579829, 0.4430379745058199981, 0.4493670884273820443, 0.4512500129516539560, 0.4556962023488430047, 0.4620253162704049954, 0.4674999940843199697, 0.4683544301918670105, 0.4746835441134290012, 0.4810126580348899616, 0.4837500081779320116, 0.4873417719564519524, 0.4936708858779140230, 0.4999999997994749590, 0.5063291137210370607, 0.5126582276424990203, 0.5162499971872059890, 0.5189873415640610110, 0.5253164554855219714, 0.5316455694070840732, 0.5325000059764910532, 0.5379746833285459218, 0.5443037972501070243, 0.5487499900616280568, 0.5506329111715689839, 0.5569620250931309746, 0.5632911390145930453, 0.5650000125471910106, 0.5696202529361540368, 0.5759493668576159964, 0.5812499926263350325, 0.5822784807791780981, 0.5886075947006399467, 0.5949367086222009382, 0.5975000098441739516, 0.6012658225436630088, 0.6075949364652249995, 0.6137499991490910078, 0.6139240503866860710, 0.6202531643082479507, 0.6265822782297100213, 0.6299999993587850344, 0.6329113921512710128, 0.6392405060727330834, 0.6455696199942949631, 0.6462500041965290043, 0.6518987339157570338, 0.6582278478373180253, 0.6624999906948350059, 0.6645569617587799849, 0.6708860756803419756, 0.6772151896018030470, 0.6787500117227039942, 0.6835443035233650377, 0.6898734174448269973, 0.6949999913591019540, 0.6962025313663889881, 0.7025316452878499485, 0.7088607592094120502, 0.7112500111636119726, 0.7151898731308740098, 0.7215189870524348903, 0.7274999980929279797, 0.7278481009738969609, 0.7341772148954590627, 0.7405063288169210223, 0.7437500016122360336, 0.7468354427384820138, 0.7531645566599439734, 0.7594936705815059641, 0.7600000025531850056, 0.7658227845029670355, 0.7721518984245289152, 0.7762499917481929801, 0.7784810123459909859, 0.7848101262675529766, 0.7911392401890140480, 0.7925000105295659791, 0.7974683541105760387, 0.8037974680320379983, 0.8087499903763730735, 0.8101265819535989898, 0.8164556958750610605, 0.8227848097966229401, 0.8250000120812989168, 0.8291139237180850108, 0.8354430376396460023, 0.8412499967467070849, 0.8417721515611080729, 0.8481012654826700636, 0.8544303794041309130, 0.8575000038524419610, 0.8607594933256930148, 0.8670886072471549744, 0.8734177211687170761, 0.8737500011633969610, 0.8797468350901779255, 0.8860759490117400272, 0.8899999931828780353, 0.8924050629332019868, 0.8987341768547630894, 0.9050632907762249380, 0.9062500090409180142, 0.9113924046977870397, 0.9177215186192489993, 0.9224999897505299362, 0.9240506325408099908, 0.9303797464622719504, 0.9367088603838339411, 0.9387500125608460033, 0.9430379743052960118, 0.9493670882268570033, 0.9549999952374580436, 0.9556962021483190739, 0.9620253160698809536, 0.9683544299913420250, 0.9712500058838849926, 0.9746835439129040157, 0.9810126578343659753, 0.9873417717559279660, 0.9875000001065180610, 0.9936708856773890375, 0.9999999995989510282 ),
 .UNSPECIFIED. ) ;
#15402=CARTESIAN_POINT ( 'NONE',  ( 6.184730801054771021, 10.88474977364208129, 3.317143460567523405 ) ) ;
#15404=CARTESIAN_POINT ( 'NONE',  ( 13.29405768023306855, 17.16992202419550040, 7.114197972723578012 ) ) ;
#15408=CARTESIAN_POINT ( 'NONE',  ( 8.854315084285317994, 11.17507848100337142, 4.651611944549387090 ) ) ;
#15409=CARTESIAN_POINT ( 'NONE',  ( 2.934619771450872605, 20.19932627889173915, 2.180100518733211867 ) ) ;
#15411=CARTESIAN_POINT ( 'NONE',  ( 5.587488707699998614, 15.19155588846434668, -1.244131986940470558 ) ) ;
#15413=CARTESIAN_POINT ( 'NONE',  ( 9.129586632131145407, 19.91511611422710359, 6.193789383866233678 ) ) ;
#15414=CARTESIAN_POINT ( 'NONE',  ( 4.163685238762522722, 21.32044071393296036, 5.231111188599066431 ) ) ;
#15418=CARTESIAN_POINT ( 'NONE',  ( 0.3827680527341568162, 18.57760016544011705, 1.316900888515376566 ) ) ;
#15423=CARTESIAN_POINT ( 'NONE',  ( 9.157588821307307114, 21.85973784873793235, 1.865442930748904216 ) ) ;
#15426=CARTESIAN_POINT ( 'NONE',  ( 11.32358359230530631, 12.92367503848713106, -2.306284810701165089 ) ) ;
#15428=CARTESIAN_POINT ( 'NONE',  ( 5.668831867569799066, 12.20187417505221994, 1.017780631167809258 ) ) ;
#15432=CARTESIAN_POINT ( 'NONE',  ( -0.4828750084152318434, 20.32260066232836238, 5.240161191498525106 ) ) ;
#15433=CARTESIAN_POINT ( 'NONE',  ( 4.495706609612955873, 19.71336308942898441, 0.7933311248715388952 ) ) ;
#15434=CARTESIAN_POINT ( 'NONE',  ( 6.095663563013475006, 11.06004392628846134, 2.889821626036587432 ) ) ;
#15436=CARTESIAN_POINT ( 'NONE',  ( 6.462165521336576290, 11.60753147827898069, 3.224331916540620124 ) ) ;
#15437=CARTESIAN_POINT ( 'NONE',  ( 8.601357627048034971, 11.53726303284714128, 3.530950561658094067 ) ) ;
#15438=CARTESIAN_POINT ( 'NONE',  ( 1.758281139847138741, 12.61021756743670252, 7.885184424230324396 ) ) ;
#15439=CARTESIAN_POINT ( 'NONE',  ( 13.33955114723241842, 16.76849418036265149, 7.284517011081861781 ) ) ;
#15443=UNCERTAINTY_MEASURE_WITH_UNIT (LENGTH_MEASURE( 1.000000000000000082E-05 ), #4485, 'distance_accuracy_value', 'NONE');
#15447=CARTESIAN_POINT ( 'NONE',  ( 11.18447833514740886, 14.12277392074263638, 6.311446057064062032 ) ) ;
#15448=CARTESIAN_POINT ( 'NONE',  ( 9.992878607143374836, 20.90214019755116226, -1.685752229938785041 ) ) ;
#15452=CARTESIAN_POINT ( 'NONE',  ( 5.257238202180718467, 13.88483174882859217, 8.323134035216043003 ) ) ;
#15455=CARTESIAN_POINT ( 'NONE',  ( 7.503791424408063016, 16.45334519770218407, 8.390729612094148138 ) ) ;
#15459=CARTESIAN_POINT ( 'NONE',  ( 0.2299619499110654997, 13.12625805216814712, 2.319564647753492359 ) ) ;
#15463=CARTESIAN_POINT ( 'NONE',  ( 1.882899281740455066, 15.00618873593124825, 0.2860482631481570115 ) ) ;
#15465=CARTESIAN_POINT ( 'NONE',  ( 3.740646147519985476, 14.76563347569464213, -0.3756423018599123198 ) ) ;
#15480=CARTESIAN_POINT ( 'NONE',  ( 9.637099489725157397, 21.04886798522784375, 3.438002499022450031 ) ) ;
#15481=CARTESIAN_POINT ( 'NONE',  ( 1.696055354432304707, 16.44733452758824654, -0.8045495263988319268 ) ) ;
#15484=CARTESIAN_POINT ( 'NONE',  ( 4.586192111020174877, 11.08290593202983310, 3.814641854836081425 ) ) ;
#15489=CARTESIAN_POINT ( 'NONE',  ( 7.677408542654871049, 18.01687583117972835, -1.852128230417407595 ) ) ;
#15497=CARTESIAN_POINT ( 'NONE',  ( 1.245798919419617956, 21.00536303059330123, 3.318209283441092339 ) ) ;
#15499=CARTESIAN_POINT ( 'NONE',  ( 7.153480333052655737, 18.17742714445450858, 7.324180098355732582 ) ) ;
#15504=CARTESIAN_POINT ( 'NONE',  ( 9.152014112632087972, 16.62671289803297370, 8.096787993944319695 ) ) ;
#15506=CARTESIAN_POINT ( 'NONE',  ( 13.07020640692051217, 18.72802180134034344, 6.676514015753832076 ) ) ;
#15509=CARTESIAN_POINT ( 'NONE',  ( 12.87588295628459001, 21.37236768246749108, 0.5100726682396032885 ) ) ;
#15510=CARTESIAN_POINT ( 'NONE',  ( 9.407243984221324240, 17.02847102510445865, 7.946678039590906018 ) ) ;
#15511=CARTESIAN_POINT ( 'NONE',  ( 1.334794203082131148, 20.33449649584820307, 3.512594067846317891 ) ) ;
#15514=CARTESIAN_POINT ( 'NONE',  ( 6.250389098271795341, 19.57090748711431161, -0.1645743329559772594 ) ) ;
#15518=CARTESIAN_POINT ( 'NONE',  ( 13.27675186413636688, 21.88443657126030217, 0.3155811547653178395 ) ) ;
#15520=CARTESIAN_POINT ( 'NONE',  ( 4.249701460077716320, 11.26224364954182100, 1.967523915872277929 ) ) ;
#15524=CARTESIAN_POINT ( 'NONE',  ( 1.874547060697949075, 16.41909622821189885, -0.01419169111653226234 ) ) ;
#15530=CARTESIAN_POINT ( 'NONE',  ( 11.43714432798503466, 15.67669137045964156, 7.541779987268694363 ) ) ;
#15533=CARTESIAN_POINT ( 'NONE',  ( 11.39716744546816862, 12.54995360374833702, -1.947677416576856890 ) ) ;
#15535=CARTESIAN_POINT ( 'NONE',  ( 7.018469835957150238, 16.59395432398027381, 7.891820759634939009 ) ) ;
#15543=CARTESIAN_POINT ( 'NONE',  ( 14.08960504820682580, 20.59139265233172367, 3.838791682861076637 ) ) ;
#15544=CARTESIAN_POINT ( 'NONE',  ( 4.465258710612409310, 19.89810213900386060, 6.216219807304937284 ) ) ;
#15547=CARTESIAN_POINT ( 'NONE',  ( 5.836838028218656049, 12.69913397707368219, 0.1851268596130520583 ) ) ;
#15548=CARTESIAN_POINT ( 'NONE',  ( 6.713027782948464584, 11.25617621838232196, 2.282006732609870081 ) ) ;
#15549=CARTESIAN_POINT ( 'NONE',  ( 7.410451725513929944, 18.37204556237463393, -2.651051064885699304 ) ) ;
#15550=DIRECTION ( 'NONE',  ( 0.2840839455009870340, -0.1392238476126010371, 0.9486374608692910160 ) ) ;
#15556=CARTESIAN_POINT ( 'NONE',  ( 9.801219140300959864, 21.83972979323944230, 3.592275403358046404 ) ) ;
#15558=CARTESIAN_POINT ( 'NONE',  ( 9.878043619689368171, 11.67119934733697129, 0.3244805056039586910 ) ) ;
#15561=CARTESIAN_POINT ( 'NONE',  ( 1.566802806665559045, 21.20295136681662385, 5.074033647315427054 ) ) ;
#15582=CARTESIAN_POINT ( 'NONE',  ( 6.497796024369758783, 11.60753147827898069, 3.213661819375602136 ) ) ;
#15584=CARTESIAN_POINT ( 'NONE',  ( 2.908793012413193324, 11.23804227924006227, 5.217805794380214301 ) ) ;
#15587=CARTESIAN_POINT ( 'NONE',  ( 5.530698010192272918, 13.68895168523844674, 8.102282649766468836 ) ) ;
#15594=CARTESIAN_POINT ( 'NONE',  ( 7.470178629798640557, 16.24275013615479679, -2.126460335357540199 ) ) ;
#15596=CARTESIAN_POINT ( 'NONE',  ( 3.326019219354948486, 13.57811087000449035, 7.466394700117205296 ) ) ;
#15604=CARTESIAN_POINT ( 'NONE',  ( 1.327372290668605848, 21.07154981679812167, 3.536567113229659665 ) ) ;
#15607=CARTESIAN_POINT ( 'NONE',  ( 4.101782029537222485, 17.20635281421107265, -0.8596899216323250492 ) ) ;
#15614=CARTESIAN_POINT ( 'NONE',  ( 8.856615887970798795, 13.10471967957858119, 6.770334555984388381 ) ) ;
#15617=CARTESIAN_POINT ( 'NONE',  ( 11.32059934594350281, 22.04125121511821916, 2.023640860796339869 ) ) ;
#15624=CARTESIAN_POINT ( 'NONE',  ( 9.139755265305351983, 11.93170736937736187, 5.902681470851192103 ) ) ;
#15625=CARTESIAN_POINT ( 'NONE',  ( -0.7765736244451648673, 19.84689652320655995, 3.563773667300057291 ) ) ;
#15628=CARTESIAN_POINT ( 'NONE',  ( 5.995600430637586520, 12.23416120028617371, 1.046533783840128740 ) ) ;
#15629=CARTESIAN_POINT ( 'NONE',  ( 7.142136784733786214, 17.57921760804553557, 7.468824909625386255 ) ) ;
#15632=CARTESIAN_POINT ( 'NONE',  ( 1.396705373849880472, 20.30655539761074735, 3.754731929609379737 ) ) ;
#15635=CARTESIAN_POINT ( 'NONE',  ( 11.23574321677510213, 19.52774875955264022, 6.574244702891200554 ) ) ;
#15636=CARTESIAN_POINT ( 'NONE',  ( 4.867729296808080974, 12.11136722865829540, 5.091807635075894289 ) ) ;
#15638=CARTESIAN_POINT ( 'NONE',  ( 3.690010452587021206, 17.35406872798134259, -1.479586497304065329 ) ) ;
#15639=CARTESIAN_POINT ( 'NONE',  ( 1.431034899629216817, 18.16898401507852867, 9.266644725746632005 ) ) ;
#15642=CARTESIAN_POINT ( 'NONE',  ( 3.122877388456776426, 12.59229297301672190, 6.489217028501734319 ) ) ;
#15652=CARTESIAN_POINT ( 'NONE',  ( 11.28297949870794170, 17.68526700538642515, 7.421515332377799368 ) ) ;
#15654=CARTESIAN_POINT ( 'NONE',  ( 12.11045644880566741, 11.20221354020535109, 1.207418464437750805 ) ) ;
#15664=CARTESIAN_POINT ( 'NONE',  ( 9.355592019679061622, 15.41930233576164433, -2.894346530100807335 ) ) ;
#15665=CARTESIAN_POINT ( 'NONE',  ( 10.33042288919505580, 11.26312240063166037, 2.170817215344111872 ) ) ;
#15666=CARTESIAN_POINT ( 'NONE',  ( 0.9885671785712810689, 20.25378384025834322, 1.764069577497025421 ) ) ;
#15674=CARTESIAN_POINT ( 'NONE',  ( 8.230913307447869087, 21.33050868956278023, 5.055680035315745613 ) ) ;
#15676=CARTESIAN_POINT ( 'NONE',  ( 10.15327187727333857, 11.38490435674824219, 1.527704889486475759 ) ) ;
#15680=CARTESIAN_POINT ( 'NONE',  ( 1.273922206673044455, 17.31795573271877942, 9.619519439844173903 ) ) ;
#15683=CARTESIAN_POINT ( 'NONE',  ( 6.552291428502512893, 10.92726696357779126, 3.523081400066527369 ) ) ;
#15704=CARTESIAN_POINT ( 'NONE',  ( 6.845745190715632589, 12.02592060257602213, 4.770099056714289354 ) ) ;
#15705=CARTESIAN_POINT ( 'NONE',  ( 3.428347309981619517, 18.28257875309041935, 8.925423822362398951 ) ) ;
#15708=CARTESIAN_POINT ( 'NONE',  ( 4.218746967243003354, 11.29694704288618290, 2.241506840608003870 ) ) ;
#15713=CARTESIAN_POINT ( 'NONE',  ( 7.596779357869561267, 13.14120497759026307, -0.9199170277768317083 ) ) ;
#15720=CARTESIAN_POINT ( 'NONE',  ( 0.9406339474007729962, 20.66888917947650484, 2.506880476070809660 ) ) ;
#15724=CARTESIAN_POINT ( 'NONE',  ( 0.7338959141973584455, 18.79999059560985231, 0.8591482719905695342 ) ) ;
#15731=CARTESIAN_POINT ( 'NONE',  ( 5.026532476923114778, 15.50533030672313828, -1.679517137562626772 ) ) ;
#15733=CARTESIAN_POINT ( 'NONE',  ( 13.22358791529405408, 12.74046206659965819, 5.993796513000479997 ) ) ;
#15738=CARTESIAN_POINT ( 'NONE',  ( 7.410350071410004347, 12.70579758959303796, -1.564945618823073925 ) ) ;
#15739=CARTESIAN_POINT ( 'NONE',  ( 7.091083114709308965, 18.17949408554134649, 7.347600680106210369 ) ) ;
#15741=CARTESIAN_POINT ( 'NONE',  ( 5.725034261819131665, 13.29448173139118161, -0.2693480136903509403 ) ) ;
#15742=CARTESIAN_POINT ( 'NONE',  ( 7.319589578518462147, 14.78174204738065356, 7.369222843865381734 ) ) ;
#15745=CARTESIAN_POINT ( 'NONE',  ( 11.45406335465086833, 12.08730048838598314, 5.725135792998135464 ) ) ;
#15748=CARTESIAN_POINT ( 'NONE',  ( 2.448534668620959476, 11.21351766718956178, 3.448322903900380432 ) ) ;
#15753=CARTESIAN_POINT ( 'NONE',  ( -0.3242065045807352996, 20.30684170721071879, 4.841807950102050562 ) ) ;
#15758=CARTESIAN_POINT ( 'NONE',  ( 10.31539917732810707, 10.57772775276799315, 2.222527011904729122 ) ) ;
#15761=CARTESIAN_POINT ( 'NONE',  ( 11.21902111245313627, 16.87095629309551725, -3.573519051852731554 ) ) ;
#15763=CARTESIAN_POINT ( 'NONE',  ( 0.04635182712760341911, 17.19594618500607908, 0.8198292707330264717 ) ) ;
#15767=CARTESIAN_POINT ( 'NONE',  ( -0.08564316121918838509, 21.03045532789668925, 5.121204207707737766 ) ) ;
#15772=CARTESIAN_POINT ( 'NONE',  ( 6.062168776474054610, 18.80106227311165767, -0.8723543407741434219 ) ) ;
#15773=CARTESIAN_POINT ( 'NONE',  ( 8.224353621346322640, 11.48768387232824217, 1.845154662582578542 ) ) ;
#15774=CARTESIAN_POINT ( 'NONE',  ( 3.175397852148950761, 11.32322398379630179, 5.121166436712352166 ) ) ;
#15781=CARTESIAN_POINT ( 'NONE',  ( 11.33455399463139734, 17.71700346048863395, 7.528911907053374541 ) ) ;
#15783=CARTESIAN_POINT ( 'NONE',  ( 10.64372375218282407, 11.67083583707339045, 3.665092760906087044 ) ) ;
#15785=CARTESIAN_POINT ( 'NONE',  ( 13.21690244079663934, 22.21723637171626464, 1.444646363038201597 ) ) ;
#15786=CARTESIAN_POINT ( 'NONE',  ( 3.777296294006362576, 11.64801722256006045, 2.252079683228215057 ) ) ;
#15808=CARTESIAN_POINT ( 'NONE',  ( 4.177528246928537747, 11.26628406262684301, 1.990635909573889473 ) ) ;
#15811=CARTESIAN_POINT ( 'NONE',  ( 4.811567550396895321, 11.20075355227730185, 4.778909014656798071 ) ) ;
#15816=CARTESIAN_POINT ( 'NONE',  ( 1.300001150583172116, 13.18543556399213124, 7.424019162913821468 ) ) ;
#15823=CARTESIAN_POINT ( 'NONE',  ( 3.602201510832755638, 16.49131183736701800, 9.203092360088074741 ) ) ;
#15826=CARTESIAN_POINT ( 'NONE',  ( 5.691239657922468886, 14.17727879546418812, 7.604247685195596240 ) ) ;
#15833=CARTESIAN_POINT ( 'NONE',  ( 10.22892371477560403, 21.50410229886458424, 0.3058668854873597964 ) ) ;
#15835=CARTESIAN_POINT ( 'NONE',  ( 11.63891272997743442, 10.83756077274092355, -0.7463790179119675905 ) ) ;
#15839=CARTESIAN_POINT ( 'NONE',  ( 7.255630842477019726, 16.46413444789888558, -2.887487180789374719 ) ) ;
#15842=CARTESIAN_POINT ( 'NONE',  ( 5.601911010437768290, 14.57750533428744255, -1.041327773958115710 ) ) ;
#15845=CARTESIAN_POINT ( 'NONE',  ( 1.868540122251793001, 20.38723677272791690, 4.979979739744280209 ) ) ;
#15847=CARTESIAN_POINT ( 'NONE',  ( 13.96517196999903376, 21.80725978669622123, 2.219877022834359170 ) ) ;
#15848=CARTESIAN_POINT ( 'NONE',  ( 4.883189917998404184, 12.13604628887379100, 5.162602853463313046 ) ) ;
#15849=CARTESIAN_POINT ( 'NONE',  ( 6.256221673970314257, 10.85576871210978211, 2.354533235149611770 ) ) ;
#15850=CARTESIAN_POINT ( 'NONE',  ( 0.4262966382305843349, 20.71823079690684466, 6.782306411708023397 ) ) ;
#15852=CARTESIAN_POINT ( 'NONE',  ( 3.341519096695713564, 13.61484622919644139, 7.613859718236023255 ) ) ;
#15858=CARTESIAN_POINT ( 'NONE',  ( 10.70904873084618281, 10.90722994128907253, 3.871866132961096163 ) ) ;
#15861=B_SPLINE_SURFACE_WITH_KNOTS ( 'NONE', 3, 3, ( 
 ( #12921, #19631, #20055, #13250, #1388, #16866, #6486, #20161, #8351, #3161, #11464, #21839, #51, #16769, #15122, #18412, #9893, #1711, #6912, #16971, #1821, #20375, #19959, #3062, #6693, #169, #8564, #13453, #8130, #9785, #21737, #1608, #5038, #4831, #18210, #3387, #15340, #13675, #16554, #14909, #6805, #11566, #8247, #5141, #18303, #13351, #21625, #1501, #16658, #15019, #6590, #4925, #11673, #15223, #10016, #3283, #11789, #18521, #13565, #10120, #8450, #20269, #11893, #18621, #3488, #10224, #20488 ),
 ( #17191, #2379, #12331, #2265, #17423, #17301, #5571, #14013, #7140, #2148, #502, #3600, #15674, #19057, #9106, #8892, #15887, #20605, #275, #3710, #13908, #8674, #5691, #18733, #7253, #1930, #17531, #712, #4040, #15556, #12225, #5240, #15781, #9005, #10786, #10452, #10342, #7462, #14233, #607, #20716, #7015, #17085, #12120, #15448, #19176, #3932, #7351, #10676, #20824, #5357, #5463, #14118, #12001, #13782, #18844, #2031, #8775, #18948, #387, #12452, #3821, #10555, #14335, #4671, #18160, #7574 ),
 ( #9633, #21051, #5903, #21455, #1446, #829, #4554, #16399, #12562, #11411, #3222, #3014, #12977, #8301, #4148, #8194, #19685, #10886, #11293, #18356, #16001, #9217, #16501, #1236, #18044, #14966, #19286, #21569, #2900, #9960, #6427, #18253, #11510, #9739, #13197, #8078, #7977, #1337, #14853, #17634, #19906, #4780, #16719, #3112, #1557, #14749, #6312, #13086, #19792, #2486, #21683, #9838, #16608, #6543, #11620, #20951, #20007, #13304, #4876, #5807, #3657, #12061, #10069, #10281, #6865, #224, #13624 ),
 ( #20323, #18788, #15402, #3543, #10402, #17147, #15289, #18471, #11846, #1987, #17031, #3439, #5193, #8728, #1877, #15504, #16818, #11946, #10173, #1763, #1658, #4981, #20427, #5097, #18900, #18673, #8625, #13399, #6964, #18574, #16916, #8397, #12176, #332, #3339, #6749, #7077, #13730, #13844, #15073, #11738, #20549, #5411, #3772, #5295, #10507, #17251, #2093, #21787, #6634, #115, #15171, #8509, #20109, #2, #13515, #20223, #2545, #17584, #17694, #3882, #5755, #3991, #17478, #10619, #20663, #14287 ),
 ( #5954, #11057, #21005, #10835, #17369, #5521, #15731, #19006, #885, #19234, #12610, #5852, #9278, #8952, #2323, #2436, #12718, #15614, #4317, #559, #21102, #659, #19443, #12510, #16053, #13964, #2213, #14179, #4096, #7303, #12282, #7626, #17812, #19121, #14067, #20774, #9056, #10938, #5636, #12396, #10735, #452, #20884, #8837, #9161, #15833, #7203, #7406, #14388, #15945, #773, #7525, #19335, #4202, #12842, #19765, #12953, #17912, #4755, #982, #2990, #14617, #21658, #9715, #21540, #14828, #14725 ),
 ( #16372, #13170, #13280, #11162, #6185, #19986, #11267, #18132, #11598, #11386, #6520, #14943, #19881, #7953, #6285, #9605, #1097, #6401, #4857, #8165, #2658, #9388, #2759, #16155, #13060, #7733, #14494, #4640, #21212, #6070, #19660, #21431, #16479, #9494, #19563, #1313, #4431, #16265, #7840, #21324, #11491, #4528, #18014, #18235, #2873, #1210, #8056, #3092, #9818, #16586, #1422, #1533, #5073, #199, #16894, #306, #5170, #8375, #20404, #11921, #8277, #3316, #5271, #20522, #18651, #15376, #11710 ),
 ( #13600, #3520, #8600, #15048, #10256, #11823, #16796, #10047, #10149, #6941, #7049, #4955, #21870, #13816, #18552, #17004, #5389, #1857, #18335, #8701, #15149, #3196, #1744, #15263, #16693, #8483, #6724, #13486, #18445, #15480, #12031, #6614, #1635, #13704, #18765, #3634, #9930, #21762, #10376, #17123, #13379, #90, #1963, #20088, #6841, #20202, #3416, #20301, #10481, #421, #8927, #18979, #7173, #5495, #532, #3853, #7281, #17223, #12257, #13938, #20635, #2065, #3748, #2185, #8806, #10591, #17337 ),
 ( #15704, #20749, #15582, #14042, #5606, #12366, #12153, #18877, #7129, #12219, #265, #11994, #5029, #21831, #16857, #20153, #2022, #20366, #13774, #15437, #3703, #10111, #18613, #18722, #13898, #16761, #5455, #1702, #378, #1812, #20597, #6901, #17183, #15113, #3379, #15333, #13665, #18512, #6686, #8765, #18938, #20261, #8443, #15214, #10216, #12110, #11780, #43, #5133, #1600, #158, #10008, #5231, #6796, #8342, #13445, #18835, #13556, #11885, #3479, #16963, #8556, #3592, #10333, #17077, #1920, #10444 ),
 ( #8665, #7007, #20477, #5347, #15547, #12443, #2258, #10667, #17521, #14329, #14430, #12320, #7344, #21147, #19171, #19277, #12773, #12554, #7670, #16097, #15773, #6000, #2369, #702, #2140, #9097, #14110, #599, #19047, #926, #12655, #14006, #17416, #7568, #10877, #21046, #3810, #15665, #19382, #5894, #10545, #15876, #821, #4137, #14222, #4250, #10986, #4034, #7247, #20815, #17742, #20940, #5681, #7449, #2590, #17627, #9325, #20708, #5799, #2480, #9208, #15991, #494, #17293, #10777, #8995, #8883 ) ),
 .UNSPECIFIED., .F., .F., .F.,
 ( 4, 1, 1, 1, 1, 1, 4 ),
 ( 4, 1, 1, 1, 1, 1, 1, 1, 1, 1, 1, 1, 1, 1, 1, 1, 1, 1, 1, 1, 1, 1, 1, 1, 1, 1, 1, 1, 1, 1, 1, 1, 1, 1, 1, 1, 1, 1, 1, 1, 1, 1, 1, 1, 1, 1, 1, 1, 1, 1, 1, 1, 1, 1, 1, 1, 1, 1, 1, 1, 1, 1, 1, 1, 4 ),
 ( 0.4887878733748999838, 0.5000000000000000000, 0.6250000000000000000, 0.7500000000000000000, 0.8750000000000000000, 1.000000000000000000, 1.011212126625000041 ),
 ( -0.02000000000000000042, -0.003749999999999999861, 0.01250000000000000069, 0.02875000000000000125, 0.04499999999999999833, 0.06124999999999999889, 0.07749999999999999944, 0.09375000000000000000, 0.1100000000000000006, 0.1262500000000000011, 0.1424999999999999878, 0.1587500000000000022, 0.1749999999999999889, 0.1912500000000000033, 0.2074999999999999900, 0.2237500000000000044, 0.2399999999999999911, 0.2562499999999999778, 0.2725000000000000200, 0.2887500000000000067, 0.3049999999999999933, 0.3212499999999999800, 0.3375000000000000222, 0.3537500000000000089, 0.3699999999999999956, 0.3862499999999999822, 0.4025000000000000244, 0.4187500000000000111, 0.4349999999999999978, 0.4512499999999999845, 0.4675000000000000266, 0.4837500000000000133, 0.5000000000000000000, 0.5162499999999999867, 0.5324999999999999734, 0.5487499999999999600, 0.5649999999999999467, 0.5812500000000000444, 0.5975000000000000311, 0.6137500000000000178, 0.6300000000000000044, 0.6462499999999999911, 0.6624999999999999778, 0.6787499999999999645, 0.6949999999999999512, 0.7112500000000000488, 0.7275000000000000355, 0.7437500000000000222, 0.7600000000000000089, 0.7762499999999999956, 0.7924999999999999822, 0.8087499999999999689, 0.8249999999999999556, 0.8412500000000000533, 0.8575000000000000400, 0.8737500000000000266, 0.8900000000000000133, 0.9062500000000000000, 0.9224999999999999867, 0.9387499999999999734, 0.9549999999999999600, 0.9712499999999999467, 0.9875000000000000444, 1.003749999999999920, 1.020000000000000018 ),
 .UNSPECIFIED. ) ;
#15863=CARTESIAN_POINT ( 'NONE',  ( 11.43322488496470157, 12.38805227212553106, -1.775723318043512799 ) ) ;
#15864=CARTESIAN_POINT ( 'NONE',  ( 5.364804770603153194, 14.99291397360876132, -1.985349221369826500 ) ) ;
#15866=CARTESIAN_POINT ( 'NONE',  ( 3.267967622520437931, 13.61749910441900191, 7.632369304580858937 ) ) ;
#15874=CARTESIAN_POINT ( 'NONE',  ( 9.425691308541154001, 13.73439867555944716, -2.265729419357018326 ) ) ;
#15875=CARTESIAN_POINT ( 'NONE',  ( 4.909756017696536468, 18.80479460024974614, 7.293209006630767099 ) ) ;
#15876=CARTESIAN_POINT ( 'NONE',  ( 9.290483991089809379, 15.41846441754162456, -2.879978118279780563 ) ) ;
#15878=CARTESIAN_POINT ( 'NONE',  ( 2.761194845577150669, 20.74767509450332170, 6.499773152090608797 ) ) ;
#15886=CARTESIAN_POINT ( 'NONE',  ( 11.18338078536718427, 16.32796899754609043, 6.823261089681437852 ) ) ;
#15887=CARTESIAN_POINT ( 'NONE',  ( 9.538671442711894599, 14.64581734927065249, 7.844515866693947181 ) ) ;
#15891=CARTESIAN_POINT ( 'NONE',  ( 10.41107459178117978, 11.41251432934954302, 2.646321841035150335 ) ) ;
#15894=CARTESIAN_POINT ( 'NONE',  ( 0.5564837971381878523, 19.70421451463541018, 7.041132247275984746 ) ) ;
#15895=CARTESIAN_POINT ( 'NONE',  ( 1.456693750638721641, 13.27625335140768215, 0.8154936714224948480 ) ) ;
#15898=CARTESIAN_POINT ( 'NONE',  ( 7.532599918355038504, 15.95844914551919302, 8.384485894956869245 ) ) ;
#15902=ORIENTED_EDGE ( 'NONE', *, *, #16161, .T. ) ;
#15922=CARTESIAN_POINT ( 'NONE',  ( 5.595233681759747668, 13.84461567157916662, 8.302901642620097888 ) ) ;
#15925=CARTESIAN_POINT ( 'NONE',  ( 5.363079780418651410, 12.55216059408865092, 7.235226968914967749 ) ) ;
#15935=CARTESIAN_POINT ( 'NONE',  ( 2.461191507070185303, 20.72975021207655288, 6.582046662092221112 ) ) ;
#15938=CARTESIAN_POINT ( 'NONE',  ( 1.904212788493860220, 17.24875406955469259, 9.107061817004916904 ) ) ;
#15945=CARTESIAN_POINT ( 'NONE',  ( 12.57069057875543550, 18.63767531088674190, 6.547553293110945027 ) ) ;
#15948=CARTESIAN_POINT ( 'NONE',  ( 13.38722737856375744, 14.77849355198858206, 6.969650373707040991 ) ) ;
#15952=CARTESIAN_POINT ( 'NONE',  ( 7.281201052484665759, 13.72469829375204675, -2.239932892534894471 ) ) ;
#15953=CARTESIAN_POINT ( 'NONE',  ( 7.318285782056717537, 16.58796963715414208, 7.711759744564571584 ) ) ;
#15955=CARTESIAN_POINT ( 'NONE',  ( 9.153486460148078763, 17.16681038731015008, 7.158488902892022665 ) ) ;
#15956=CARTESIAN_POINT ( 'NONE',  ( 7.289870466149695361, 14.17692335100063161, 7.110251240425253805 ) ) ;
#15961=CARTESIAN_POINT ( 'NONE',  ( 7.199513328304186999, 11.36662928180900245, 4.932186602622403271 ) ) ;
#15962=CARTESIAN_POINT ( 'NONE',  ( 5.134883484631279416, 19.21498006567040306, 8.078918003304201179 ) ) ;
#15963=CARTESIAN_POINT ( 'NONE',  ( 1.548165812409910025, 17.46078721926186361, 9.485929473351337293 ) ) ;
#15965=CARTESIAN_POINT ( 'NONE',  ( 1.883633422024908022, 16.41907190720915466, -0.01618598629114483337 ) ) ;
#15975=CARTESIAN_POINT ( 'NONE',  ( 11.42442798422983685, 14.30946655864417671, 7.226238609427539039 ) ) ;
#15979=CARTESIAN_POINT ( 'NONE',  ( 11.49429421792066996, 18.69515674907532699, -3.066687557635257910 ) ) ;
#15980=CARTESIAN_POINT ( 'NONE',  ( 5.377061541145786272, 14.53036832121391164, -1.845926119401802623 ) ) ;
#15982=CARTESIAN_POINT ( 'NONE',  ( 1.878793507312973787, 13.53433865536812064, 1.020842242705974678 ) ) ;
#15990=CARTESIAN_POINT ( 'NONE',  ( 7.540178019304795143, 16.36402550683704860, -2.249428100403033870 ) ) ;
#15991=CARTESIAN_POINT ( 'NONE',  ( 11.75259991899696033, 19.71652463870320204, -2.548980710552388285 ) ) ;
#15996=CARTESIAN_POINT ( 'NONE',  ( 5.276755280550131211, 18.51750724673628667, 8.329952144543302239 ) ) ;
#16001=CARTESIAN_POINT ( 'NONE',  ( 8.070802031145120736, 10.68384337266676276, 1.758507783024191973 ) ) ;
#16005=CARTESIAN_POINT ( 'NONE',  ( 10.25666463770645365, 11.36678447621568289, 1.976058869409572205 ) ) ;
#16006=CARTESIAN_POINT ( 'NONE',  ( 1.345153252091858542, 17.14040452170628370, 8.773309266493196645 ) ) ;
#16007=CARTESIAN_POINT ( 'NONE',  ( 2.873840625336028243, 18.12196835462199829, 8.704036440046063916 ) ) ;
#16030=CARTESIAN_POINT ( 'NONE',  ( 7.541081845515885007, 16.64385683817606321, 8.488075708221099802 ) ) ;
#16033=CARTESIAN_POINT ( 'NONE',  ( 3.585433298076192710, 13.67760018920084164, -0.7025886874450966157 ) ) ;
#16038=CARTESIAN_POINT ( 'NONE',  ( 2.957488341128261311, 12.27600719534943607, 5.634643733745038574 ) ) ;
#16045=CARTESIAN_POINT ( 'NONE',  ( 2.892783912874654639, 11.35831051514739976, 5.278155357869695585 ) ) ;
#16047=CARTESIAN_POINT ( 'NONE',  ( 7.614317487531611306, 16.59395432398027381, 7.713385099270380074 ) ) ;
#16053=CARTESIAN_POINT ( 'NONE',  ( 6.911024701182626018, 16.37218494104095967, -2.488299197932800855 ) ) ;
#16057=CARTESIAN_POINT ( 'NONE',  ( 12.30817927592476835, 10.43710490882117981, 2.034649068642048864 ) ) ;
#16061=CARTESIAN_POINT ( 'NONE',  ( 7.885219324757854586, 20.04620933819776241, -1.563507728803273045 ) ) ;
#16064=CARTESIAN_POINT ( 'NONE',  ( 7.753549000504421862, 20.82617040976970202, 3.772397917800740075 ) ) ;
#16066=CARTESIAN_POINT ( 'NONE',  ( 2.082326296619658734, 20.28604016155938794, 5.534141863331107025 ) ) ;
#16070=CARTESIAN_POINT ( 'NONE',  ( 9.316887094131077518, 18.56746232396120533, 7.628866700226834219 ) ) ;
#16074=CARTESIAN_POINT ( 'NONE',  ( 1.125632047368157584, 11.63764180229748213, 6.559284911491262804 ) ) ;
#16075=CARTESIAN_POINT ( 'NONE',  ( 0.6387658443185789681, 11.44537632918167169, 4.316053075454154175 ) ) ;
#16077=CARTESIAN_POINT ( 'NONE',  ( 4.942683224323132229, 18.75934072859504198, 7.437106419775259880 ) ) ;
#16083=CARTESIAN_POINT ( 'NONE',  ( 11.39144718466197226, 13.80490758105914750, 7.009419656893866701 ) ) ;
#16086=CARTESIAN_POINT ( 'NONE',  ( 5.424505126996017168, 13.78855881373742776, -1.522162338289739125 ) ) ;
#16095=CARTESIAN_POINT ( 'NONE',  ( 8.491692939339465340, 11.40205806595764138, 1.750967937658206797 ) ) ;
#16096=CARTESIAN_POINT ( 'NONE',  ( 5.299847422448394241, 16.73342696359956605, 8.025596137169321409 ) ) ;
#16097=CARTESIAN_POINT ( 'NONE',  ( 8.610284304070962236, 11.53658052784436094, 3.528423034965584293 ) ) ;
#16101=CARTESIAN_POINT ( 'NONE',  ( 4.649021650351502721, 20.44826945341173641, 6.786196569202606277 ) ) ;
#16106=CARTESIAN_POINT ( 'NONE',  ( 11.25455419701103921, 21.25597139212561260, 1.837441195538858763 ) ) ;
#16108=CARTESIAN_POINT ( 'NONE',  ( 0.3634868636840050682, 19.95706598340423099, 6.556391343133318728 ) ) ;
#16115=CARTESIAN_POINT ( 'NONE',  ( 0.4550004815227328137, 18.61582597019792118, 1.433257286243621920 ) ) ;
#16120=CARTESIAN_POINT ( 'NONE',  ( 1.944368897882448266, 16.62334027767684930, 0.06855819222581667483 ) ) ;
#16130=CARTESIAN_POINT ( 'NONE',  ( 0.8544710534764644594, 20.20188058797412012, 7.859027440807365927 ) ) ;
#16133=CARTESIAN_POINT ( 'NONE',  ( 3.707196599236265211, 17.88651271022806100, -1.213880038145912721 ) ) ;
#16137=CARTESIAN_POINT ( 'NONE',  ( 0.9999235395336120158, 12.37449380620932260, 5.956091945474599747 ) ) ;
#16146=CARTESIAN_POINT ( 'NONE',  ( 3.519663612133736130, 13.19443745317615324, 8.148135684914707966 ) ) ;
#16155=CARTESIAN_POINT ( 'NONE',  ( 7.100511544796050956, 14.62096091062142023, -1.910049678553054076 ) ) ;
#16159=CARTESIAN_POINT ( 'NONE',  ( 11.45688759763531017, 19.74712408279570397, -3.340234307731413832 ) ) ;
#16161=EDGE_CURVE ( 'NONE', #8219, #14025, #1609, .T. ) ;
#16164=CARTESIAN_POINT ( 'NONE',  ( 7.219586368393647646, 15.63079142330355431, -2.842886198857130342 ) ) ;
#16166=CARTESIAN_POINT ( 'NONE',  ( 8.943293099748036212, 18.40455973696678171, 6.765881260930631136 ) ) ;
#16169=CARTESIAN_POINT ( 'NONE',  ( 2.339047551884789300, 20.04416362538683316, 6.193340813788498878 ) ) ;
#16173=CARTESIAN_POINT ( 'NONE',  ( 6.573394049933097172, 10.79308423060320088, 3.201986252843589842 ) ) ;
#16176=CARTESIAN_POINT ( 'NONE',  ( 1.263792660725098438, 18.94197024501346505, 8.993320458267341166 ) ) ;
#16177=CARTESIAN_POINT ( 'NONE',  ( 1.645748489547319116, 13.85855418379529702, 8.959199678648232634 ) ) ;
#16179=CARTESIAN_POINT ( 'NONE',  ( 2.541631375165741780, 19.25518317520560174, 0.9982165646741868459 ) ) ;
#16185=CARTESIAN_POINT ( 'NONE',  ( 9.472187362630734242, 11.71793829268833242, -1.348010422977820921 ) ) ;
#16190=CARTESIAN_POINT ( 'NONE',  ( 11.64281951131889237, 19.29374815207993876, -2.722012555705051184 ) ) ;
#16193=CARTESIAN_POINT ( 'NONE',  ( 5.412656472264093743, 13.93293247221977715, -1.594745895433004934 ) ) ;
#16195=CARTESIAN_POINT ( 'NONE',  ( 4.492686771805626478, 11.78541955647214046, 3.831345326553988961 ) ) ;
#16196=ORIENTED_EDGE ( 'NONE', *, *, #6432, .F. ) ;
#16200=CARTESIAN_POINT ( 'NONE',  ( 7.927587859631255007, 18.10524492707348898, -2.105417880674745224 ) ) ;
#16201=CARTESIAN_POINT ( 'NONE',  ( 5.360969217315594726, 15.89262681558415302, 8.016724612055000421 ) ) ;
#16203=CARTESIAN_POINT ( 'NONE',  ( 3.546160502010647253, 11.97425653754774189, 6.753784413642313744 ) ) ;
#16214=CARTESIAN_POINT ( 'NONE',  ( 10.98450716361348611, 21.21059770410760947, 1.107460585341796033 ) ) ;
#16216=CARTESIAN_POINT ( 'NONE',  ( 1.474443682498560948, 15.66970848929637228, 8.798798342679392093 ) ) ;
#16218=CARTESIAN_POINT ( 'NONE',  ( 0.8556435366884832527, 20.72409300549792022, 3.542841960764134601 ) ) ;
#16228=CARTESIAN_POINT ( 'NONE',  ( 9.307353458992574602, 13.73189003748300685, -2.234787557808452174 ) ) ;
#16229=CARTESIAN_POINT ( 'NONE',  ( 9.397344280094475977, 11.74680749646248223, -1.572083189369575251 ) ) ;
#16240=CARTESIAN_POINT ( 'NONE',  ( 0.6936882041921323960, 20.32439072914841915, 1.798629773014991162 ) ) ;
#16243=CARTESIAN_POINT ( 'NONE',  ( 3.513372137076729906, 15.46707393753248816, -1.345952314047888843 ) ) ;
#16248=CARTESIAN_POINT ( 'NONE',  ( 2.745171094293236802, 12.05874077879421158, 4.659437464387258920 ) ) ;
#16255=CARTESIAN_POINT ( 'NONE',  ( 3.650123795476809985, 14.95939606358802365, 9.021213235581008405 ) ) ;
#16265=CARTESIAN_POINT ( 'NONE',  ( 10.00659469058676976, 11.17647817907412211, 2.270694458645354796 ) ) ;
#16270=CARTESIAN_POINT ( 'NONE',  ( 10.92231696702098098, 15.18632195086740566, -4.231608765564518926 ) ) ;
#16274=CARTESIAN_POINT ( 'NONE',  ( 8.151680067859278012, 20.73185275495596258, -0.8723213122503620243 ) ) ;
#16276=CARTESIAN_POINT ( 'NONE',  ( 8.987010725829778224, 18.18998750146314691, 6.856259478869401569 ) ) ;
#16281=CARTESIAN_POINT ( 'NONE',  ( 0.7383804360333685590, 11.42036430616624187, 4.749601484146273478 ) ) ;
#16284=CARTESIAN_POINT ( 'NONE',  ( -0.5539956361495408377, 20.04712316396406280, 3.943730590064324026 ) ) ;
#16292=CARTESIAN_POINT ( 'NONE',  ( 9.107214270684286461, 14.05054535227951185, -3.143078356159366926 ) ) ;
#16296=CARTESIAN_POINT ( 'NONE',  ( 5.365966479128769784, 15.46734445848809791, -2.079964192967793224 ) ) ;
#16298=CARTESIAN_POINT ( 'NONE',  ( 1.387271843693158591, 17.16051976808181578, 8.849130394416750534 ) ) ;
#16306=CARTESIAN_POINT ( 'NONE',  ( 8.303166099514529108, 19.61749303057682070, -1.245790386501098190 ) ) ;
#16308=CARTESIAN_POINT ( 'NONE',  ( 3.923284618780132238, 17.33544538521946876, -1.455743775410417440 ) ) ;
#16312=CARTESIAN_POINT ( 'NONE',  ( 6.662566001476148081, 11.59927578851775287, 2.759431188061297391 ) ) ;
#16320=CARTESIAN_POINT ( 'NONE',  ( 11.06533559283524148, 21.23783741712729523, 1.325821793394421411 ) ) ;
#16335=CARTESIAN_POINT ( 'NONE',  ( 11.97860041647407314, 11.13144644120788307, 0.7672358936978520561 ) ) ;
#16337=CARTESIAN_POINT ( 'NONE',  ( 10.29335322697429511, 10.45400687491624225, 2.209017800539377241 ) ) ;
#16347=CARTESIAN_POINT ( 'NONE',  ( 4.894910957408831642, 21.42306324396562189, 2.018202348579825056 ) ) ;
#16350=CARTESIAN_POINT ( 'NONE',  ( 4.360118323002954988, 20.34695651380200587, 0.3338233916395515477 ) ) ;
#16353=CARTESIAN_POINT ( 'NONE',  ( 0.8183488901082509592, 12.22193901380214065, 5.111763293916161466 ) ) ;
#16356=CARTESIAN_POINT ( 'NONE',  ( 4.111172719939895970, 12.39521241338711199, 1.660306762232565791 ) ) ;
#16362=CARTESIAN_POINT ( 'NONE',  ( 3.294987831897750574, 12.14111609449092555, 7.060071635313232008 ) ) ;
#16372=CARTESIAN_POINT ( 'NONE',  ( 6.538910913721166729, 11.94621801824261986, 4.894387607941162344 ) ) ;
#16375=CARTESIAN_POINT ( 'NONE',  ( 12.41424834072428141, 21.83950410014850974, -0.7887902040342423815 ) ) ;
#16380=CARTESIAN_POINT ( 'NONE',  ( 9.125410677652650904, 17.38129722174117120, 7.116283853237153956 ) ) ;
#16381=CARTESIAN_POINT ( 'NONE',  ( 3.342783359414524202, 16.78689288444595107, 8.424322633587635778 ) ) ;
#16384=CARTESIAN_POINT ( 'NONE',  ( 13.39756118469465029, 22.16307784260286340, 1.948616576935187750 ) ) ;
#16387=CARTESIAN_POINT ( 'NONE',  ( 4.959019311868959612, 21.41828792979770313, 2.000495739218702607 ) ) ;
#16388=CARTESIAN_POINT ( 'NONE',  ( 1.696681809872754076, 14.67257190654929566, 9.334167604556698805 ) ) ;
#16391=CARTESIAN_POINT ( 'NONE',  ( 7.273569272673938713, 16.58792154420486042, 7.724425322274861117 ) ) ;
#16399=CARTESIAN_POINT ( 'NONE',  ( 5.363510341419825522, 17.41197255053186055, -2.152950441668251891 ) ) ;
#16400=CARTESIAN_POINT ( 'NONE',  ( 10.57816040564219229, 21.72525362062316390, -0.03273866274248853070 ) ) ;
#16404=CARTESIAN_POINT ( 'NONE',  ( 7.679949084132842607, 21.66123601093154960, 3.598503736773588368 ) ) ;
#16406=CARTESIAN_POINT ( 'NONE',  ( 0.2332795718711392907, 20.17752205389220066, 6.179227157311926177 ) ) ;
#16414=CARTESIAN_POINT ( 'NONE',  ( 11.56370448131011841, 15.74068497743424189, 6.880329954670749260 ) ) ;
#16416=CARTESIAN_POINT ( 'NONE',  ( 4.938346711425525726, 18.70539829994152115, 7.357799927494061087 ) ) ;
#16419=CARTESIAN_POINT ( 'NONE',  ( -0.1301685750265853259, 15.59583246595391692, -0.03297570318400730449 ) ) ;
#16430=CARTESIAN_POINT ( 'NONE',  ( 10.83382871988236928, 21.12904306104314855, 0.7014701641843944513 ) ) ;
#16439=CARTESIAN_POINT ( 'NONE',  ( 3.752833204253988697, 16.02103694708570814, -0.6544082234691355193 ) ) ;
#16442=CARTESIAN_POINT ( 'NONE',  ( 0.2870103912946987412, 17.92877166684071710, 1.083135389032180873 ) ) ;
#16445=CARTESIAN_POINT ( 'NONE',  ( 10.65847098557893347, 21.11843953786754113, 0.3043021127257425906 ) ) ;
#16448=CARTESIAN_POINT ( 'NONE',  ( 10.41141284089941799, 21.01241846032922211, 5.365001480791137922 ) ) ;
#16456=CARTESIAN_POINT ( 'NONE',  ( 7.343712728639111731, 12.97967409473248246, 7.433702222329153564 ) ) ;
#16459=CARTESIAN_POINT ( 'NONE',  ( 3.654533980080661326, 17.51885244241539041, -1.309317591557538574 ) ) ;
#16466=CARTESIAN_POINT ( 'NONE',  ( 4.192958223415248931, 12.21630804426136230, 2.039899256093704594 ) ) ;
#16471=CARTESIAN_POINT ( 'NONE',  ( 3.491312425488612980, 13.00100667128629262, 7.999424012500742975 ) ) ;
#16479=CARTESIAN_POINT ( 'NONE',  ( 10.81808670305476028, 17.53555608635337393, 6.953175927443941973 ) ) ;
#16481=CARTESIAN_POINT ( 'NONE',  ( 11.12006939743884537, 18.08540889854115363, -4.117412775282417670 ) ) ;
#16487=CARTESIAN_POINT ( 'NONE',  ( 8.821459635400524135, 12.02303503703761223, 4.606412285287802888 ) ) ;
#16488=CARTESIAN_POINT ( 'NONE',  ( 13.70619102061564298, 21.99218769696788200, 1.831112504243990413 ) ) ;
#16490=CARTESIAN_POINT ( 'NONE',  ( 5.454615826616862506, 17.51021144529294560, 8.784396340176970241 ) ) ;
#16491=CARTESIAN_POINT ( 'NONE',  ( 1.695370511798163671, 15.71096035366437427, 9.573348142837362573 ) ) ;
#16495=CARTESIAN_POINT ( 'NONE',  ( 0.1287471594020603571, 14.29405283160754614, 1.226153466862331065 ) ) ;
#16501=CARTESIAN_POINT ( 'NONE',  ( 7.292876639776774361, 12.62524416591024057, -1.628278476874152947 ) ) ;
#16502=CARTESIAN_POINT ( 'NONE',  ( 9.610208719281146728, 19.70821819264820718, -2.605398466078559849 ) ) ;
#16505=CARTESIAN_POINT ( 'NONE',  ( 8.915785587245871113, 19.67583050180649806, 6.892551414178150537 ) ) ;
#16507=CARTESIAN_POINT ( 'NONE',  ( 3.158507891489228836, 12.59229297301672190, 6.478546931336934378 ) ) ;
#16509=CARTESIAN_POINT ( 'NONE',  ( 6.892929529354196561, 18.75718618419412564, 6.956112666771808506 ) ) ;
#16513=CARTESIAN_POINT ( 'NONE',  ( 11.32992743752204312, 12.55266643930576187, 5.310610498300123439 ) ) ;
#16515=CARTESIAN_POINT ( 'NONE',  ( 7.847407104022815716, 14.74276822600529258, 8.097202368905350056 ) ) ;
#16530=CARTESIAN_POINT ( 'NONE',  ( 13.10365782807650525, 16.69016472798375972, 6.399640439207225917 ) ) ;
#16538=CARTESIAN_POINT ( 'NONE',  ( 4.010039403972132988, 18.11389644008795585, -0.3279598888530740886 ) ) ;
#16545=CARTESIAN_POINT ( 'NONE',  ( 7.395190866011299491, 14.64975276093931100, -1.912940321280476752 ) ) ;
#16547=CARTESIAN_POINT ( 'NONE',  ( 12.00188337831979801, 21.69121361356170397, 3.968932558729561411 ) ) ;
#16553=CARTESIAN_POINT ( 'NONE',  ( 8.109003715218610964, 19.66538549285581539, -0.8655619987938839577 ) ) ;
#16554=CARTESIAN_POINT ( 'NONE',  ( 9.856817040269220342, 10.74905493727258232, 0.1947764129590014437 ) ) ;
#16561=CARTESIAN_POINT ( 'NONE',  ( -0.2589530521705579180, 13.90637430850843081, 0.5894001625122522459 ) ) ;
#16564=CARTESIAN_POINT ( 'NONE',  ( 6.263355025072034010, 21.08859062641374038, 5.475190995882099010 ) ) ;
#16569=CARTESIAN_POINT ( 'NONE',  ( 9.920056955027456880, 10.74433361426668121, 0.1741698353093955043 ) ) ;
#16576=CARTESIAN_POINT ( 'NONE',  ( 1.853075885237863929, 17.83409906757449548, -0.4903821156112312396 ) ) ;
#16586=CARTESIAN_POINT ( 'NONE',  ( 12.61172719285503341, 18.50160361240584095, 6.235549524936597976 ) ) ;
#16591=CARTESIAN_POINT ( 'NONE',  ( 8.057976852920029742, 11.73130284909294119, 1.232157028814356403 ) ) ;
#16592=CARTESIAN_POINT ( 'NONE',  ( 6.822572929214665294, 12.01675953414323139, 4.751156277397826422 ) ) ;
#16596=CARTESIAN_POINT ( 'NONE',  ( 1.761257652907455062, 13.02131026627836086, 0.3965737215900302370 ) ) ;
#16597=CARTESIAN_POINT ( 'NONE',  ( 0.1099108948849764067, 12.41872062087720607, 1.953321936160630434 ) ) ;
#16602=CARTESIAN_POINT ( 'NONE',  ( -0.7122774860577034683, 19.84248487494580004, 3.546694122126617277 ) ) ;
#16608=CARTESIAN_POINT ( 'NONE',  ( 13.17436130925518967, 12.73805723869360129, 6.175612552832564717 ) ) ;
#16609=CARTESIAN_POINT ( 'NONE',  ( 9.181556427945844590, 17.35025276895908064, -3.541092686917109766 ) ) ;
#16612=CARTESIAN_POINT ( 'NONE',  ( 8.208960929233390047, 21.21049822788766193, 5.041055855688859388 ) ) ;
#16614=CARTESIAN_POINT ( 'NONE',  ( 1.986054180200191643, 13.53163558985986192, 0.9852467751172055976 ) ) ;
#16618=CARTESIAN_POINT ( 'NONE',  ( 9.415202144866304579, 11.84307591169006102, 5.174863401006513541 ) ) ;
#16620=CARTESIAN_POINT ( 'NONE',  ( 6.575770747954134521, 10.94213887786034078, 2.272703023869682148 ) ) ;
#16624=CARTESIAN_POINT ( 'NONE',  ( 6.694325579490929101, 11.08857721632392135, 2.712616371685049987 ) ) ;
#16634=CARTESIAN_POINT ( 'NONE',  ( 13.16830043700046460, 15.09637057925005799, 6.264522879333630279 ) ) ;
#16646=CARTESIAN_POINT ( 'NONE',  ( 5.594467393561600943, 13.98451010310800768, -0.8567667164377248401 ) ) ;
#16649=CARTESIAN_POINT ( 'NONE',  ( 14.11562798333356916, 21.64660035503122160, 3.663432050408041096 ) ) ;
#16657=CARTESIAN_POINT ( 'NONE',  ( 8.659021043980340337, 20.69798781994444425, 0.5487958848404460577 ) ) ;
#16658=CARTESIAN_POINT ( 'NONE',  ( 12.65941454051080406, 20.52367786489136137, 5.608094639784014568 ) ) ;
#16664=CARTESIAN_POINT ( 'NONE',  ( 5.535619616285561762, 15.64056738454816120, 8.892138302534441152 ) ) ;
#16667=CARTESIAN_POINT ( 'NONE',  ( 7.125557253250215162, 19.02648549786798426, 7.691136940842363323 ) ) ;
#16673=CARTESIAN_POINT ( 'NONE',  ( 0.1806150403938127091, 13.36329209284379793, 2.058942537303792619 ) ) ;
#16677=CARTESIAN_POINT ( 'NONE',  ( 11.40832977423153594, 17.71807980195418608, 7.511151340609421467 ) ) ;
#16683=CARTESIAN_POINT ( 'NONE',  ( 2.295644084928958328, 19.71408608352444247, 0.5126537937488709895 ) ) ;
#16693=CARTESIAN_POINT ( 'NONE',  ( 7.359377386964466083, 16.36402550683702373, -2.195284595531059590 ) ) ;
#16701=CARTESIAN_POINT ( 'NONE',  ( 8.734026292629820887, 11.84157558182232606, 4.211351354823381854 ) ) ;
#16702=CARTESIAN_POINT ( 'NONE',  ( 6.671301235538900976, 11.80771363267201224, 4.070312667603704249 ) ) ;
#16710=CARTESIAN_POINT ( 'NONE',  ( 0.2410472161520063328, 18.96554497951561302, 0.7464930760089547590 ) ) ;
#16713=CARTESIAN_POINT ( 'NONE',  ( 1.599345239557343090, 20.41800832758468331, 3.409096474281709810 ) ) ;
#16719=CARTESIAN_POINT ( 'NONE',  ( 9.054956828960067483, 17.37326356681460382, -3.634900410956593664 ) ) ;
#16722=CARTESIAN_POINT ( 'NONE',  ( 9.191111131702870196, 13.13842489233451616, -2.664320628172200944 ) ) ;
#16723=CARTESIAN_POINT ( 'NONE',  ( 6.750174310882091078, 21.34127784185943000, 1.051171576271183072 ) ) ;
#16732=CARTESIAN_POINT ( 'NONE',  ( 9.682029097783299676, 17.29611120545237313, -3.402978531621489555 ) ) ;
#16733=CARTESIAN_POINT ( 'NONE',  ( 5.277159435657938324, 13.56613987398194254, 7.097935826007862659 ) ) ;
#16735=CARTESIAN_POINT ( 'NONE',  ( 0.9277850458616880847, 20.20533454244034033, 7.839724834913604390 ) ) ;
#16747=CARTESIAN_POINT ( 'NONE',  ( 13.16369351907254526, 14.77213119101223526, 6.175811950428527375 ) ) ;
#16757=CARTESIAN_POINT ( 'NONE',  ( 6.008532079804368209, 11.28156496648768226, 2.932085512598874733 ) ) ;
#16760=CARTESIAN_POINT ( 'NONE',  ( 12.86918211560430514, 18.46417960692862437, 6.076019728440299694 ) ) ;
#16761=CARTESIAN_POINT ( 'NONE',  ( 7.670774570915360968, 18.07295993736750361, -1.943745484816997937 ) ) ;
#16763=CARTESIAN_POINT ( 'NONE',  ( 5.633227044593422939, 12.08264022589296260, -0.3004653588455272750 ) ) ;
#16768=CARTESIAN_POINT ( 'NONE',  ( 8.501344007088352583, 20.47739890484253067, 0.1352862916589856745 ) ) ;
#16769=CARTESIAN_POINT ( 'NONE',  ( 8.817286373918717501, 20.20007397076694033, 6.586875430813535992 ) ) ;
#16774=CARTESIAN_POINT ( 'NONE',  ( 5.063315581345954719, 19.21739139815786146, 8.104051299585993462 ) ) ;
#16777=CARTESIAN_POINT ( 'NONE',  ( 7.017698028421007095, 19.43385999692815602, 7.433407674448314850 ) ) ;
#16784=CARTESIAN_POINT ( 'NONE',  ( 11.23451117572187918, 16.27132894921272310, -4.476865026338582076 ) ) ;
#16787=CARTESIAN_POINT ( 'NONE',  ( 1.659792374793198411, 15.50571454768893709, -0.6235934458232202937 ) ) ;
#16796=CARTESIAN_POINT ( 'NONE',  ( 5.473594542650097594, 15.56639808041640372, -1.390812284269987265 ) ) ;
#16805=CARTESIAN_POINT ( 'NONE',  ( 8.566873072168270653, 11.62770347711273011, 3.469410504889820501 ) ) ;
#16808=CARTESIAN_POINT ( 'NONE',  ( 0.06308363157408580779, 12.60631702034428692, 1.730364172241236620 ) ) ;
#16811=CARTESIAN_POINT ( 'NONE',  ( 1.820434556146364402, 15.68905071955487962, 8.881803553093584824 ) ) ;
#16818=CARTESIAN_POINT ( 'NONE',  ( 9.198936130449542503, 14.67110634242510159, 7.858938460866098374 ) ) ;
#16819=CARTESIAN_POINT ( 'NONE',  ( 13.31981936710468339, 16.89510937500811849, 7.147718160282645172 ) ) ;
#16821=CARTESIAN_POINT ( 'NONE',  ( 8.669746721805902112, 10.90552857616499161, 3.865604682332115516 ) ) ;
#16828=CARTESIAN_POINT ( 'NONE',  ( 5.869188306888136530, 15.50533030672313828, -1.931863268461263106 ) ) ;
#16829=CARTESIAN_POINT ( 'NONE',  ( 5.194454836083180815, 13.07028570565210224, 6.652979041940234595 ) ) ;
#16830=CARTESIAN_POINT ( 'NONE',  ( 5.573107417874706648, 17.51139020089073028, 8.753967866118298247 ) ) ;
#16833=CARTESIAN_POINT ( 'NONE',  ( 0.4276177683824305409, 12.38241104890028232, 3.439344687585752514 ) ) ;
#16841=CARTESIAN_POINT ( 'NONE',  ( 8.692131961109870630, 21.56859194724540174, 0.5848482333739358774 ) ) ;
#16844=CARTESIAN_POINT ( 'NONE',  ( 13.06483546133407891, 17.09753932500757756, 6.359823774401709429 ) ) ;
#16848=CARTESIAN_POINT ( 'NONE',  ( 4.747186406083175214, 20.72645064840772022, 2.280034233475693117 ) ) ;
#16854=CARTESIAN_POINT ( 'NONE',  ( 6.015389740508374494, 11.22565445350847213, 2.925956496411346475 ) ) ;
#16856=CARTESIAN_POINT ( 'NONE',  ( 10.66741777435992233, 21.11777521280046344, 0.3018417449422642895 ) ) ;
#16857=CARTESIAN_POINT ( 'NONE',  ( 9.031267397129903785, 18.23281813489354164, 6.939219899636122513 ) ) ;
#16858=CARTESIAN_POINT ( 'NONE',  ( 1.567589786362412196, 18.89460405061472414, 8.826553739152313227 ) ) ;
#16859=CARTESIAN_POINT ( 'NONE',  ( 6.238925459287739450, 20.69394519596638204, -0.2505430798033594364 ) ) ;
#16865=CARTESIAN_POINT ( 'NONE',  ( 9.417227436378860617, 21.07740322983227443, 2.575106661504599881 ) ) ;
#16866=CARTESIAN_POINT ( 'NONE',  ( 5.436098872970559270, 13.59057812530450171, -1.547591233524117982 ) ) ;
#16871=CARTESIAN_POINT ( 'NONE',  ( 10.92301329967130030, 14.92480105555379488, -4.179632980644835349 ) ) ;
#16872=CARTESIAN_POINT ( 'NONE',  ( 4.834045568277948846, 19.16583807351516100, 8.093579589020821530 ) ) ;
#16875=CARTESIAN_POINT ( 'NONE',  ( 5.015481723962230021, 21.32780660904764858, 2.079200966080708479 ) ) ;
#16883=CARTESIAN_POINT ( 'NONE',  ( 2.775292155461787758, 20.75260234445946850, 1.748868790410040619 ) ) ;
#16894=CARTESIAN_POINT ( 'NONE',  ( 12.13375240738266214, 11.13394627749852361, 2.666777367712576119 ) ) ;
#16896=CARTESIAN_POINT ( 'NONE',  ( 3.568489545713221300, 13.11399658182230077, 8.209792117522704658 ) ) ;
#16902=CARTESIAN_POINT ( 'NONE',  ( 9.249936709118586009, 16.07436072946943284, 7.222823812574241664 ) ) ;
#16906=CARTESIAN_POINT ( 'NONE',  ( 0.2530718558280443675, 19.01130769708743173, 0.7743534949120846056 ) ) ;
#16911=CARTESIAN_POINT ( 'NONE',  ( 6.399950078107855767, 11.66082179432958377, 2.440713941562763445 ) ) ;
#16916=CARTESIAN_POINT ( 'NONE',  ( 10.11714758980606099, 20.94030016091612367, 5.401611073718733280 ) ) ;
#16919=CARTESIAN_POINT ( 'NONE',  ( 12.71023870408584777, 20.14709925075540653, 5.798634777724255507 ) ) ;
#16922=CARTESIAN_POINT ( 'NONE',  ( 9.426324800990981245, 13.63054490249874995, 7.306473834158507152 ) ) ;
#16923=CARTESIAN_POINT ( 'NONE',  ( 6.097718537102145397, 12.01182390341870310, 1.432571743024261490 ) ) ;
#16926=CARTESIAN_POINT ( 'NONE',  ( 1.092213287054645487, 20.02445172838347887, 2.973282941953453218 ) ) ;
#16929=CARTESIAN_POINT ( 'NONE',  ( 13.82166201609697609, 21.49735766717988383, 2.189693031311231053 ) ) ;
#16930=CARTESIAN_POINT ( 'NONE',  ( 6.082277496570703157, 11.26983891803934235, 1.116890723640061145 ) ) ;
#16935=CARTESIAN_POINT ( 'NONE',  ( 2.171297880429710059, 12.53189561649392125, 2.160350752502488536 ) ) ;
#16939=PRESENTATION_STYLE_ASSIGNMENT (( #5006 ) ) ;
#16941=CARTESIAN_POINT ( 'NONE',  ( 10.99397269632869012, 12.69350398869253205, 5.272832363251270138 ) ) ;
#16942=CARTESIAN_POINT ( 'NONE',  ( 10.77664050532247941, 20.02775797062505703, 6.254703954331844784 ) ) ;
#16945=CARTESIAN_POINT ( 'NONE',  ( 12.88838202479853834, 18.27243614694899776, 6.040255587177526309 ) ) ;
#16948=CARTESIAN_POINT ( 'NONE',  ( -0.8930781184004659146, 19.84248487494580004, 3.600837626999320751 ) ) ;
#16952=CARTESIAN_POINT ( 'NONE',  ( 4.138389979685599407, 18.66904148099360583, -0.05536455928733001464 ) ) ;
#16955=CARTESIAN_POINT ( 'NONE',  ( 6.061592232884255083, 11.51780679014957087, 2.933444363316426440 ) ) ;
#16961=CARTESIAN_POINT ( 'NONE',  ( 8.995636894096717739, 18.23281813489354164, 6.949889996801141834 ) ) ;
#16962=CARTESIAN_POINT ( 'NONE',  ( 3.394140864483894848, 20.53104011336272094, 3.431716963511205254 ) ) ;
#16963=CARTESIAN_POINT ( 'NONE',  ( 11.36309470493123897, 18.10709300986449222, -3.422778098908139555 ) ) ;
#16964=CARTESIAN_POINT ( 'NONE',  ( 2.171104116788205030, 14.75527451915623267, -0.2596362615752321190 ) ) ;
#16965=CARTESIAN_POINT ( 'NONE',  ( 10.93146967960046823, 19.57756785145604184, 6.739420547765535119 ) ) ;
#16970=CARTESIAN_POINT ( 'NONE',  ( 10.99993813090866723, 17.89902992434649676, 6.574171548972360668 ) ) ;
#16971=CARTESIAN_POINT ( 'NONE',  ( 8.656775701180432492, 10.74414689430484238, 3.683671093170405086 ) ) ;
#16975=CARTESIAN_POINT ( 'NONE',  ( 2.687727953910716838, 19.71984925633132235, 8.028051864564421436 ) ) ;
#16978=CARTESIAN_POINT ( 'NONE',  ( 7.314098963983371782, 18.09774034698478218, 8.106240407049199348 ) ) ;
#16991=CARTESIAN_POINT ( 'NONE',  ( 1.872722183360863157, 17.96163139729105396, -0.4538458379064382875 ) ) ;
#17004=CARTESIAN_POINT ( 'NONE',  ( 9.151378930904229492, 16.57955862325433571, 7.339540571888535148 ) ) ;
#17005=CARTESIAN_POINT ( 'NONE',  ( 6.751629654752353105, 10.91861244885538085, 4.241390806295360250 ) ) ;
#17011=CARTESIAN_POINT ( 'NONE',  ( 7.478304415730235633, 16.36322443626852419, -2.127097502218570746 ) ) ;
#17012=CARTESIAN_POINT ( 'NONE',  ( 6.396056618077795797, 11.71523274630726164, 2.847703469759983008 ) ) ;
#17021=CARTESIAN_POINT ( 'NONE',  ( -0.1736154422522359353, 14.44032826713222128, 0.4251795190948972070 ) ) ;
#17024=CARTESIAN_POINT ( 'NONE',  ( 3.802763359353439121, 15.57349433917940651, -0.7085367696333115806 ) ) ;
#17031=CARTESIAN_POINT ( 'NONE',  ( 6.588601868897780989, 21.50782955549438213, 1.509499892929852871 ) ) ;
#17033=CARTESIAN_POINT ( 'NONE',  ( 11.33816213662683658, 22.03852486858766468, 2.072419947804004181 ) ) ;
#17038=CARTESIAN_POINT ( 'NONE',  ( 8.956708553948161011, 11.38351765046557240, 5.092834062626511837 ) ) ;
#17040=CARTESIAN_POINT ( 'NONE',  ( 1.396353529130816007, 17.16067149510373469, 8.847120485111785726 ) ) ;
#17045=CARTESIAN_POINT ( 'NONE',  ( 12.29981543294080737, 11.04557676861940152, 0.6586324886113450461 ) ) ;
#17047=CARTESIAN_POINT ( 'NONE',  ( 7.524513360980607857, 12.97967409473248246, 7.379558717456829342 ) ) ;
#17050=CARTESIAN_POINT ( 'NONE',  ( 1.069455055759913620, 18.50002798056422293, 8.344371670258649232 ) ) ;
#17054=FILL_AREA_STYLE ('',( #13421 ) ) ;
#17056=CARTESIAN_POINT ( 'NONE',  ( 10.50711560308353576, 20.71248852664919227, 5.553285430361647457 ) ) ;
#17061=CARTESIAN_POINT ( 'NONE',  ( 11.14798570045502757, 14.97143068324439952, -3.398342535127277575 ) ) ;
#17063=CARTESIAN_POINT ( 'NONE',  ( 3.436982027802252038, 14.00947850804536721, -0.1224347454001346730 ) ) ;
#17073=CARTESIAN_POINT ( 'NONE',  ( 6.132461250435506273, 11.01939018619295041, 2.875831410282900791 ) ) ;
#17075=CARTESIAN_POINT ( 'NONE',  ( 14.08082576063683966, 20.59196267482642284, 3.841811385045580618 ) ) ;
#17077=CARTESIAN_POINT ( 'NONE',  ( 13.53602369538046624, 21.41212481752907948, 2.255110409604365262 ) ) ;
#17078=CARTESIAN_POINT ( 'NONE',  ( 2.206629122547881572, 16.43321537790008335, -0.5355436742070719403 ) ) ;
#17079=CARTESIAN_POINT ( 'NONE',  ( 9.343455618504858506, 12.85930032217342145, 6.960085675539649408 ) ) ;
#17085=CARTESIAN_POINT ( 'NONE',  ( 9.164380456484101600, 17.37245550884448875, -3.663273155025991379 ) ) ;
#17091=CARTESIAN_POINT ( 'NONE',  ( 0.08330173461052782502, 11.70670645901422091, 3.276484165168652041 ) ) ;
#17094=CARTESIAN_POINT ( 'NONE',  ( 6.663477872564956606, 10.97989248988408129, 3.994247116546560061 ) ) ;
#17098=B_SPLINE_CURVE_WITH_KNOTS ( 'NONE', 3,
 ( #17619, #9200, #7559, #7120, #10439, #15767, #816 ),
 .UNSPECIFIED., .F., .F.,
 ( 4, 1, 1, 1, 4 ),
 ( 0.000000000000000000, 0.2500006855674758999, 0.4999999868738881914, 0.7499992881803003719, 1.000000000000000000 ),
 .UNSPECIFIED. ) ;
#17100=CARTESIAN_POINT ( 'NONE',  ( 0.2478183796511415904, 13.05293322038485115, 2.411138524767726832 ) ) ;
#17103=CARTESIAN_POINT ( 'NONE',  ( 1.887406236850739827, 14.81135336773366262, 0.3543419383998758221 ) ) ;
#17110=CARTESIAN_POINT ( 'NONE',  ( 2.971172838354379397, 21.01571605643849239, 2.270049746313111960 ) ) ;
#17123=CARTESIAN_POINT ( 'NONE',  ( 9.472577224383265104, 12.37763185624888074, -1.056739919939418515 ) ) ;
#17124=CARTESIAN_POINT ( 'NONE',  ( 3.581047328855178069, 13.65542567351872272, -0.8225916644656748877 ) ) ;
#17127=CARTESIAN_POINT ( 'NONE',  ( 4.627810217995094177, 11.08939391142007125, 3.992289214736410408 ) ) ;
#17131=CARTESIAN_POINT ( 'NONE',  ( 7.851649675483148627, 12.13857061077464117, 0.3032157741965843534 ) ) ;
#17134=CARTESIAN_POINT ( 'NONE',  ( 3.394489146645805810, 14.19730798917363046, 7.892569254303055004 ) ) ;
#17137=CARTESIAN_POINT ( 'NONE',  ( 2.839491163282604091, 20.06052443223327586, 7.567163413262116833 ) ) ;
#17140=CARTESIAN_POINT ( 'NONE',  ( 4.620295239943375876, 19.89361395305066083, 0.8378290896073241623 ) ) ;
#17147=CARTESIAN_POINT ( 'NONE',  ( 5.133199192818605816, 13.63276237276972047, -1.377827687522245936 ) ) ;
#17149=CARTESIAN_POINT ( 'NONE',  ( 13.38806052202257035, 14.82377123802367258, 6.981245510777174701 ) ) ;
#17153=CARTESIAN_POINT ( 'NONE',  ( 8.170188656671399485, 10.80366213796246200, 1.764733202284918034 ) ) ;
#17154=CARTESIAN_POINT ( 'NONE',  ( 7.368554159940218007, 14.94905092387569745, 7.517420915597164743 ) ) ;
#17156=CARTESIAN_POINT ( 'NONE',  ( 6.085205599414213573, 19.08150731743860717, -0.5615252065633009604 ) ) ;
#17157=CARTESIAN_POINT ( 'NONE',  ( 1.228144954732434124, 20.17113937976969140, 3.320710288574150848 ) ) ;
#17159=CARTESIAN_POINT ( 'NONE',  ( 5.973951565552006571, 12.14871438356658295, -0.3439209542975838474 ) ) ;
#17161=CARTESIAN_POINT ( 'NONE',  ( 1.758324707547593846, 16.44750854861721834, -0.8283970866775586250 ) ) ;
#17169=CARTESIAN_POINT ( 'NONE',  ( 10.40983118653084105, 20.91151375369596366, 5.294894658175683944 ) ) ;
#17171=CARTESIAN_POINT ( 'NONE',  ( 11.33353759921747539, 17.80752733036843694, -3.397307814249996394 ) ) ;
#17173=CARTESIAN_POINT ( 'NONE',  ( 2.556459638088360187, 19.27890597942106155, 7.589709452800516232 ) ) ;
#17182=CARTESIAN_POINT ( 'NONE',  ( 6.208034055486434610, 11.87704527764502060, 1.587409285954058058 ) ) ;
#17183=CARTESIAN_POINT ( 'NONE',  ( 11.10955948574564900, 17.51362067755397334, 6.777590957738523159 ) ) ;
#17184=CARTESIAN_POINT ( 'NONE',  ( 8.134723707567005135, 10.68876677029517985, 1.740177802357664616 ) ) ;
#17191=CARTESIAN_POINT ( 'NONE',  ( 6.928309554343074161, 11.28692669747560018, 5.045805056684474543 ) ) ;
#17193=CARTESIAN_POINT ( 'NONE',  ( 10.20496955028552577, 11.36774521743359223, 1.751886196687873598 ) ) ;
#17196=CARTESIAN_POINT ( 'NONE',  ( 7.251559452448354648, 14.74276822600529258, 8.275638029269909879 ) ) ;
#17199=CARTESIAN_POINT ( 'NONE',  ( 7.403462572312458967, 13.02891555264111112, 7.298645462994318045 ) ) ;
#17205=CARTESIAN_POINT ( 'NONE',  ( 2.133183598781188905, 12.85820387514107033, 1.817181390205857561 ) ) ;
#17211=CARTESIAN_POINT ( 'NONE',  ( 4.091290149016956867, 21.18971284961126145, 5.301660524291831322 ) ) ;
#17223=CARTESIAN_POINT ( 'NONE',  ( 11.21039383726165184, 12.85296284657052190, -2.355313754033094398 ) ) ;
#17224=CARTESIAN_POINT ( 'NONE',  ( 2.307410737991283600, 19.81104553907935895, 0.4478696585410927855 ) ) ;
#17226=CARTESIAN_POINT ( 'NONE',  ( 5.537219767437146167, 13.75671170515803077, 8.140707804000232528 ) ) ;
#17232=CARTESIAN_POINT ( 'NONE',  ( 7.838781466353688110, 18.78645029527194410, -1.510171260141905281 ) ) ;
#17235=CARTESIAN_POINT ( 'NONE',  ( 3.332431224701041916, 13.62386199439126599, 7.503246970460915044 ) ) ;
#17243=CARTESIAN_POINT ( 'NONE',  ( 3.485229903966501563, 17.58310126945597673, 9.057586764078154218 ) ) ;
#17247=CARTESIAN_POINT ( 'NONE',  ( 7.384935211504371821, 18.21544151669790068, 7.341947698684717416 ) ) ;
#17251=CARTESIAN_POINT ( 'NONE',  ( 11.02290331352381791, 22.07868470824458385, 2.113619312756540136 ) ) ;
#17253=CARTESIAN_POINT ( 'NONE',  ( 11.42651139047453768, 22.02362793052084200, 2.317792814824360725 ) ) ;
#17256=CARTESIAN_POINT ( 'NONE',  ( 12.95548479057611502, 21.40508096933954363, 0.7262709874220900641 ) ) ;
#17258=CARTESIAN_POINT ( 'NONE',  ( 9.385496763270603893, 17.22841133438524608, 7.914895363721495158 ) ) ;
#17259=CARTESIAN_POINT ( 'NONE',  ( 1.919263925057361542, 16.41907190720915466, -0.02685608345594442739 ) ) ;
#17261=CARTESIAN_POINT ( 'NONE',  ( 5.618432726368788543, 16.25838397047299111, -1.398541098735894606 ) ) ;
#17262=CARTESIAN_POINT ( 'NONE',  ( 7.263313943976001497, 16.57996653523900932, 7.625354271785694138 ) ) ;
#17265=CARTESIAN_POINT ( 'NONE',  ( 9.340232214130086419, 11.57391542797248007, 5.373554129697876824 ) ) ;
#17267=CARTESIAN_POINT ( 'NONE',  ( 2.985887990111508739, 19.78048590522542227, 8.004448071915154728 ) ) ;
#17268=CARTESIAN_POINT ( 'NONE',  ( 0.2766951009951102436, 20.85331682198317438, 6.385187645444293736 ) ) ;
#17271=CARTESIAN_POINT ( 'NONE',  ( 2.818516750425272388, 19.21826933052950181, 7.445547682248660593 ) ) ;
#17278=CARTESIAN_POINT ( 'NONE',  ( 9.775410964689198678, 21.72172014376007354, 3.570919871311593052 ) ) ;
#17281=CARTESIAN_POINT ( 'NONE',  ( 11.24486007184577829, 13.45202003486185127, -2.714015282924980177 ) ) ;
#17290=CARTESIAN_POINT ( 'NONE',  ( 9.332179563246018716, 16.57955862325433571, 7.285397067016122996 ) ) ;
#17293=CARTESIAN_POINT ( 'NONE',  ( 12.89786562617043586, 21.48375758380098333, 0.4863175907518038077 ) ) ;
#17294=CARTESIAN_POINT ( 'NONE',  ( 0.2312783866436057267, 17.35729252269350553, 0.02433704674567344767 ) ) ;
#17301=CARTESIAN_POINT ( 'NONE',  ( 5.427037647511713025, 13.59023913265000338, -1.545513002505085165 ) ) ;
#17304=CARTESIAN_POINT ( 'NONE',  ( 9.383108080252510419, 13.57643509814862526, -2.023504206776891134 ) ) ;
#17306=CARTESIAN_POINT ( 'NONE',  ( 12.85172960207861337, 22.16157334387418842, 0.4256939560979881021 ) ) ;
#17308=CARTESIAN_POINT ( 'NONE',  ( -0.06148638314567612950, 18.97471059823722328, 0.8203174876396049919 ) ) ;
#17311=CARTESIAN_POINT ( 'NONE',  ( 7.334099821040434009, 12.60367174608902729, 6.953311051513514585 ) ) ;
#17316=CARTESIAN_POINT ( 'NONE',  ( 0.1102113429977584769, 16.78173416929226391, 0.8122148397512033435 ) ) ;
#17321=CARTESIAN_POINT ( 'NONE',  ( 1.884251155305252112, 15.59442180266581701, 0.1340261972781983113 ) ) ;
#17337=CARTESIAN_POINT ( 'NONE',  ( 14.01635924107887199, 20.58788406416984174, 3.858321978819213349 ) ) ;
#17339=CARTESIAN_POINT ( 'NONE',  ( 0.2423679456950503242, 19.02238102577908307, 0.6537417863645457183 ) ) ;
#17342=CARTESIAN_POINT ( 'NONE',  ( 4.483212079453008592, 11.09257280940468071, 3.375105758503219811 ) ) ;
#17348=CARTESIAN_POINT ( 'NONE',  ( 7.940458870083464404, 19.15559514504086280, -1.273737374462845295 ) ) ;
#17349=CARTESIAN_POINT ( 'NONE',  ( 1.479369755814697651, 14.83370841331159973, 8.578845862358663865 ) ) ;
#17359=CARTESIAN_POINT ( 'NONE',  ( 2.447168770603926458, 20.74837111547305213, 6.544952949461906755 ) ) ;
#17363=CARTESIAN_POINT ( 'NONE',  ( 3.716496455301536717, 18.12196835462199829, 8.451690309147281255 ) ) ;
#17369=CARTESIAN_POINT ( 'NONE',  ( 5.313704621423529062, 12.39088710148332062, 0.06850381583308091937 ) ) ;
#17371=CARTESIAN_POINT ( 'NONE',  ( 12.72335754809818553, 10.91377108077479186, 3.768601682827632970 ) ) ;
#17379=CARTESIAN_POINT ( 'NONE',  ( 7.558441812221111000, 18.80437392093399396, -2.356808005286376240 ) ) ;
#17380=CARTESIAN_POINT ( 'NONE',  ( 4.555732288980417266, 19.89758433537658178, 0.8540176713598968128 ) ) ;
#17382=CARTESIAN_POINT ( 'NONE',  ( 6.008477055667284183, 18.80194823471332910, -0.7371998150550872486 ) ) ;
#17385=CARTESIAN_POINT ( 'NONE',  ( 1.580519713932151182, 20.39156962568002029, 4.231171962872529946 ) ) ;
#17388=CARTESIAN_POINT ( 'NONE',  ( 11.97441025620787514, 11.34274383772578254, -1.271560673672284869 ) ) ;
#17391=CARTESIAN_POINT ( 'NONE',  ( 1.219148700260345164, 21.11368951514764092, 3.320743722783168650 ) ) ;
#17392=CARTESIAN_POINT ( 'NONE',  ( 1.350832016589100570, 18.54689706714595232, 9.095633459574033353 ) ) ;
#17395=CARTESIAN_POINT ( 'NONE',  ( 3.729879025887206989, 14.05198016149147122, -0.1312770743009889218 ) ) ;
#17401=CARTESIAN_POINT ( 'NONE',  ( 10.62170397221806084, 10.78185011543068228, 3.503052559935591059 ) ) ;
#17406=CARTESIAN_POINT ( 'NONE',  ( 11.62317935382189660, 11.79670150420027674, -0.9113138770421064239 ) ) ;
#17415=CARTESIAN_POINT ( 'NONE',  ( 10.39407546256930281, 11.26810435610842198, 2.151588622715834731 ) ) ;
#17416=CARTESIAN_POINT ( 'NONE',  ( 11.11863957019668803, 17.51379554528373816, 6.775575702281829926 ) ) ;
#17423=CARTESIAN_POINT ( 'NONE',  ( 5.677614812627209240, 12.08210925389420076, -0.3142286978463815217 ) ) ;
#17427=CARTESIAN_POINT ( 'NONE',  ( 9.337275534366419549, 14.04566788780411635, -2.298141133598044394 ) ) ;
#17431=CARTESIAN_POINT ( 'NONE',  ( -1.102394795307540809, 20.42992192302084220, 3.974520701941598233 ) ) ;
#17434=CARTESIAN_POINT ( 'NONE',  ( 7.537868633733004309, 14.58841703367216169, 8.112932634158456224 ) ) ;
#17438=CARTESIAN_POINT ( 'NONE',  ( 0.05952623492205127986, 14.33507843624741085, 1.323949193066850771 ) ) ;
#17453=CARTESIAN_POINT ( 'NONE',  ( 3.450391172034505960, 21.44980502101282127, 3.507873031676746578 ) ) ;
#17456=CARTESIAN_POINT ( 'NONE',  ( 5.596169840114256111, 14.78911034132691427, 8.577020563439660350 ) ) ;
#17467=CARTESIAN_POINT ( 'NONE',  ( 3.584452600926797849, 16.72241728061646526, 9.195045433009065405 ) ) ;
#17469=CARTESIAN_POINT ( 'NONE',  ( 5.716839746668139988, 15.72743057685165802, 8.084269252690832630 ) ) ;
#17478=CARTESIAN_POINT ( 'NONE',  ( 12.54513423051922949, 22.19922814609550343, 0.4896788010615997777 ) ) ;
#17482=CARTESIAN_POINT ( 'NONE',  ( 12.41603076232164149, 10.50003331104365145, 2.481808480734982503 ) ) ;
#17486=CARTESIAN_POINT ( 'NONE',  ( 13.36585934105912976, 21.37707621349031228, 1.842755075219712380 ) ) ;
#17487=CARTESIAN_POINT ( 'NONE',  ( 7.739444420806847802, 11.44787533346460329, -0.07146953005562114991 ) ) ;
#17490=CARTESIAN_POINT ( 'NONE',  ( 6.121636652558352765, 11.97495218357331126, 1.622048758636034371 ) ) ;
#17491=CARTESIAN_POINT ( 'NONE',  ( 7.159321783504445591, 13.10796198399429180, 6.354849902668623152 ) ) ;
#17493=CARTESIAN_POINT ( 'NONE',  ( 9.357486251614197670, 15.29706862181782512, -3.643147517251545953 ) ) ;
#17497=CARTESIAN_POINT ( 'NONE',  ( 1.654834657223931416, 13.92071940861192658, 9.115514740275299843 ) ) ;
#17498=CARTESIAN_POINT ( 'NONE',  ( 1.199470371641251809, 19.13002063928019680, 8.749493374470841189 ) ) ;
#17500=CARTESIAN_POINT ( 'NONE',  ( 3.684248113294236404, 15.57273015692113560, -0.6781872857148856237 ) ) ;
#17507=CARTESIAN_POINT ( 'NONE',  ( 10.30969903151489753, 10.57682959022645086, 2.198775769149219794 ) ) ;
#17510=CARTESIAN_POINT ( 'NONE',  ( 11.39871391131987544, 18.20778558999124996, -3.270776772179419201 ) ) ;
#17511=CARTESIAN_POINT ( 'NONE',  ( 5.418943138485480482, 16.68965774897775844, -2.152926305030879561 ) ) ;
#17519=CARTESIAN_POINT ( 'NONE',  ( 11.29885047147741872, 14.04693538215814108, 6.356497555191443993 ) ) ;
#17521=CARTESIAN_POINT ( 'NONE',  ( 5.997264362299300267, 18.80374057110937969, -0.8573060022457920093 ) ) ;
#17522=CARTESIAN_POINT ( 'NONE',  ( 2.162650458241309526, 21.20295136681662385, 4.895597986950482650 ) ) ;
#17531=CARTESIAN_POINT ( 'NONE',  ( 7.869492175089545682, 20.10324751469710236, -1.674706184886148197 ) ) ;
#17534=CARTESIAN_POINT ( 'NONE',  ( 10.33879874242046881, 11.37625080756972196, 2.332289602398126327 ) ) ;
#17537=CARTESIAN_POINT ( 'NONE',  ( 6.821800543401555394, 11.73277151300288246, 6.051479129978276639 ) ) ;
#17540=CARTESIAN_POINT ( 'NONE',  ( 7.539611788425835570, 15.71225078316309087, 8.356678781641505793 ) ) ;
#17545=CARTESIAN_POINT ( 'NONE',  ( 0.07524201242303449333, 14.12641634776789701, 1.440853565142458548 ) ) ;
#17549=CARTESIAN_POINT ( 'NONE',  ( 2.167054928856627427, 18.10873905883254054, 0.4144402421202247888 ) ) ;
#17558=CARTESIAN_POINT ( 'NONE',  ( 13.39756118469465029, 22.16307784260286340, 1.948616576935187750 ) ) ;
#17561=CARTESIAN_POINT ( 'NONE',  ( 5.170513987664465461, 19.21498006567040306, 8.068247906139180969 ) ) ;
#17564=CARTESIAN_POINT ( 'NONE',  ( 5.308873048291212093, 12.30939206186834234, 6.978150703179593073 ) ) ;
#17569=CARTESIAN_POINT ( 'NONE',  ( 2.833759500333274506, 12.12335935744747673, 5.064409189712415049 ) ) ;
#17574=CARTESIAN_POINT ( 'NONE',  ( 3.360528770871516357, 18.30797757280501514, 8.812766717346661949 ) ) ;
#17576=CARTESIAN_POINT ( 'NONE',  ( 3.203589963913604510, 20.27761254839711924, 2.059023497881901310 ) ) ;
#17584=CARTESIAN_POINT ( 'NONE',  ( 10.64102610220981404, 14.18796137044646777, -3.896004485940504303 ) ) ;
#17587=CARTESIAN_POINT ( 'NONE',  ( 12.77823618144881657, 11.02768345846162212, 4.001507650519105397 ) ) ;
#17591=CARTESIAN_POINT ( 'NONE',  ( 7.880086733409702227, 20.03079912825525355, -1.576550733578341301 ) ) ;
#17594=CARTESIAN_POINT ( 'NONE',  ( 8.260560628456950383, 20.28274240130079065, 5.104618557005875523 ) ) ;
#17600=CARTESIAN_POINT ( 'NONE',  ( 1.869412468721153076, 18.25238594264126135, -0.4582093693669330725 ) ) ;
#17601=CARTESIAN_POINT ( 'NONE',  ( 0.7473452975581560409, 20.25628870484626631, 7.621704803408686502 ) ) ;
#17603=CARTESIAN_POINT ( 'NONE',  ( -0.8210072273473643101, 19.84627995571224091, 3.577383950576946692 ) ) ;
#17610=CARTESIAN_POINT ( 'NONE',  ( 11.21047793104343704, 12.39978222132418573, 6.074997740956973757 ) ) ;
#17612=B_SPLINE_SURFACE_WITH_KNOTS ( 'NONE', 3, 3, ( 
 ( #18553, #10048, #13380, #4957, #11711, #1211, #15264, #5390, #8807, #20751, #7050, #5607, #10377, #11923, #15377, #3635, #20302, #17339, #8485, #12154, #5171, #5496, #13939, #15705, #5272, #1964, #16896, #1745, #15584, #91, #12033, #8702, #2066, #15481, #12367, #17224, #533, #307, #18878, #18653, #2187, #423, #20636, #7174, #18981, #13601, #18766, #14043, #12258, #17124, #3854, #3963, #3749, #19093, #10592, #6842, #200, #6942, #8928, #7282, #13706, #3521, #10257, #17005, #20405, #1858, #13818 ),
 ( #20523, #10482, #8601, #634, #16130, #5729, #19418, #7603, #2411, #20979, #4406, #12484, #14262, #14364, #17668, #9137, #959, #6162, #16240, #1070, #19636, #19206, #2297, #21080, #21299, #12927, #11032, #4073, #21186, #5832, #861, #5930, #10814, #10708, #2634, #7813, #14591, #17453, #9033, #6044, #17561, #7496, #11140, #15922, #12590, #17888, #2521, #15808, #7384, #14154, #20858, #19314, #14469, #744, #4176, #10919, #9251, #12815, #4292, #16030, #12694, #17787, #9363, #7709, #19541, #2734, #9470 ),
 ( #19964, #13256, #18419, #6595, #10021, #21742, #4836, #6371, #1393, #21632, #2845, #14916, #18311, #8356, #16561, #15126, #19857, #21407, #2964, #13143, #7927, #4931, #17989, #6492, #14703, #15025, #1507, #3290, #14806, #11470, #4504, #11241, #3167, #9577, #21514, #18215, #11571, #3067, #21845, #9898, #16774, #9793, #16664, #6262, #11679, #8252, #13356, #20061, #1615, #1185, #4730, #6699, #13460, #8135, #16347, #13034, #19738, #4612, #11357, #18107, #9690, #16456, #1292, #8030, #1936, #5246, #18627 ),
 ( #3827, #7260, #6812, #11795, #8678, #8900, #15680, #20493, #15229, #8781, #8571, #10347, #17091, #13571, #20171, #12126, #10562, #17308, #5046, #2155, #15561, #60, #16975, #13914, #20275, #174, #5469, #12006, #509, #18528, #3393, #10127, #6916, #2036, #5146, #15346, #11898, #3494, #393, #7021, #16872, #10230, #18737, #15452, #1719, #7147, #1829, #20611, #8457, #13679, #20379, #279, #3607, #13789, #18955, #5364, #18850, #3718, #10459, #12231, #17196, #613, #17537, #9446, #721, #7581, #1045 ),
 ( #7469, #17431, #14446, #5579, #9227, #2272, #2607, #11002, #12790, #2385, #20957, #14019, #20723, #12671, #12338, #9112, #5813, #21058, #12569, #16218, #14343, #19513, #19292, #16007, #9011, #21163, #19393, #17761, #5909, #939, #10684, #15895, #11115, #4264, #14240, #9337, #19064, #2493, #3938, #7686, #17867, #12459, #4048, #6019, #4381, #19182, #2712, #15786, #7358, #14128, #20831, #5699, #10792, #4154, #10892, #836, #17641, #9869, #13333, #3145, #1365, #14779, #4706, #3044, #6133, #14885, #21604 ),
 ( #14558, #6466, #3260, #4904, #11331, #9996, #6344, #11446, #21277, #13230, #19940, #17970, #4813, #2820, #21718, #9556, #11546, #18284, #11981, #8654, #1592, #13431, #17173, #12099, #13765, #15323, #8427, #6783, #18710, #18823, #20465, #1799, #5017, #20250, #3690, #3579, #11875, #6892, #2013, #10318, #10434, #18497, #20354, #18603, #10204, #3369, #20142, #6994, #10101, #17063, #5223, #15203, #3470, #8754, #16848, #5125, #1909, #8542, #31, #15535, #18931, #7116, #13885, #10536, #1688, #15103, #15428 ),
 ( #16948, #145, #365, #20583, #5443, #3801, #11772, #13544, #8334, #21817, #3913, #20696, #918, #19484, #5673, #10655, #15763, #2358, #5554, #2582, #12432, #19159, #4026, #7440, #10770, #14215, #15866, #19272, #20929, #5789, #12548, #15982, #813, #14321, #5886, #6437, #6105, #7873, #4786, #4462, #12984, #18259, #18052, #6549, #2693, #20012, #16195, #19693, #14860, #11194, #21356, #19596, #12877, #13203, #19802, #1020, #17946, #2910, #14756, #13310, #19915, #2794, #21575, #14534, #9530, #21691, #7985 ),
 ( #6213, #9640, #8202, #16406, #11516, #11094, #16298, #14650, #17847, #4562, #4678, #9422, #11420, #14976, #1454, #1133, #7767, #1242, #21462, #21253, #11305, #6319, #13092, #18168, #3019, #3120, #9744, #16507, #1343, #8085, #9844, #16614, #13522, #17259, #5419, #13856, #15409, #8517, #6872, #12070, #18908, #20558, #1886, #5102, #20329, #12184, #18797, #11953, #6971, #2100, #10412, #10513, #18581, #20435, #18684, #10290, #3444, #20229, #7086, #10179, #17154, #5305, #15298, #3552, #8846, #16923, #5203 ),
 ( #15625, #3666, #3779, #463, #7211, #1770, #17040, #1994, #20670, #13973, #5530, #8633, #231, #13741, #12289, #8735, #19014, #6756, #122, #15511, #341, #13631, #11850, #3889, #10627, #1664, #8402, #15178, #7, #12520, #2445, #11066, #9287, #19131, #17703, #14075, #4000, #19452, #9170, #567, #21111, #14398, #7414, #19243, #12728, #4105, #2555, #4327, #12405, #669, #17821, #20896, #14295, #17380, #21015, #2222, #8962, #14188, #15739, #15953, #7532, #20782, #5763, #5861, #5644, #9065, #7311 ) ),
 .UNSPECIFIED., .F., .F., .F.,
 ( 4, 1, 1, 1, 1, 1, 4 ),
 ( 4, 1, 1, 1, 1, 1, 1, 1, 1, 1, 1, 1, 1, 1, 1, 1, 1, 1, 1, 1, 1, 1, 1, 1, 1, 1, 1, 1, 1, 1, 1, 1, 1, 1, 1, 1, 1, 1, 1, 1, 1, 1, 1, 1, 1, 1, 1, 1, 1, 1, 1, 1, 1, 1, 1, 1, 1, 1, 1, 1, 1, 1, 1, 1, 4 ),
 ( 0.4887878733748999838, 0.5000000000000000000, 0.6250000000000000000, 0.7500000000000000000, 0.8750000000000000000, 1.000000000000000000, 1.011212126625000041 ),
 ( -0.02000000000000000042, -0.003749999999999999861, 0.01250000000000000069, 0.02875000000000000125, 0.04499999999999999833, 0.06124999999999999889, 0.07749999999999999944, 0.09375000000000000000, 0.1100000000000000006, 0.1262500000000000011, 0.1424999999999999878, 0.1587500000000000022, 0.1749999999999999889, 0.1912500000000000033, 0.2074999999999999900, 0.2237500000000000044, 0.2399999999999999911, 0.2562499999999999778, 0.2725000000000000200, 0.2887500000000000067, 0.3049999999999999933, 0.3212499999999999800, 0.3375000000000000222, 0.3537500000000000089, 0.3699999999999999956, 0.3862499999999999822, 0.4025000000000000244, 0.4187500000000000111, 0.4349999999999999978, 0.4512499999999999845, 0.4675000000000000266, 0.4837500000000000133, 0.5000000000000000000, 0.5162499999999999867, 0.5324999999999999734, 0.5487499999999999600, 0.5649999999999999467, 0.5812500000000000444, 0.5975000000000000311, 0.6137500000000000178, 0.6300000000000000044, 0.6462499999999999911, 0.6624999999999999778, 0.6787499999999999645, 0.6949999999999999512, 0.7112500000000000488, 0.7275000000000000355, 0.7437500000000000222, 0.7600000000000000089, 0.7762499999999999956, 0.7924999999999999822, 0.8087499999999999689, 0.8249999999999999556, 0.8412500000000000533, 0.8575000000000000400, 0.8737500000000000266, 0.8900000000000000133, 0.9062500000000000000, 0.9224999999999999867, 0.9387499999999999734, 0.9549999999999999600, 0.9712499999999999467, 0.9875000000000000444, 1.003749999999999920, 1.020000000000000018 ),
 .UNSPECIFIED. ) ;
#17614=CARTESIAN_POINT ( 'NONE',  ( 6.107171055585940422, 11.13133987716735973, 1.634779367331249844 ) ) ;
#17619=CARTESIAN_POINT ( 'NONE',  ( -0.1849527131266449076, 20.23672349358593792, 5.150944217628095068 ) ) ;
#17620=CARTESIAN_POINT ( 'NONE',  ( 5.674198503080612355, 20.72820056094829866, 3.861845262972528836 ) ) ;
#17625=CARTESIAN_POINT ( 'NONE',  ( 13.90474715608841905, 20.92783617524978013, 3.353010216828454126 ) ) ;
#17627=CARTESIAN_POINT ( 'NONE',  ( 12.03200418959231932, 11.13144644120788307, 0.7512433199295541764 ) ) ;
#17628=CARTESIAN_POINT ( 'NONE',  ( 1.992131233281914993, 16.44430802189885199, -0.8027766641775135881 ) ) ;
#17630=CARTESIAN_POINT ( 'NONE',  ( 4.183994795703180891, 21.11486309459522204, 5.551682479814725291 ) ) ;
#17634=CARTESIAN_POINT ( 'NONE',  ( 9.323981051820602772, 11.74348662527086162, -1.552944996175415815 ) ) ;
#17637=CARTESIAN_POINT ( 'NONE',  ( 9.914072323211984283, 11.61724307103066245, 0.4831293664772999819 ) ) ;
#17640=CARTESIAN_POINT ( 'NONE',  ( 1.327966776992419939, 17.25716549828085888, 8.748930041179065142 ) ) ;
#17641=CARTESIAN_POINT ( 'NONE',  ( 5.815434679165389475, 20.81351436963172219, 5.507186064765134503 ) ) ;
#17644=DIRECTION ( 'NONE',  ( 1.000000000000000000, 0.000000000000000000, 0.000000000000000000 ) ) ;
#17656=CARTESIAN_POINT ( 'NONE',  ( 1.891993562269222329, 15.79923009215404583, 0.1066366400433323702 ) ) ;
#17668=CARTESIAN_POINT ( 'NONE',  ( -0.1496539994742919766, 13.90840449083211183, 0.5606114275089872923 ) ) ;
#17670=CARTESIAN_POINT ( 'NONE',  ( 3.679434963568711581, 17.70425422745077526, -1.266375082759285231 ) ) ;
#17676=CARTESIAN_POINT ( 'NONE',  ( 1.223645171401676501, 12.88107361349177715, 7.032740771049156514 ) ) ;
#17679=CARTESIAN_POINT ( 'NONE',  ( 3.319333245867002624, 13.53315903595815151, 7.428627571892030268 ) ) ;
#17683=CARTESIAN_POINT ( 'NONE',  ( 2.457276989675134526, 11.33093577474142144, 3.398861036160339744 ) ) ;
#17687=CARTESIAN_POINT ( 'NONE',  ( 2.376677803493876251, 17.97529088148273502, 0.08679864734725686870 ) ) ;
#17694=CARTESIAN_POINT ( 'NONE',  ( 10.63866352414856031, 16.27132894921270534, -4.298429365974365091 ) ) ;
#17697=CARTESIAN_POINT ( 'NONE',  ( 11.42459273946487741, 11.33173356210819982, -1.660656841338600698 ) ) ;
#17702=CARTESIAN_POINT ( 'NONE',  ( 7.444839536017474835, 18.18305382322718700, -2.602598617944788195 ) ) ;
#17703=CARTESIAN_POINT ( 'NONE',  ( 2.128425141234220774, 17.94205954657215685, 0.2447211690924122052 ) ) ;
#17705=CARTESIAN_POINT ( 'NONE',  ( 7.477064758050143034, 20.91351444903647305, 3.036128329970051887 ) ) ;
#17711=CARTESIAN_POINT ( 'NONE',  ( 9.874098502813611233, 21.84389315528099829, 3.571521444139809098 ) ) ;
#17714=CARTESIAN_POINT ( 'NONE',  ( -0.7439932220394867013, 20.80806006231328098, 3.735380117767566510 ) ) ;
#17715=CARTESIAN_POINT ( 'NONE',  ( 1.227962039276562889, 11.89880261940416695, 6.900897714592743704 ) ) ;
#17717=CARTESIAN_POINT ( 'NONE',  ( 3.996171515784880057, 20.53258833712626341, 5.065504506774320959 ) ) ;
#17726=CARTESIAN_POINT ( 'NONE',  ( 11.30218536120831807, 12.95440410905304773, 6.520132354090415028 ) ) ;
#17731=CARTESIAN_POINT ( 'NONE',  ( 11.76196212326084378, 19.67897817189895449, -2.430607981699549835 ) ) ;
#17732=CARTESIAN_POINT ( 'NONE',  ( 5.460238740336566643, 13.43797717707083805, -1.319921016749001863 ) ) ;
#17736=CARTESIAN_POINT ( 'NONE',  ( 5.163813313501020019, 20.63322025226451473, 2.513191214141544005 ) ) ;
#17741=CARTESIAN_POINT ( 'NONE',  ( 11.81737553005730490, 19.71324643990528358, -2.564459159478865935 ) ) ;
#17742=CARTESIAN_POINT ( 'NONE',  ( 13.16173767730900401, 16.70056792996117068, 6.496424000728083570 ) ) ;
#17749=CARTESIAN_POINT ( 'NONE',  ( 3.495813267034087790, 21.35899666354531945, 3.686983560158256346 ) ) ;
#17756=CARTESIAN_POINT ( 'NONE',  ( 10.13769997516062560, 20.17993208692285023, -1.137326984910994376 ) ) ;
#17758=CARTESIAN_POINT ( 'NONE',  ( 1.289267033706648746, 17.50162684153391268, 8.689449867824082574 ) ) ;
#17761=CARTESIAN_POINT ( 'NONE',  ( 2.779637312247832615, 12.24591714145684129, 6.811322434960999317 ) ) ;
#17774=CARTESIAN_POINT ( 'NONE',  ( 10.70530029303066044, 21.89451842192714182, 0.03457279810376413798 ) ) ;
#17787=CARTESIAN_POINT ( 'NONE',  ( 7.450947465380786561, 12.98226186039768137, 7.398020146545584375 ) ) ;
#17790=CARTESIAN_POINT ( 'NONE',  ( 3.615277320435647646, 17.17694927600387800, -1.367159509867317713 ) ) ;
#17801=CARTESIAN_POINT ( 'NONE',  ( 3.209779917707810348, 11.89484142146541146, 6.673094556525186682 ) ) ;
#17812=CARTESIAN_POINT ( 'NONE',  ( 10.78291357368954273, 17.61531206902142799, 7.284759546427739707 ) ) ;
#17816=CARTESIAN_POINT ( 'NONE',  ( 12.91084050336935363, 11.37372653473270390, 4.572161392691734605 ) ) ;
#17820=CARTESIAN_POINT ( 'NONE',  ( 7.605715420845187147, 11.83137677356064721, -0.6597813618126635582 ) ) ;
#17821=CARTESIAN_POINT ( 'NONE',  ( 3.737651886413042579, 15.57273015692113560, -0.6941798594830854707 ) ) ;
#17823=CARTESIAN_POINT ( 'NONE',  ( 8.605384428358668458, 19.55736841712971952, 5.976435672814039535 ) ) ;
#17825=CARTESIAN_POINT ( 'NONE',  ( 7.183656975975698522, 13.24117894531195638, 6.480836668891950758 ) ) ;
#17827=CARTESIAN_POINT ( 'NONE',  ( 11.44137618178793936, 12.37556557019096282, -2.997012553075396823 ) ) ;
#17829=CARTESIAN_POINT ( 'NONE',  ( 13.65503668246327074, 22.05527566784187243, 1.855690361662355903 ) ) ;
#17831=CARTESIAN_POINT ( 'NONE',  ( -0.1175964564627289266, 17.37652828937785543, 0.04057638788381107142 ) ) ;
#17832=CARTESIAN_POINT ( 'NONE',  ( 1.139206278029827768, 11.73021259349723167, 6.504762513190087247 ) ) ;
#17835=CARTESIAN_POINT ( 'NONE',  ( 2.059594139655736900, 13.53433865536812064, 0.9666987378332712044 ) ) ;
#17842=CARTESIAN_POINT ( 'NONE',  ( 11.38874951053466233, 13.77064647055242652, 6.993025784648827070 ) ) ;
#17845=CARTESIAN_POINT ( 'NONE',  ( 5.498135393614799860, 17.47580698470410354, -2.050589633226200359 ) ) ;
#17847=CARTESIAN_POINT ( 'NONE',  ( 1.495258403766146493, 14.30699635049795226, 8.420657258073232398 ) ) ;
#17851=CARTESIAN_POINT ( 'NONE',  ( 9.648141209897488579, 17.23623480047593404, -3.067103124126105307 ) ) ;
#17857=CARTESIAN_POINT ( 'NONE',  ( 4.562544981526344579, 20.60715472197122011, 6.559660940956183239 ) ) ;
#17863=CARTESIAN_POINT ( 'NONE',  ( 11.33566261673852793, 21.24491547887863163, 2.056737376786678784 ) ) ;
#17864=CARTESIAN_POINT ( 'NONE',  ( 0.6175707511495683866, 19.59963610279798729, 7.191875376456732027 ) ) ;
#17865=B_SPLINE_CURVE_WITH_KNOTS ( 'NONE', 3,
 ( #3130, #17958, #6451, #1253, #6225, #14663, #21474, #9855, #9982, #16312, #11316, #6118, #7993, #1351, #2806, #8095, #9540, #20024, #19703, #7888, #6331, #19817, #21369, #12997, #4576, #6559, #18066, #14767, #2928, #16624, #8215, #9654, #9755, #4690, #13214, #11434, #18179, #14988, #21703, #13320, #8645, #11967, #18811 ),
 .UNSPECIFIED., .F., .F.,
 ( 4, 3, 3, 3, 3, 3, 3, 3, 3, 3, 3, 3, 3, 3, 4 ),
 ( 0.000000000000000000, 0.09090909086281399876, 0.1818181817256480093, 0.2499255670981249955, 0.2727272725884720139, 0.3636363634512960186, 0.4545454543141200232, 0.4999095035919020047, 0.5454545451768439968, 0.6363636360396680569, 0.7272727269024920060, 0.7499460449993119449, 0.8181818177653160662, 0.9090909086281400153, 0.9999999994909640755 ),
 .UNSPECIFIED. ) ;
#17867=CARTESIAN_POINT ( 'NONE',  ( 4.635270691011046829, 18.98716039713233883, 7.878850228405285705 ) ) ;
#17870=SHAPE_REPRESENTATION_RELATIONSHIP ( 'NONE' , 'NONE' ,  #10883, #20091 ) ;
#17877=CARTESIAN_POINT ( 'NONE',  ( 6.692329841978265748, 11.82482810032952081, 4.288276300720819556 ) ) ;
#17878=CARTESIAN_POINT ( 'NONE',  ( 7.198342133457991565, 16.38025891712375781, -2.997146290384534506 ) ) ;
#17888=CARTESIAN_POINT ( 'NONE',  ( 5.026927007283006787, 11.34913591283086021, 5.616092169482095109 ) ) ;
#17891=CARTESIAN_POINT ( 'NONE',  ( 3.796584004741204499, 12.36211805266656683, 0.3638733142846966029 ) ) ;
#17902=CARTESIAN_POINT ( 'NONE',  ( 3.395237882159598541, 12.51188876831191088, 7.527755607962313356 ) ) ;
#17912=CARTESIAN_POINT ( 'NONE',  ( 10.79087687479066382, 12.58417018233828166, -2.552037637521815228 ) ) ;
#17916=CARTESIAN_POINT ( 'NONE',  ( 10.93549532874515329, 15.97885840934050883, -4.336554052330052755 ) ) ;
#17920=CARTESIAN_POINT ( 'NONE',  ( 8.468684176319758450, 21.29060048360308244, -0.02303094090340797664 ) ) ;
#17922=CARTESIAN_POINT ( 'NONE',  ( 8.984891047036883904, 18.20044315508863519, 6.851887545445102923 ) ) ;
#17923=CARTESIAN_POINT ( 'NONE',  ( 6.444640499250375854, 11.70121090254869145, 3.063182600979447390 ) ) ;
#17927=CARTESIAN_POINT ( 'NONE',  ( 11.44907295303830352, 18.36121671486396778, -4.154917505379187581 ) ) ;
#17928=CARTESIAN_POINT ( 'NONE',  ( 13.61114377367988837, 22.09400156900517942, 1.874518249454760088 ) ) ;
#17931=CARTESIAN_POINT ( 'NONE',  ( 3.234432283654637530, 11.90013693509636106, 6.894066948143128926 ) ) ;
#17932=CARTESIAN_POINT ( 'NONE',  ( 1.141638631687549088, 11.73439853126398091, 6.515573991307596735 ) ) ;
#17934=CARTESIAN_POINT ( 'NONE',  ( 1.414015556765540138, 13.15932452227622207, 7.490709649508223045 ) ) ;
#17940=CARTESIAN_POINT ( 'NONE',  ( 10.38839620284240972, 21.50507767694745453, -0.5529639877510099666 ) ) ;
#17944=CARTESIAN_POINT ( 'NONE',  ( 5.803153002628106627, 19.17693049791878934, -1.408338056234150981 ) ) ;
#17946=CARTESIAN_POINT ( 'NONE',  ( 6.097804090699195712, 20.44074137114568046, 5.245935090663635947 ) ) ;
#17952=CARTESIAN_POINT ( 'NONE',  ( 12.96175805149838212, 21.47881914407666315, 0.4678899323171995528 ) ) ;
#17955=CARTESIAN_POINT ( 'NONE',  ( 0.3048720416742233819, 19.02512202735066182, 0.6306780995777144794 ) ) ;
#17958=CARTESIAN_POINT ( 'NONE',  ( 6.432178468024032369, 11.71523184318539279, 2.836886883351238176 ) ) ;
#17967=CARTESIAN_POINT ( 'NONE',  ( 10.68594047828121418, 21.00681492881632195, 0.3047970212069722740 ) ) ;
#17968=CARTESIAN_POINT ( 'NONE',  ( 1.484066998577597385, 15.20418130093746001, 8.701018632067329506 ) ) ;
#17970=CARTESIAN_POINT ( 'NONE',  ( 0.4657302212947604381, 12.03899270364792073, 4.948057704354145159 ) ) ;
#17979=CARTESIAN_POINT ( 'NONE',  ( 9.159028214282953329, 13.35013903698374094, 6.344229879298691088 ) ) ;
#17980=CARTESIAN_POINT ( 'NONE',  ( 9.450995817226065299, 19.32892518063468046, -2.971067605327898598 ) ) ;
#17989=CARTESIAN_POINT ( 'NONE',  ( 2.914188686793144800, 19.78346126529704208, 8.029142585942892651 ) ) ;
#17992=CARTESIAN_POINT ( 'NONE',  ( 3.514438851728853397, 15.55170815036052367, -1.360445981688413353 ) ) ;
#17998=CARTESIAN_POINT ( 'NONE',  ( 4.210488876653085022, 12.18174440138109027, 2.120801485575080303 ) ) ;
#18004=CARTESIAN_POINT ( 'NONE',  ( 3.642626662481108557, 14.63523096079658181, 8.921394353827624357 ) ) ;
#18014=CARTESIAN_POINT ( 'NONE',  ( 9.052293558324171485, 17.23623480047593404, -2.888667463761888765 ) ) ;
#18018=CARTESIAN_POINT ( 'NONE',  ( 12.32999047502645773, 21.73372772506127149, -1.020500756129577580 ) ) ;
#18026=CARTESIAN_POINT ( 'NONE',  ( 8.548988628242938148, 19.70142182889846794, 5.837084678231597934 ) ) ;
#18029=CARTESIAN_POINT ( 'NONE',  ( 13.76432530034137613, 21.82393085918102571, 1.789009612944968186 ) ) ;
#18032=CARTESIAN_POINT ( 'NONE',  ( 2.439682189296471737, 11.21420404894608147, 3.451098197904673093 ) ) ;
#18033=CARTESIAN_POINT ( 'NONE',  ( 1.413168230598596864, 12.44285152367415748, 7.753309353558566208 ) ) ;
#18037=CARTESIAN_POINT ( 'NONE',  ( 3.230455007503029830, 12.59595915030716284, 6.454679934702889810 ) ) ;
#18044=CARTESIAN_POINT ( 'NONE',  ( 7.124527213025964478, 16.38034437524489206, -2.979516426361350057 ) ) ;
#18045=CARTESIAN_POINT ( 'NONE',  ( 9.276037966993236239, 18.10005428927824767, -3.373736345999344799 ) ) ;
#18050=CARTESIAN_POINT ( 'NONE',  ( 6.295715859104048739, 20.62233829775750138, -0.1650162826167260732 ) ) ;
#18052=CARTESIAN_POINT ( 'NONE',  ( 5.302404883823700565, 15.73838188847654784, 8.113367678063646338 ) ) ;
#18057=CARTESIAN_POINT ( 'NONE',  ( 11.60913865796776712, 21.44411105555546015, 1.903085412513896291 ) ) ;
#18058=CARTESIAN_POINT ( 'NONE',  ( 5.249757807197408255, 17.14787612431637598, 7.964819928734911514 ) ) ;
#18062=CARTESIAN_POINT ( 'NONE',  ( 6.572371458150938039, 21.10281604008488188, 5.417636278889840007 ) ) ;
#18066=CARTESIAN_POINT ( 'NONE',  ( 6.745904810994247214, 11.18924887071056240, 2.704525624254954685 ) ) ;
#18077=CARTESIAN_POINT ( 'NONE',  ( 10.36704172787692890, 20.61404234333509322, -0.5420488695692129433 ) ) ;
#18088=CARTESIAN_POINT ( 'NONE',  ( 0.7153167063906088474, 19.36228057343206999, 2.036841758829455618 ) ) ;
#18092=CARTESIAN_POINT ( 'NONE',  ( 6.801299041159860614, 12.02528521847468213, 4.783667443132798347 ) ) ;
#18094=CARTESIAN_POINT ( 'NONE',  ( 6.465162621008090582, 10.79737175431668206, 3.234340088657999601 ) ) ;
#18107=CARTESIAN_POINT ( 'NONE',  ( 7.434093443094676346, 16.64415285869171868, 8.524580364682270428 ) ) ;
#18110=CARTESIAN_POINT ( 'NONE',  ( 3.583776055977702324, 13.69441953482172636, -0.7122204557510644074 ) ) ;
#18113=CARTESIAN_POINT ( 'NONE',  ( 0.9676402247297362091, 12.33599599044877237, 5.805161455712580576 ) ) ;
#18116=CARTESIAN_POINT ( 'NONE',  ( 2.277511255392748790, 12.44482274936954624, 2.512107328279189034 ) ) ;
#18122=CARTESIAN_POINT ( 'NONE',  ( 2.639050747364091176, 11.24676862501781294, 4.183082657504865409 ) ) ;
#18132=CARTESIAN_POINT ( 'NONE',  ( 5.360055287488979303, 17.26127046106770635, -1.409361485115639523 ) ) ;
#18134=CARTESIAN_POINT ( 'NONE',  ( 11.49570108219309716, 19.89147748586559317, -3.243642535669593929 ) ) ;
#18139=CARTESIAN_POINT ( 'NONE',  ( 8.916212456033903777, 12.27243947381834666, 5.041701324839980458 ) ) ;
#18141=CARTESIAN_POINT ( 'NONE',  ( 3.372867663120830528, 16.47655830875484639, 8.442787653594567843 ) ) ;
#18145=CARTESIAN_POINT ( 'NONE',  ( 13.55239428341091212, 21.42532649923676402, 1.793975647907078308 ) ) ;
#18147=CARTESIAN_POINT ( 'NONE',  ( 4.560374023055850046, 10.97171856713620031, 3.825589676116931681 ) ) ;
#18148=CARTESIAN_POINT ( 'NONE',  ( 1.580932918030141687, 13.29898186247538838, 8.589096705807090615 ) ) ;
#18153=CARTESIAN_POINT ( 'NONE',  ( 0.9039476154303529576, 19.66626656054290123, 2.236627047933878121 ) ) ;
#18160=CARTESIAN_POINT ( 'NONE',  ( 14.04250245428990951, 21.64281653910636294, 3.683363989245958869 ) ) ;
#18162=CARTESIAN_POINT ( 'NONE',  ( 9.219858665001117615, 17.68564764128002409, -3.478853225350395650 ) ) ;
#18166=CARTESIAN_POINT ( 'NONE',  ( 7.157577278382974306, 21.65757474929394277, 2.163353812009434218 ) ) ;
#18168=CARTESIAN_POINT ( 'NONE',  ( 3.206323496511946480, 17.96108129601270775, 8.216359125560503074 ) ) ;
#18173=CARTESIAN_POINT ( 'NONE',  ( 13.45774086459438479, 16.70784808449734982, 6.497954125047418650 ) ) ;
#18175=CARTESIAN_POINT ( 'NONE',  ( 1.957410110268193559, 21.29427857361828202, 4.965368193760166804 ) ) ;
#18179=CARTESIAN_POINT ( 'NONE',  ( 6.586735130854707521, 10.98645991353044238, 2.737382233163811573 ) ) ;
#18187=CARTESIAN_POINT ( 'NONE',  ( 9.483053905913827464, 17.79016367847964375, -2.669168664533136948 ) ) ;
#18203=CARTESIAN_POINT ( 'NONE',  ( 9.271855056728114164, 14.88009260821627500, 7.115526499326136900 ) ) ;
#18205=CARTESIAN_POINT ( 'NONE',  ( 9.765588637266073846, 21.83972979323944230, 3.602945500523575095 ) ) ;
#18210=CARTESIAN_POINT ( 'NONE',  ( 11.44401274691345094, 13.68327412096624229, 7.073018589382568777 ) ) ;
#18215=CARTESIAN_POINT ( 'NONE',  ( 2.189264113347045626, 19.81445010932126038, 0.4794500746898018306 ) ) ;
#18217=CARTESIAN_POINT ( 'NONE',  ( 5.557121319643879787, 21.53978237414855812, 3.555717224815803768 ) ) ;
#18223=CARTESIAN_POINT ( 'NONE',  ( 4.587395795194475490, 11.87708295117914581, 3.824518294629957627 ) ) ;
#18227=CARTESIAN_POINT ( 'NONE',  ( 1.951509951783207519, 18.39930244975314722, -0.2931944764921431412 ) ) ;
#18235=CARTESIAN_POINT ( 'NONE',  ( 9.347881490430607343, 18.95229069147438139, -2.296150461628721384 ) ) ;
#18240=CARTESIAN_POINT ( 'NONE',  ( 9.271140109599555146, 14.96309120728511211, 7.029251134958126812 ) ) ;
#18243=CARTESIAN_POINT ( 'NONE',  ( 5.840875039352013687, 11.58534598419692152, 0.6053728465774781409 ) ) ;
#18244=CARTESIAN_POINT ( 'NONE',  ( 0.1136883046600123126, 18.41686720684693412, 0.4625772567203307872 ) ) ;
#18247=CARTESIAN_POINT ( 'NONE',  ( 0.2878105301525723525, 13.13938098413696132, 2.151847065340643628 ) ) ;
#18253=CARTESIAN_POINT ( 'NONE',  ( 10.86894147956441437, 19.58043239906450239, 6.762403744219564139 ) ) ;
#18255=CARTESIAN_POINT ( 'NONE',  ( 10.60219209945084273, 21.74929657561690277, 0.03335953411089977172 ) ) ;
#18257=CARTESIAN_POINT ( 'NONE',  ( 9.078296277872521358, 19.06912958161391103, 7.286269445716254900 ) ) ;
#18259=CARTESIAN_POINT ( 'NONE',  ( 5.164072674603092494, 17.31775664876643006, 8.045972464850111194 ) ) ;
#18261=CARTESIAN_POINT ( 'NONE',  ( 6.707929841484892464, 19.34112545770926062, 6.521503817312878759 ) ) ;
#18267=CARTESIAN_POINT ( 'NONE',  ( 11.28455321728826988, 19.34515354661070319, 6.288198492919301330 ) ) ;
#18269=CARTESIAN_POINT ( 'NONE',  ( 3.766814826540537453, 14.72191889613304205, 9.034809729852785409 ) ) ;
#18277=CARTESIAN_POINT ( 'NONE',  ( 10.87724638690646017, 12.23061227675764151, 4.718482727644354391 ) ) ;
#18281=CARTESIAN_POINT ( 'NONE',  ( 12.41893761992812628, 11.32628166863733021, 2.535021602169117649 ) ) ;
#18284=CARTESIAN_POINT ( 'NONE',  ( 0.09077472999913152596, 18.62527059298274068, 1.328760847605261919 ) ) ;
#18289=CARTESIAN_POINT ( 'NONE',  ( 3.970142618090055198, 17.91763227041811746, -0.4079429902366753513 ) ) ;
#18298=CARTESIAN_POINT ( 'NONE',  ( 11.47995025628694599, 10.98646219477360297, -1.324771271245920090 ) ) ;
#18302=CARTESIAN_POINT ( 'NONE',  ( 9.004191089903370582, 20.99879615889430085, 1.466809581464092016 ) ) ;
#18303=CARTESIAN_POINT ( 'NONE',  ( 10.00188843905044855, 20.90159167551892239, -1.688002078711951626 ) ) ;
#18311=CARTESIAN_POINT ( 'NONE',  ( 0.2815462692566809144, 11.62092872259188070, 3.183352938865285697 ) ) ;
#18314=CARTESIAN_POINT ( 'NONE',  ( 4.621627147662794144, 20.85603566110601292, 1.020116771113178666 ) ) ;
#18320=CARTESIAN_POINT ( 'NONE',  ( 11.23687375378556474, 14.18796137044646777, -4.074440146305448707 ) ) ;
#18323=DIRECTION ( 'NONE',  ( -0.9579671649362032637, -0.000000000000000000, 0.2868778675745010664 ) ) ;
#18325=CARTESIAN_POINT ( 'NONE',  ( 1.928551063676404942, 12.48261359942508264, 1.042194909420577131 ) ) ;
#18335=CARTESIAN_POINT ( 'NONE',  ( 8.841065195333532856, 12.18989644830414321, 5.119707677163611415 ) ) ;
#18341=CARTESIAN_POINT ( 'NONE',  ( 8.925307470792780862, 12.29983341362659566, 5.083992750741611388 ) ) ;
#18342=CARTESIAN_POINT ( 'NONE',  ( 6.493485979265003039, 11.70317488892350077, 3.279535273129327244 ) ) ;
#18344=CARTESIAN_POINT ( 'NONE',  ( 3.768677667698563383, 12.20035416735056266, 0.3928182328957318670 ) ) ;
#18345=CARTESIAN_POINT ( 'NONE',  ( -0.1933157125360287776, 15.43497882239525509, 0.1253114254156900143 ) ) ;
#18350=CARTESIAN_POINT ( 'NONE',  ( 6.278604723040791313, 20.44074137114568046, 5.191791585791021291 ) ) ;
#18356=CARTESIAN_POINT ( 'NONE',  ( 8.539960005814746680, 10.73926345162572105, 3.719695862443936463 ) ) ;
#18358=CARTESIAN_POINT ( 'NONE',  ( 10.22900826487382808, 21.26279264426276328, -0.9859047892954733161 ) ) ;
#18361=CARTESIAN_POINT ( 'NONE',  ( 6.290834976258575573, 20.61203802677264108, -0.1778393911984611497 ) ) ;
#18368=CARTESIAN_POINT ( 'NONE',  ( 7.894657137420193038, 12.88806360044558197, -1.480813047728780640 ) ) ;
#18369=CARTESIAN_POINT ( 'NONE',  ( 5.355787749307895140, 14.39168280676499556, 7.605419266839439807 ) ) ;
#18371=CARTESIAN_POINT ( 'NONE',  ( 0.8536167157666036953, 11.31186333555498180, 4.830306691737135338 ) ) ;
#18384=CARTESIAN_POINT ( 'NONE',  ( 12.78616414870638351, 12.03792853171452215, 4.155831503912295055 ) ) ;
#18393=CARTESIAN_POINT ( 'NONE',  ( 6.176127164391592927, 10.98645767192390110, 2.860351699068144349 ) ) ;
#18398=CARTESIAN_POINT ( 'NONE',  ( 8.914303899894372663, 12.18626401121546188, 5.100153663711656016 ) ) ;
#18401=CARTESIAN_POINT ( 'NONE',  ( 7.176325731368327965, 14.38111527192631200, -2.643793538748910876 ) ) ;
#18411=CARTESIAN_POINT ( 'NONE',  ( 9.496038166692052584, 21.06521520967978134, 2.786730198130631386 ) ) ;
#18412=CARTESIAN_POINT ( 'NONE',  ( 9.501456576801587062, 16.63233464712778087, 8.082444101715321239 ) ) ;
#18419=CARTESIAN_POINT ( 'NONE',  ( -0.4161015405540489098, 21.11857065418899992, 4.799063142585588082 ) ) ;
#18422=CARTESIAN_POINT ( 'NONE',  ( 6.488669288154311765, 20.75080086149703718, 6.076603587721198352 ) ) ;
#18431=CARTESIAN_POINT ( 'NONE',  ( 9.461694371501065959, 12.85627548497952155, 6.928812902285866215 ) ) ;
#18435=CARTESIAN_POINT ( 'NONE',  ( 1.811815405336057783, 13.09036154768227611, 0.4682391260633863572 ) ) ;
#18445=CARTESIAN_POINT ( 'NONE',  ( 9.026333315608731311, 21.14801334772412034, 1.793015295882868898 ) ) ;
#18452=CARTESIAN_POINT ( 'NONE',  ( 8.687903267574414556, 11.77246275954110644, 4.005785389838548483 ) ) ;
#18455=CARTESIAN_POINT ( 'NONE',  ( 3.271205700320040322, 17.33608809750036883, 8.332789245943363454 ) ) ;
#18463=CARTESIAN_POINT ( 'NONE',  ( -0.1373303213323190108, 13.91591237273533643, 0.6777295261262165083 ) ) ;
#18465=CARTESIAN_POINT ( 'NONE',  ( 5.483205516165491566, 15.73838188847654784, 8.059224173191235963 ) ) ;
#18471=CARTESIAN_POINT ( 'NONE',  ( 5.181714843770189205, 17.39297272447799614, -2.004891181105121767 ) ) ;
#18473=CARTESIAN_POINT ( 'NONE',  ( 13.16653485932300605, 18.18704292219559804, 6.886964970145631248 ) ) ;
#18475=CARTESIAN_POINT ( 'NONE',  ( 6.795993791136487161, 21.39258517102323154, 1.175440690275210587 ) ) ;
#18478=CARTESIAN_POINT ( 'NONE',  ( 6.648854909583223893, 19.49398999500200702, 6.377479405198467788 ) ) ;
#18483=CARTESIAN_POINT ( 'NONE',  ( 11.07157954474111250, 21.50410229886458424, 0.05352075458857742662 ) ) ;
#18484=CARTESIAN_POINT ( 'NONE',  ( 7.224192598190189329, 11.65531656196440125, 5.982166327705092712 ) ) ;
#18495=CARTESIAN_POINT ( 'NONE',  ( 12.61159337879046838, 19.40172461140289073, 5.406710191991988879 ) ) ;
#18497=CARTESIAN_POINT ( 'NONE',  ( 4.982102255498003451, 17.33943586079730181, 8.193447612696807880 ) ) ;
#18502=CARTESIAN_POINT ( 'NONE',  ( -0.4828751281428080300, 20.94457815382166288, 5.240160791693938336 ) ) ;
#18503=CARTESIAN_POINT ( 'NONE',  ( 3.766650751444651224, 16.23556631072887768, -0.6615111522120750154 ) ) ;
#18505=CARTESIAN_POINT ( 'NONE',  ( 6.030241924700674438, 11.44921767649160138, 2.937825647248552663 ) ) ;
#18510=CARTESIAN_POINT ( 'NONE',  ( 7.635144067882908558, 18.07295993736750361, -1.933075387652198440 ) ) ;
#18511=CARTESIAN_POINT ( 'NONE',  ( 3.857526900225019428, 20.53171221136609503, 4.646854770459164286 ) ) ;
#18512=CARTESIAN_POINT ( 'NONE',  ( 10.32152984533092521, 11.26381867368412060, 2.173457052760668251 ) ) ;
#18514=CARTESIAN_POINT ( 'NONE',  ( 9.120059585750226461, 17.37232422777100993, -3.649286426821030993 ) ) ;
#18520=CARTESIAN_POINT ( 'NONE',  ( 10.28124151015280852, 20.25644008567019583, 4.865497118489055417 ) ) ;
#18521=CARTESIAN_POINT ( 'NONE',  ( 11.15139589856166147, 12.31865010030356089, -2.978430479911657436 ) ) ;
#18527=CARTESIAN_POINT ( 'NONE',  ( 11.15439167821005029, 12.38857047172271031, -2.867789696427907931 ) ) ;
#18528=CARTESIAN_POINT ( 'NONE',  ( 2.172710587819679517, 11.29961739780916119, 3.546512833330152326 ) ) ;
#18531=CARTESIAN_POINT ( 'NONE',  ( 5.516160446314412269, 21.53913100960356175, 3.443779750929269579 ) ) ;
#18538=CARTESIAN_POINT ( 'NONE',  ( 3.748624155036380579, 14.56599487236573687, -0.2957577876794132421 ) ) ;
#18542=CARTESIAN_POINT ( 'NONE',  ( 1.672457707464642063, 14.56602435239780746, -0.3694984668618649382 ) ) ;
#18552=CARTESIAN_POINT ( 'NONE',  ( 8.921930343624811854, 18.23105645554593934, 6.967881739085774129 ) ) ;
#18553=CARTESIAN_POINT ( 'NONE',  ( -0.8735635081908617039, 20.56277232864792026, 3.239896734077844176 ) ) ;
#18560=CARTESIAN_POINT ( 'NONE',  ( 8.398975721931316585, 11.53959439960164168, 2.731685725725969238 ) ) ;
#18565=CARTESIAN_POINT ( 'NONE',  ( -0.08781225755531263388, 13.44674506006041170, 0.9678096409466712124 ) ) ;
#18568=CARTESIAN_POINT ( 'NONE',  ( 7.337216344270507840, 13.47382733369860119, 6.754120465228507619 ) ) ;
#18574=CARTESIAN_POINT ( 'NONE',  ( 9.479482390282207405, 21.75488213915048163, 3.666800339307922485 ) ) ;
#18575=CARTESIAN_POINT ( 'NONE',  ( 12.93232447009971509, 19.36079900857183489, 6.353122240160271161 ) ) ;
#18580=CARTESIAN_POINT ( 'NONE',  ( 9.494406476674157602, 15.01763621828074236, 7.831721205212923032 ) ) ;
#18581=CARTESIAN_POINT ( 'NONE',  ( 4.125927529995728094, 18.69411302701743338, -0.1543514116386320856 ) ) ;
#18583=CARTESIAN_POINT ( 'NONE',  ( 7.323328843850104519, 15.41683489813229180, 7.541440311446245381 ) ) ;
#18585=CARTESIAN_POINT ( 'NONE',  ( 13.16571366779050223, 21.56964499642510091, 0.3938296393673330065 ) ) ;
#18586=CARTESIAN_POINT ( 'NONE',  ( 5.449727700892514015, 12.34694125381258267, 7.158361069179933089 ) ) ;
#18595=CARTESIAN_POINT ( 'NONE',  ( 9.372025013462977228, 21.88221636350534993, 2.458001116284384668 ) ) ;
#18600=CARTESIAN_POINT ( 'NONE',  ( 13.01173305175439232, 17.52789639782027109, 6.278958820054959311 ) ) ;
#18603=CARTESIAN_POINT ( 'NONE',  ( 5.095392006347933211, 14.17727879546418812, 7.782683345560178267 ) ) ;
#18607=CARTESIAN_POINT ( 'NONE',  ( 4.546228995060008771, 19.82055208975022254, 0.9194446738514544526 ) ) ;
#18609=CARTESIAN_POINT ( 'NONE',  ( 6.025094433076758627, 11.18924701328941040, 2.920388319698000501 ) ) ;
#18612=CARTESIAN_POINT ( 'NONE',  ( 13.11702139709938386, 16.70050942663215210, 6.509090343710545845 ) ) ;
#18613=CARTESIAN_POINT ( 'NONE',  ( 7.580253574866159916, 13.14813038638666143, -1.062414283180728614 ) ) ;
#18614=CARTESIAN_POINT ( 'NONE',  ( 2.786775659238538871, 19.53481664226216452, 0.6126602542314601996 ) ) ;
#18615=CARTESIAN_POINT ( 'NONE',  ( 9.948484665932129545, 20.90159167551892239, -1.672009504943896552 ) ) ;
#18620=CARTESIAN_POINT ( 'NONE',  ( 8.087630817559809060, 19.60821679331170486, -0.9184393018855864232 ) ) ;
#18621=CARTESIAN_POINT ( 'NONE',  ( 12.86638604525510843, 22.28511555871962102, 0.3811982759095605133 ) ) ;
#18626=CARTESIAN_POINT ( 'NONE',  ( 10.99961054126760729, 17.04339191392503494, -4.321057179415156213 ) ) ;
#18627=CARTESIAN_POINT ( 'NONE',  ( 5.776492041582129922, 11.58109048093756321, 0.6221623434578115175 ) ) ;
#18630=CARTESIAN_POINT ( 'NONE',  ( 5.097018562294259425, 21.39650696725259849, 2.300254011810204613 ) ) ;
#18639=CARTESIAN_POINT ( 'NONE',  ( 1.709033155221383993, 13.94841408984046005, -0.1006121354318848110 ) ) ;
#18651=CARTESIAN_POINT ( 'NONE',  ( 13.22581436452122539, 21.49735766717988383, 2.368128691676176345 ) ) ;
#18653=CARTESIAN_POINT ( 'NONE',  ( 4.693615291679356538, 20.53859366438406298, 6.837946208588576269 ) ) ;
#18659=CARTESIAN_POINT ( 'NONE',  ( 7.569648848239395100, 13.31117041489053499, -1.062061557284633473 ) ) ;
#18665=CARTESIAN_POINT ( 'NONE',  ( 0.1350596924166655444, 12.33293199756963077, 2.070595033201866109 ) ) ;
#18668=CARTESIAN_POINT ( 'NONE',  ( 3.775593739218882749, 14.94275550331619229, 8.308998658764112477 ) ) ;
#18673=CARTESIAN_POINT ( 'NONE',  ( 7.162339363255674662, 18.34001794662099982, -2.492660041346614896 ) ) ;
#18677=CARTESIAN_POINT ( 'NONE',  ( 13.38176279160079396, 15.86059960773468092, 7.158817725216849226 ) ) ;
#18680=ORIENTED_EDGE ( 'NONE', *, *, #20264, .F. ) ;
#18683=CARTESIAN_POINT ( 'NONE',  ( 9.381748681430247316, 13.20209339969382079, 7.058320365009602249 ) ) ;
#18684=CARTESIAN_POINT ( 'NONE',  ( 5.070112026744222788, 20.64273285859446361, 2.209479276278648818 ) ) ;
#18689=CARTESIAN_POINT ( 'NONE',  ( 9.699271717935820547, 13.10471967957858119, 6.517988425085752269 ) ) ;
#18690=CARTESIAN_POINT ( 'NONE',  ( 5.375212648061713949, 14.86102846204294714, 7.798069169802851697 ) ) ;
#18693=CARTESIAN_POINT ( 'NONE',  ( 7.665089006313953846, 14.71660677864375799, 8.243516518557306938 ) ) ;
#18706=CARTESIAN_POINT ( 'NONE',  ( 11.35402150168352620, 17.07583819629140720, 7.537287116278762689 ) ) ;
#18708=CARTESIAN_POINT ( 'NONE',  ( 12.67900527298905367, 11.74404568948788175, 3.672993509785967170 ) ) ;
#18710=CARTESIAN_POINT ( 'NONE',  ( 2.545705333780837520, 11.94763405986570071, 5.186584416886813820 ) ) ;
#18716=CARTESIAN_POINT ( 'NONE',  ( 6.239172611192463691, 10.95050572681988044, 2.838845822508675898 ) ) ;
#18719=CARTESIAN_POINT ( 'NONE',  ( 7.404266004599425521, 14.64998413227717577, -1.914972092386549418 ) ) ;
#18720=CARTESIAN_POINT ( 'NONE',  ( 3.982060119604976745, 20.45969085187979175, 4.972192302677306053 ) ) ;
#18722=CARTESIAN_POINT ( 'NONE',  ( 7.439896507631877931, 14.64998413227717577, -1.925642189551348915 ) ) ;
#18723=CARTESIAN_POINT ( 'NONE',  ( 3.865727471797527404, 21.04679274153226132, 3.426517514587319457 ) ) ;
#18732=CARTESIAN_POINT ( 'NONE',  ( 11.21471861299752248, 14.75766247937585618, 6.567071003333057710 ) ) ;
#18733=CARTESIAN_POINT ( 'NONE',  ( 7.220654365899250138, 14.38088390058819144, -2.657754341408458565 ) ) ;
#18737=CARTESIAN_POINT ( 'NONE',  ( 5.301985385782669979, 15.65151869617330682, 8.867093223034917315 ) ) ;
#18739=EDGE_LOOP ( 'NONE', ( #16196, #7382 ) ) ;
#18740=CARTESIAN_POINT ( 'NONE',  ( 7.038019125744845006, 11.55073413761267176, 5.606060742231384175 ) ) ;
#18747=( GEOMETRIC_REPRESENTATION_CONTEXT ( 3 ) GLOBAL_UNCERTAINTY_ASSIGNED_CONTEXT ( ( #12326 ) ) GLOBAL_UNIT_ASSIGNED_CONTEXT ( ( #3461, #21806, #5215 ) ) REPRESENTATION_CONTEXT ( 'NONE', 'WORKASPACE' ) );
#18749=CARTESIAN_POINT ( 'NONE',  ( 3.878057801843542762, 13.31387814151853100, 0.5091637933335767530 ) ) ;
#18765=CARTESIAN_POINT ( 'NONE',  ( 11.11804983913708789, 14.04693538215814108, 6.410641060063417385 ) ) ;
#18766=CARTESIAN_POINT ( 'NONE',  ( 4.613777796174654888, 10.97171856713620031, 3.809597102348731834 ) ) ;
#18771=CARTESIAN_POINT ( 'NONE',  ( 7.622376558701811966, 12.99890566801571801, -0.7894648885981262465 ) ) ;
#18780=CARTESIAN_POINT ( 'NONE',  ( 0.7990183446076977170, 20.43784215561237616, 2.136429022385333720 ) ) ;
#18782=CARTESIAN_POINT ( 'NONE',  ( 0.5202139640632184037, 20.26160593876955929, 6.118137731981865279 ) ) ;
#18788=CARTESIAN_POINT ( 'NONE',  ( 6.472117061228174428, 11.13551934581288094, 4.539831998221737663 ) ) ;
#18790=CARTESIAN_POINT ( 'NONE',  ( 10.98481630133226972, 22.00956135593990126, 1.091099386501859891 ) ) ;
#18795=CARTESIAN_POINT ( 'NONE',  ( 9.257010659763754035, 12.43204336432666679, 6.443182332374063570 ) ) ;
#18797=CARTESIAN_POINT ( 'NONE',  ( 4.600923355963855599, 11.78113229454884170, 3.799008705536232711 ) ) ;
#18800=CARTESIAN_POINT ( 'NONE',  ( 5.758048114252814820, 17.57362948320378493, -1.250247827883776974 ) ) ;
#18804=CARTESIAN_POINT ( 'NONE',  ( 14.59117433460712476, 20.92287966070258065, 3.915742219214028541 ) ) ;
#18806=CARTESIAN_POINT ( 'NONE',  ( 5.189412234176333349, 13.04569946892264198, 6.627088851125058966 ) ) ;
#18807=CARTESIAN_POINT ( 'NONE',  ( -0.3434148217290114435, 21.11429744052310298, 4.777665891053347380 ) ) ;
#18811=CARTESIAN_POINT ( 'NONE',  ( 6.380166963026771221, 10.92343582149830183, 2.794643371853744007 ) ) ;
#18817=CARTESIAN_POINT ( 'NONE',  ( 11.19012038083658567, 18.30292129351066777, 7.238227121531449981 ) ) ;
#18821=CARTESIAN_POINT ( 'NONE',  ( 11.16285581286486916, 14.48099254937300095, -3.237536915232507528 ) ) ;
#18823=CARTESIAN_POINT ( 'NONE',  ( 2.203866969713045076, 11.92572550326888070, 3.650552894295490347 ) ) ;
#18830=CARTESIAN_POINT ( 'NONE',  ( 6.189386483567429487, 11.65214456485618300, 2.904983884989000398 ) ) ;
#18832=CARTESIAN_POINT ( 'NONE',  ( 11.07392898271076120, 17.51362067755397334, 6.788261054904052294 ) ) ;
#18835=CARTESIAN_POINT ( 'NONE',  ( 11.62621442616514678, 11.69902548067542192, -0.9660039452025425133 ) ) ;
#18836=CARTESIAN_POINT ( 'NONE',  ( 0.6791493861838465707, 11.70670645901422091, 3.098048504804435055 ) ) ;
#18837=CARTESIAN_POINT ( 'NONE',  ( 13.39304148437000386, 14.65557762784733598, 7.068600972872675747 ) ) ;
#18843=CARTESIAN_POINT ( 'NONE',  ( 11.19568187662517467, 16.10043549507820870, 6.812789942806879218 ) ) ;
#18844=CARTESIAN_POINT ( 'NONE',  ( 11.99126722525327082, 10.32956393789710070, 0.6475472086173773567 ) ) ;
#18847=CARTESIAN_POINT ( 'NONE',  ( 9.313964464681076194, 14.38829612573348093, -2.460586518476112872 ) ) ;
#18850=CARTESIAN_POINT ( 'NONE',  ( 5.976523806576305553, 21.10281604008488188, 5.596071939254449568 ) ) ;
#18853=CARTESIAN_POINT ( 'NONE',  ( 6.380166963026771221, 10.92343582149830183, 2.794643371853744007 ) ) ;
#18860=CARTESIAN_POINT ( 'NONE',  ( 0.4780069470470488802, 12.44023573197847199, 3.531212066111156123 ) ) ;
#18867=CARTESIAN_POINT ( 'NONE',  ( 5.434136948886521878, 17.60830669131005877, 8.646509754689903460 ) ) ;
#18877=CARTESIAN_POINT ( 'NONE',  ( 5.700318986066064575, 17.24315932450417321, -1.422019646414491856 ) ) ;
#18878=CARTESIAN_POINT ( 'NONE',  ( 4.099623927830029047, 21.31561936814513913, 5.248974889739956851 ) ) ;
#18881=CARTESIAN_POINT ( 'NONE',  ( 4.703503668085327050, 11.11441527681874142, 4.315609331493701184 ) ) ;
#18885=CARTESIAN_POINT ( 'NONE',  ( 7.888376708752765865, 12.04261116452797609, 0.4714777786467096998 ) ) ;
#18891=CARTESIAN_POINT ( 'NONE',  ( 2.888697626805730945, 19.94910490213707277, 7.692677454159938755 ) ) ;
#18894=CARTESIAN_POINT ( 'NONE',  ( 5.517512485557888091, 12.88680353640996223, 6.629587463472963904 ) ) ;
#18900=CARTESIAN_POINT ( 'NONE',  ( 6.943297528318779221, 16.37851731477712391, -2.829567754717221106 ) ) ;
#18902=CARTESIAN_POINT ( 'NONE',  ( 11.23807322027795941, 22.05295773698684059, 1.794423719884019608 ) ) ;
#18907=CARTESIAN_POINT ( 'NONE',  ( 9.444405600912201493, 16.57974156473798644, 7.980283251028787106 ) ) ;
#18908=CARTESIAN_POINT ( 'NONE',  ( 4.978313727356318275, 18.75934072859504198, 7.426436322610240559 ) ) ;
#18910=CARTESIAN_POINT ( 'NONE',  ( 5.595240304620284100, 15.74558502937677851, -1.353109612183827304 ) ) ;
#18911=CARTESIAN_POINT ( 'NONE',  ( 0.8982290014495240005, 19.73309768672615405, 2.485244984172155114 ) ) ;
#18914=CARTESIAN_POINT ( 'NONE',  ( 10.71299524138181347, 20.94030016091612367, 5.223175413353787988 ) ) ;
#18916=CARTESIAN_POINT ( 'NONE',  ( -0.1852845025067436646, 13.90840449083211183, 0.5712815246737864561 ) ) ;
#18925=CARTESIAN_POINT ( 'NONE',  ( 10.28455556095842205, 21.13454001091563228, 4.959045466106354993 ) ) ;
#18928=CARTESIAN_POINT ( 'NONE',  ( 11.22362340204833409, 13.65647046284849253, -2.836478600376960202 ) ) ;
#18931=CARTESIAN_POINT ( 'NONE',  ( 7.076841547715329028, 14.92411314052326965, 7.692205025965034082 ) ) ;
#18937=CARTESIAN_POINT ( 'NONE',  ( 8.673696226316383928, 11.54146397052094208, 3.508390839460689303 ) ) ;
#18938=CARTESIAN_POINT ( 'NONE',  ( 9.352043289815954452, 13.73224064219962592, -2.247542222848531779 ) ) ;
#18939=CARTESIAN_POINT ( 'NONE',  ( 2.415895693004135314, 18.09708922108623241, -0.2312783618673834030 ) ) ;
#18947=CARTESIAN_POINT ( 'NONE',  ( 11.20183242851396166, 15.98666862805646005, 6.807554364040996120 ) ) ;
#18948=CARTESIAN_POINT ( 'NONE',  ( 10.93328336395047451, 14.15736234249478720, -4.068969855961862336 ) ) ;
#18951=CARTESIAN_POINT ( 'NONE',  ( 9.574157909608086214, 12.48569481993280839, -1.056400077264328052 ) ) ;
#18955=CARTESIAN_POINT ( 'NONE',  ( 4.694926625316558244, 21.33523753305656001, 2.105523894130039597 ) ) ;
#18958=CARTESIAN_POINT ( 'NONE',  ( 6.719255672218935160, 11.03203715683660135, 4.231726879825330911 ) ) ;
#18979=CARTESIAN_POINT ( 'NONE',  ( 13.10461138620464361, 14.87610706663263826, 6.337233188073541967 ) ) ;
#18981=CARTESIAN_POINT ( 'NONE',  ( 5.385071355335792731, 12.35064203674882144, 7.174237779700658457 ) ) ;
#18984=CARTESIAN_POINT ( 'NONE',  ( 5.076974952998434709, 11.60801150508606128, 5.931021133774994958 ) ) ;
#18988=CARTESIAN_POINT ( 'NONE',  ( 7.887801445722042004, 18.97569031398505146, -1.398027553882073004 ) ) ;
#18989=CARTESIAN_POINT ( 'NONE',  ( 1.473177303762296608, 14.65264615020049099, 8.504923832329929212 ) ) ;
#18996=CARTESIAN_POINT ( 'NONE',  ( 1.401597142160411202, 21.11691655071049922, 3.736020553106880193 ) ) ;
#19000=CARTESIAN_POINT ( 'NONE',  ( 4.384837209473736230, 18.74075759514924400, -0.3090233597782079400 ) ) ;
#19006=CARTESIAN_POINT ( 'NONE',  ( 5.147480976434583688, 17.32712159277285124, -1.670171097842100050 ) ) ;
#19008=CARTESIAN_POINT ( 'NONE',  ( 12.47629024345491899, 10.55913518404749141, 2.732682640108681227 ) ) ;
#19013=CARTESIAN_POINT ( 'NONE',  ( 8.622933100223315606, 10.85996554133373060, 3.667822295698338397 ) ) ;
#19014=CARTESIAN_POINT ( 'NONE',  ( 0.1620597292614394114, 17.19705222221691088, 0.7801052633530786151 ) ) ;
#19016=CARTESIAN_POINT ( 'NONE',  ( 5.881467817102347340, 12.57312689154560736, 0.5107683554711034413 ) ) ;
#19019=CARTESIAN_POINT ( 'NONE',  ( 9.390327731862623040, 21.87018156742340125, 1.595481807788067030 ) ) ;
#19022=CARTESIAN_POINT ( 'NONE',  ( 0.2519962783006516327, 20.95646860120554322, 6.403714366392914137 ) ) ;
#19027=CARTESIAN_POINT ( 'NONE',  ( 4.081241395634245706, 18.69448487464559250, -0.1415844030543617349 ) ) ;
#19033=CARTESIAN_POINT ( 'NONE',  ( 11.35066781222083065, 13.35192466491865204, 6.773944610407871991 ) ) ;
#19037=CARTESIAN_POINT ( 'NONE',  ( 12.04285459910253664, 11.22180268030754213, 0.9169839392688694524 ) ) ;
#19045=CARTESIAN_POINT ( 'NONE',  ( 12.01669072522048154, 20.94460807410368020, 3.624609020444634844 ) ) ;
#19047=CARTESIAN_POINT ( 'NONE',  ( 9.143268736852048661, 21.15296384697220233, 1.757390325529230024 ) ) ;
#19048=CARTESIAN_POINT ( 'NONE',  ( -0.02560407305274986500, 21.02721105424156178, 4.690030914906221149 ) ) ;
#19057=CARTESIAN_POINT ( 'NONE',  ( 8.808541549489559586, 20.20056482616064031, 6.590010215270987182 ) ) ;
#19060=CARTESIAN_POINT ( 'NONE',  ( 9.762688185902014482, 11.89947507744004795, -0.1889497053391823445 ) ) ;
#19062=CARTESIAN_POINT ( 'NONE',  ( 12.58831425534056869, 22.00048094112651853, -0.3068354446663246748 ) ) ;
#19064=CARTESIAN_POINT ( 'NONE',  ( 2.443839657807668431, 20.56225727104456169, 2.139178112839631218 ) ) ;
#19067=CARTESIAN_POINT ( 'NONE',  ( 7.531689760312532123, 14.42957034058409604, 8.057596976765562857 ) ) ;
#19072=CARTESIAN_POINT ( 'NONE',  ( 0.03263962654255925938, 15.61251617902083844, 0.8683832099246990843 ) ) ;
#19076=CARTESIAN_POINT ( 'NONE',  ( 2.077130412032726081, 17.63363686242983519, 0.2456684943282234079 ) ) ;
#19093=CARTESIAN_POINT ( 'NONE',  ( 4.415446871197127976, 20.54185615358932182, 0.3855645798335944896 ) ) ;
#19097=CARTESIAN_POINT ( 'NONE',  ( 5.345771735889576881, 12.47140775907805832, 7.152587718021153229 ) ) ;
#19102=CARTESIAN_POINT ( 'NONE',  ( 1.362477653891336793, 13.51601408089542211, 7.762560417787443434 ) ) ;
#19111=CARTESIAN_POINT ( 'NONE',  ( 3.241640988598431861, 18.85000704986485687, 8.551504305367847891 ) ) ;
#19115=CARTESIAN_POINT ( 'NONE',  ( -0.2597389653420326683, 20.42992192302084220, 3.722174571042816460 ) ) ;
#19121=CARTESIAN_POINT ( 'NONE',  ( 10.93510241507968850, 15.70746112734460986, 7.398426013499326714 ) ) ;
#19123=CARTESIAN_POINT ( 'NONE',  ( 11.69641261104832353, 10.74240771329982103, -0.5047199525474890258 ) ) ;
#19130=CARTESIAN_POINT ( 'NONE',  ( 7.650701833136086982, 11.68635701119769976, -0.4599083425468352693 ) ) ;
#19131=CARTESIAN_POINT ( 'NONE',  ( 1.927950833816268084, 16.41909622821189885, -0.03018426488458642726 ) ) ;
#19134=CARTESIAN_POINT ( 'NONE',  ( 5.863121774503869510, 12.63765592565710705, 0.4230228709285713262 ) ) ;
#19139=CARTESIAN_POINT ( 'NONE',  ( 2.615483950589470474, 19.61703011493782967, 6.888558279248298888 ) ) ;
#19141=CARTESIAN_POINT ( 'NONE',  ( 10.13601329052621658, 10.83116634084218077, 0.1401833725585602819 ) ) ;
#19143=CARTESIAN_POINT ( 'NONE',  ( 6.707153380113150654, 10.91793053508332001, 4.254858596453126474 ) ) ;
#19146=CARTESIAN_POINT ( 'NONE',  ( 0.3918216066353466531, 18.57721708583670761, 1.314797039972573689 ) ) ;
#19154=CARTESIAN_POINT ( 'NONE',  ( 9.826606975627045770, 10.88625345693648150, 0.1783350857751269669 ) ) ;
#19157=CARTESIAN_POINT ( 'NONE',  ( 12.00933040723107403, 11.24147212942736118, 0.7726907669949114599 ) ) ;
#19158=CARTESIAN_POINT ( 'NONE',  ( 5.363080482404605220, 15.22688935535643573, -2.039950826354700819 ) ) ;
#19159=CARTESIAN_POINT ( 'NONE',  ( 2.282999857009965439, 20.09148914161242061, 6.315958300496411049 ) ) ;
#19164=CARTESIAN_POINT ( 'NONE',  ( 5.468534317627838703, 20.74776807699790027, 3.317767048404099750 ) ) ;
#19169=CARTESIAN_POINT ( 'NONE',  ( 9.817900122067920066, 21.04886798522784375, 3.383858994149747002 ) ) ;
#19170=CARTESIAN_POINT ( 'NONE',  ( 4.844186739043601975, 19.02074804359552118, 7.142938902112708988 ) ) ;
#19171=CARTESIAN_POINT ( 'NONE',  ( 9.040336234276225014, 18.23310434598736052, 6.937167086216335044 ) ) ;
#19176=CARTESIAN_POINT ( 'NONE',  ( 10.63308548515679774, 21.89042938493124169, 0.05754589513367810993 ) ) ;
#19179=CARTESIAN_POINT ( 'NONE',  ( 9.393035566209373854, 17.09556050276089678, -2.811126736337388632 ) ) ;
#19182=CARTESIAN_POINT ( 'NONE',  ( 4.545153868657309637, 11.72601213311298274, 5.605246626590751013 ) ) ;
#19185=CARTESIAN_POINT ( 'NONE',  ( 7.176498194401259134, 11.94873204706878056, 6.222147181184805476 ) ) ;
#19191=CARTESIAN_POINT ( 'NONE',  ( 0.06220981948177380788, 14.29877793608298830, 1.344091684615118965 ) ) ;
#19197=CARTESIAN_POINT ( 'NONE',  ( 13.35516194159795234, 12.73805723869360129, 6.121469047959861243 ) ) ;
#19206=CARTESIAN_POINT ( 'NONE',  ( 2.491886806202981752, 20.82653447492750232, 6.619722005571624379 ) ) ;
#19209=CARTESIAN_POINT ( 'NONE',  ( 5.592450108068661940, 15.67876173997583322, 8.758473581429681687 ) ) ;
#19215=CARTESIAN_POINT ( 'NONE',  ( 1.292113498908112890, 13.15017386328606186, 7.382771724034875582 ) ) ;
#19217=CARTESIAN_POINT ( 'NONE',  ( 3.269967501978980451, 13.23265724051127634, 7.157293919752532041 ) ) ;
#19223=CARTESIAN_POINT ( 'NONE',  ( 2.996463091073017893, 19.66541386574806793, 7.962514975033100129 ) ) ;
#19226=CARTESIAN_POINT ( 'NONE',  ( -0.4304425378944187197, 20.20483442592724188, 3.283658422123586718 ) ) ;
#19234=CARTESIAN_POINT ( 'NONE',  ( 5.914053747146598816, 20.37078616557504063, 0.1005632906319847558 ) ) ;
#19237=CARTESIAN_POINT ( 'NONE',  ( 13.30192323483472983, 13.36279638818773208, 6.395705296019483121 ) ) ;
#19242=CARTESIAN_POINT ( 'NONE',  ( 7.396207190460517999, 17.87138037546853653, -2.699953620006905197 ) ) ;
#19243=CARTESIAN_POINT ( 'NONE',  ( 5.397938743089579994, 14.21717427261922673, 7.611741220669421715 ) ) ;
#19246=CARTESIAN_POINT ( 'NONE',  ( 5.639233624224025299, 14.00976992351738559, -0.7654035218331123325 ) ) ;
#19250=CARTESIAN_POINT ( 'NONE',  ( 6.578503335167750876, 20.62467454825192092, -0.2978276507856368327 ) ) ;
#19253=CARTESIAN_POINT ( 'NONE',  ( 4.649213468993561804, 20.53916262649988056, 6.851662615090752695 ) ) ;
#19256=CARTESIAN_POINT ( 'NONE',  ( 1.842148214019495800, 14.88408257588732653, 0.2398186081272557224 ) ) ;
#19266=CARTESIAN_POINT ( 'NONE',  ( 9.490334072463598503, 11.65861747434272111, -1.267925462873313425 ) ) ;
#19269=CARTESIAN_POINT ( 'NONE',  ( 11.64810702638509099, 11.73795319285898131, -0.8004304160343337360 ) ) ;
#19270=CARTESIAN_POINT ( 'NONE',  ( 5.919258205413525431, 19.60814919271167867, -1.127688298506704045 ) ) ;
#19272=CARTESIAN_POINT ( 'NONE',  ( 3.049654375162700326, 12.59595915030716284, 6.508823439574863201 ) ) ;
#19276=CARTESIAN_POINT ( 'NONE',  ( 11.70823332671042749, 19.71606648096064163, -2.535146659683900072 ) ) ;
#19277=CARTESIAN_POINT ( 'NONE',  ( 9.269908071869892296, 16.57988186816537279, 7.309237487032761216 ) ) ;
#19280=CARTESIAN_POINT ( 'NONE',  ( 5.130991270212533095, 19.13552603310812117, 7.996869729160946960 ) ) ;
#19286=CARTESIAN_POINT ( 'NONE',  ( 7.760365661431780637, 20.10612899863186342, -1.645341292727603655 ) ) ;
#19289=CARTESIAN_POINT ( 'NONE',  ( 9.306704478242739498, 15.95877063496000581, -2.845665734436647831 ) ) ;
#19291=CARTESIAN_POINT ( 'NONE',  ( 0.4932393519182353692, 19.79695343917473949, 6.883184639792627735 ) ) ;
#19292=CARTESIAN_POINT ( 'NONE',  ( 2.498689706804295252, 19.49937761787746382, 7.845835893948169826 ) ) ;
#19299=CARTESIAN_POINT ( 'NONE',  ( 0.02858491886840053980, 15.02004020798568185, 1.018833874744118129 ) ) ;
#19314=CARTESIAN_POINT ( 'NONE',  ( 3.618629837795121595, 17.35319764795464792, -1.453827791231713018 ) ) ;
#19317=CARTESIAN_POINT ( 'NONE',  ( 4.968297847841906645, 11.40330044108586094, 5.455941518735753171 ) ) ;
#19325=CARTESIAN_POINT ( 'NONE',  ( 2.586256820664998735, 11.26173031269666147, 3.955566897847509811 ) ) ;
#19329=CARTESIAN_POINT ( 'NONE',  ( 7.565709627428113038, 13.41850193825106174, 6.761998452700021645 ) ) ;
#19331=CARTESIAN_POINT ( 'NONE',  ( 13.30933468305810585, 22.15284641732971593, 1.973535763860893688 ) ) ;
#19335=CARTESIAN_POINT ( 'NONE',  ( 12.74873341173676167, 12.98021359793846230, 5.958482511230140943 ) ) ;
#19338=CARTESIAN_POINT ( 'NONE',  ( 12.55110607399917022, 10.63801454700946181, 3.044453194121171880 ) ) ;
#19342=CARTESIAN_POINT ( 'NONE',  ( 7.370218150239237431, 12.95355782316449655, -1.762137703980258596 ) ) ;
#19345=CARTESIAN_POINT ( 'NONE',  ( 6.469343941046106217, 20.06331668064719764, 0.3840982914384075131 ) ) ;
#19347=CARTESIAN_POINT ( 'NONE',  ( 2.222337027708588320, 20.17600262083952956, 5.895190365622971385 ) ) ;
#19350=CARTESIAN_POINT ( 'NONE',  ( 9.788131959061814769, 19.28339334790884152, -2.994169572174589788 ) ) ;
#19354=CARTESIAN_POINT ( 'NONE',  ( 1.769989151042760334, 13.02087111295804256, 0.3933944368290009375 ) ) ;
#19360=CARTESIAN_POINT ( 'NONE',  ( 3.801506843055717511, 17.18874207142271970, -0.6811624414094943347 ) ) ;
#19367=CARTESIAN_POINT ( 'NONE',  ( 9.841056877679053017, 10.86540522446826174, 0.2393104589039902752 ) ) ;
#19370=CARTESIAN_POINT ( 'NONE',  ( 5.681085220776317612, 12.17129757418337199, -0.2378145488336220192 ) ) ;
#19375=CARTESIAN_POINT ( 'NONE',  ( 5.391733748237763635, 20.73460212580145878, 3.114551668807497897 ) ) ;
#19381=CARTESIAN_POINT ( 'NONE',  ( 10.85750912504734522, 19.10987469415690043, 6.066339372520253015 ) ) ;
#19382=CARTESIAN_POINT ( 'NONE',  ( 9.931220000398274905, 11.51518149844540240, 0.4432291548185011698 ) ) ;
#19391=CARTESIAN_POINT ( 'NONE',  ( 10.51466052783852234, 20.82419441543289906, -0.1522035372867676650 ) ) ;
#19392=CARTESIAN_POINT ( 'NONE',  ( 1.318808768746996929, 17.31501546851630025, 8.734854497731600276 ) ) ;
#19393=CARTESIAN_POINT ( 'NONE',  ( 3.029311592522686780, 13.36420590592894264, 8.039591749172359414 ) ) ;
#19418=CARTESIAN_POINT ( 'NONE',  ( 1.614128406362234980, 17.33698837102782520, 9.606669273329499603 ) ) ;
#19421=CARTESIAN_POINT ( 'NONE',  ( 3.662491624849550931, 13.06014951857161321, -0.2875058916943667442 ) ) ;
#19424=CARTESIAN_POINT ( 'NONE',  ( 1.458148681563614879, 14.39063534605306671, 8.374873237808131421 ) ) ;
#19434=CARTESIAN_POINT ( 'NONE',  ( 2.135935944106437390, 11.82688626209604621, 1.990821043935844026 ) ) ;
#19443=CARTESIAN_POINT ( 'NONE',  ( 7.052001307456389867, 12.88806360044558197, -1.228466916830508682 ) ) ;
#19446=CARTESIAN_POINT ( 'NONE',  ( 13.21799010538730812, 12.70407506772013129, 5.966476990678911463 ) ) ;
#19451=CARTESIAN_POINT ( 'NONE',  ( 7.563764764072376856, 11.98948496040201306, -0.8495171220973293247 ) ) ;
#19452=CARTESIAN_POINT ( 'NONE',  ( 3.482904747837870740, 20.64447347884702211, 3.584108899128696901 ) ) ;
#19453=CARTESIAN_POINT ( 'NONE',  ( 7.828815060326342667, 20.77749002548769042, 3.972184785381453587 ) ) ;
#19457=CARTESIAN_POINT ( 'NONE',  ( 2.488984304238356593, 19.83350231766241478, 6.572627150490618853 ) ) ;
#19461=CARTESIAN_POINT ( 'NONE',  ( 14.31159658034589555, 21.56570388316688280, 3.562700818068579522 ) ) ;
#19465=CARTESIAN_POINT ( 'NONE',  ( 4.991296504249822519, 11.34913591283086021, 5.626762266647114430 ) ) ;
#19466=CARTESIAN_POINT ( 'NONE',  ( 1.606218844064036144, 13.47661576675192663, 8.724755388575742288 ) ) ;
#19468=CARTESIAN_POINT ( 'NONE',  ( 1.290330672387997035, 20.33382539468342287, 3.526104413675141380 ) ) ;
#19476=CARTESIAN_POINT ( 'NONE',  ( 10.08697080318449579, 10.61613734897275130, 1.270570921979556456 ) ) ;
#19480=CARTESIAN_POINT ( 'NONE',  ( 12.46191723504852433, 21.05992202225752052, -0.6087379413794911098 ) ) ;
#19481=CARTESIAN_POINT ( 'NONE',  ( 5.508984985521168554, 17.56310428172361782, -2.032606368940984343 ) ) ;
#19484=CARTESIAN_POINT ( 'NONE',  ( 0.1070098978122437372, 13.13938098413696132, 2.205990570212618351 ) ) ;
#19494=CARTESIAN_POINT ( 'NONE',  ( 9.943729142003926214, 18.95229069147438139, -2.474586121992937926 ) ) ;
#19495=CARTESIAN_POINT ( 'NONE',  ( 5.351158161824543846, 16.10253209244224593, 8.037206358779434012 ) ) ;
#19501=CARTESIAN_POINT ( 'NONE',  ( 3.930212692675568498, 21.29697021551619329, 4.866220384958813483 ) ) ;
#19509=CARTESIAN_POINT ( 'NONE',  ( 10.29536085631526454, 20.49447628526758436, -0.7298637714113751507 ) ) ;
#19511=CARTESIAN_POINT ( 'NONE',  ( 1.417191649792139296, 16.55315478993970402, 8.850408389496440265 ) ) ;
#19513=CARTESIAN_POINT ( 'NONE',  ( 2.002672932925127824, 20.46094657096126213, 6.584029723752546026 ) ) ;
#19526=CARTESIAN_POINT ( 'NONE',  ( 5.655606339218213208, 17.24330370537085955, -1.409341170596322801 ) ) ;
#19541=CARTESIAN_POINT ( 'NONE',  ( 6.291852177003497637, 10.85576871210978211, 2.343863137984593781 ) ) ;
#19544=CARTESIAN_POINT ( 'NONE',  ( 3.973159551739567696, 19.20098565268092727, -0.6330842699365994974 ) ) ;
#19554=CARTESIAN_POINT ( 'NONE',  ( 3.518930018599623288, 13.18938088783941787, 8.144277403441783747 ) ) ;
#19563=CARTESIAN_POINT ( 'NONE',  ( 10.93405359717582215, 14.00597049205862277, 6.551351406591241933 ) ) ;
#19567=CARTESIAN_POINT ( 'NONE',  ( 11.71072533466843346, 20.55886875348996412, -2.691199719323197126 ) ) ;
#19571=CARTESIAN_POINT ( 'NONE',  ( 7.433331065033467411, 18.10929869608010634, -2.625636931304927479 ) ) ;
#19573=CARTESIAN_POINT ( 'NONE',  ( 8.983827027755273420, 18.20566418143656406, 6.849687620904892249 ) ) ;
#19575=CARTESIAN_POINT ( 'NONE',  ( 6.680730399758177285, 11.81714183159373199, 4.112448148044469676 ) ) ;
#19577=CARTESIAN_POINT ( 'NONE',  ( 7.292079158261280725, 14.37945976953094629, -2.683365525959949593 ) ) ;
#19578=CARTESIAN_POINT ( 'NONE',  ( 13.70405149357018004, 21.54752288430403695, 1.766493360091446085 ) ) ;
#19580=CARTESIAN_POINT ( 'NONE',  ( 3.374943536863300508, 18.28257875309041935, 8.941416396130453137 ) ) ;
#19581=CARTESIAN_POINT ( 'NONE',  ( 1.456944856587381709, 12.62211961469936128, 7.963006803835855685 ) ) ;
#19583=CARTESIAN_POINT ( 'NONE',  ( 2.925846556779251095, 19.21529397045534182, 7.410183071057827142 ) ) ;
#19590=CARTESIAN_POINT ( 'NONE',  ( 9.906809305938214294, 20.59416953720186783, -1.845156594728350141 ) ) ;
#19593=CARTESIAN_POINT ( 'NONE',  ( 11.75807948570318295, 19.66724708567648605, -2.440222580272270569 ) ) ;
#19594=CARTESIAN_POINT ( 'NONE',  ( 5.761094208437596897, 19.00053386114307230, -1.506891469455103438 ) ) ;
#19596=CARTESIAN_POINT ( 'NONE',  ( 3.739208544156527925, 17.18772947144893948, -0.6574115393716641886 ) ) ;
#19601=CARTESIAN_POINT ( 'NONE',  ( 9.243363897212034885, 12.11223639541018215, 5.050083142846552242 ) ) ;
#19605=PLANE ( 'NONE',  #11031 ) ;
#19613=CARTESIAN_POINT ( 'NONE',  ( 10.19629082482998150, 20.30350291925140382, -0.9866510706609600279 ) ) ;
#19614=CARTESIAN_POINT ( 'NONE',  ( 1.082545292382026458, 18.42541199074858227, 8.282403339363888506 ) ) ;
#19623=CARTESIAN_POINT ( 'NONE',  ( 8.905523458406561232, 12.18567386761292148, 5.103169512634847749 ) ) ;
#19626=CARTESIAN_POINT ( 'NONE',  ( 9.017034975940656949, 15.28237876918361948, -3.631115729470330677 ) ) ;
#19631=CARTESIAN_POINT ( 'NONE',  ( 6.802866078812881412, 11.05277248166000170, 4.463065346860751070 ) ) ;
#19636=CARTESIAN_POINT ( 'NONE',  ( 1.884718254017690997, 21.29000687509540413, 4.986748289960942770 ) ) ;
#19639=CARTESIAN_POINT ( 'NONE',  ( 4.026112509266686068, 19.40402007317530675, -0.5074809695937115839 ) ) ;
#19642=CARTESIAN_POINT ( 'NONE',  ( 0.7492674540166441854, 12.21418807727941136, 4.792696233684067053 ) ) ;
#19645=CARTESIAN_POINT ( 'NONE',  ( 2.510246471197546292, 12.10255669127714739, 3.589570832737527528 ) ) ;
#19651=CARTESIAN_POINT ( 'NONE',  ( 3.569277441639647996, 13.57212688075029661, 8.416253947611240349 ) ) ;
#19660=CARTESIAN_POINT ( 'NONE',  ( 10.01420173804988956, 20.41586353969747947, 5.057845461604397741 ) ) ;
#19664=CARTESIAN_POINT ( 'NONE',  ( 12.21532007410937304, 21.58072960932728179, -1.335272812607331883 ) ) ;
#19668=CARTESIAN_POINT ( 'NONE',  ( 8.393974790171371936, 20.04483644391566699, 5.447030543808771164 ) ) ;
#19669=CARTESIAN_POINT ( 'NONE',  ( 6.909362352619732306, 12.19147799795061182, 5.147458291921238605 ) ) ;
#19673=CARTESIAN_POINT ( 'NONE',  ( 13.62955006427684879, 22.07962435715549177, 1.866896178110612814 ) ) ;
#19676=CARTESIAN_POINT ( 'NONE',  ( 1.860710414810725410, 18.25211889560055667, -0.4549317619264000023 ) ) ;
#19677=CARTESIAN_POINT ( 'NONE',  ( 0.4412527074930906457, 11.62816711700305206, 3.451613267458483403 ) ) ;
#19679=CARTESIAN_POINT ( 'NONE',  ( 5.960941858113148584, 12.27647896852458231, 0.9739740074785588897 ) ) ;
#19685=CARTESIAN_POINT ( 'NONE',  ( 9.431633338501304920, 14.64457645186116252, 7.880854554680595925 ) ) ;
#19686=CARTESIAN_POINT ( 'NONE',  ( 9.242220441921224605, 17.85059929941992962, -3.437012189181674060 ) ) ;
#19689=CARTESIAN_POINT ( 'NONE',  ( 11.54223276252992747, 18.90513505042380160, -2.958155071492406751 ) ) ;
#19691=CARTESIAN_POINT ( 'NONE',  ( 8.131041595892833485, 21.31202829439499169, 4.830511473850858550 ) ) ;
#19693=CARTESIAN_POINT ( 'NONE',  ( 4.147546957899959530, 12.03379079558084186, 2.284289319685276265 ) ) ;
#19697=CARTESIAN_POINT ( 'NONE',  ( 9.610489285031960094, 13.68826078499848187, -2.403762545223697700 ) ) ;
#19698=CARTESIAN_POINT ( 'NONE',  ( 5.080147692099665768, 18.14094701354450478, 7.664661620491963312 ) ) ;
#19699=CARTESIAN_POINT ( 'NONE',  ( 1.567997441699468419, 12.54098868903164110, 8.004899158126836056 ) ) ;
#19703=CARTESIAN_POINT ( 'NONE',  ( 6.765426361287598667, 11.37554263597316151, 2.712286843111946233 ) ) ;
#19712=CARTESIAN_POINT ( 'NONE',  ( 9.419377328995013343, 17.32343871894041953, -2.774712070466804015 ) ) ;
#19725=CARTESIAN_POINT ( 'NONE',  ( 11.31839047608332827, 18.10733791853621710, -3.410071512985684450 ) ) ;
#19726=CARTESIAN_POINT ( 'NONE',  ( 2.470079502529485715, 19.19535844608499175, 1.088228707528946515 ) ) ;
#19729=CARTESIAN_POINT ( 'NONE',  ( 8.195282804414690148, 21.33050868956278023, 5.066350132480763158 ) ) ;
#19738=CARTESIAN_POINT ( 'NONE',  ( 6.194920465254885933, 21.18628736811522373, 5.570234412840648908 ) ) ;
#19741=CARTESIAN_POINT ( 'NONE',  ( 3.516703214434496516, 14.76933982512905885, -1.184109074939236672 ) ) ;
#19748=CARTESIAN_POINT ( 'NONE',  ( 2.472191904324769762, 12.13218657682475055, 3.415641386168698723 ) ) ;
#19749=CARTESIAN_POINT ( 'NONE',  ( 4.458800082910141072, 11.90016196835719242, 3.247083169787960522 ) ) ;
#19756=CARTESIAN_POINT ( 'NONE',  ( 3.638193303819591495, 14.51711042508261151, 8.878930407153470483 ) ) ;
#19765=CARTESIAN_POINT ( 'NONE',  ( 11.56806292758007793, 10.73085021393864125, 0.8322797596209885462 ) ) ;
#19767=CARTESIAN_POINT ( 'NONE',  ( 11.00610965153222054, 13.43923525470570723, -3.604247308733671495 ) ) ;
#19774=CARTESIAN_POINT ( 'NONE',  ( 9.093129788387537715, 17.59128346607696614, 7.060036749039768189 ) ) ;
#19776=CARTESIAN_POINT ( 'NONE',  ( 3.380877013741256487, 16.38364594039518707, 8.445040901272195200 ) ) ;
#19780=CARTESIAN_POINT ( 'NONE',  ( 13.58266658209738331, 21.44526949881736755, 1.787837019446894216 ) ) ;
#19782=CARTESIAN_POINT ( 'NONE',  ( 4.640211518560553472, 20.53859366438406298, 6.853938782356775228 ) ) ;
#19783=CARTESIAN_POINT ( 'NONE',  ( 1.668587280488517788, 14.12956687025133284, 9.105894972235919482 ) ) ;
#19786=CARTESIAN_POINT ( 'NONE',  ( 7.229981607529511578, 13.47123956803594069, 6.789802541014523740 ) ) ;
#19792=CARTESIAN_POINT ( 'NONE',  ( 12.54330750292673535, 20.52725722417916288, 5.646485819856933652 ) ) ;
#19793=CARTESIAN_POINT ( 'NONE',  ( 9.321147220187416593, 12.33153251133805028, -2.031490842037978251 ) ) ;
#19800=CARTESIAN_POINT ( 'NONE',  ( 8.733521366538639086, 20.20800283656023311, 6.430388172760417298 ) ) ;
#19802=CARTESIAN_POINT ( 'NONE',  ( 4.962249093223817020, 20.63862493749866189, 2.243063623533420259 ) ) ;
#19805=CARTESIAN_POINT ( 'NONE',  ( 6.787877011713288056, 19.10393197244254893, 6.711799629438941039 ) ) ;
#19808=CARTESIAN_POINT ( 'NONE',  ( 8.424495705925030720, 20.67359808219790196, 4.682861630976923095 ) ) ;
#19809=CARTESIAN_POINT ( 'NONE',  ( 5.229436589262380863, 17.29530047414887051, 7.935297285553942537 ) ) ;
#19812=CARTESIAN_POINT ( 'NONE',  ( -0.8104627873563117202, 20.56718397690614353, 3.218825348147362764 ) ) ;
#19817=CARTESIAN_POINT ( 'NONE',  ( 6.768303840451392439, 11.31933340188284198, 2.707322785470000159 ) ) ;
#19827=CARTESIAN_POINT ( 'NONE',  ( 9.905291570324402883, 19.59492360076687589, -1.723128527427267187 ) ) ;
#19842=CARTESIAN_POINT ( 'NONE',  ( 5.783434255099849430, 12.69913397707368219, 0.2011194333812519330 ) ) ;
#19844=CARTESIAN_POINT ( 'NONE',  ( 9.812235820622445814, 10.74839508995118109, 0.2078937617495408285 ) ) ;
#19857=CARTESIAN_POINT ( 'NONE',  ( -0.1826891866692206545, 17.37763432658893947, 0.05499588537583813969 ) ) ;
#19860=CARTESIAN_POINT ( 'NONE',  ( 5.347305277071898288, 21.51930324994589938, 2.982367603555873714 ) ) ;
#19866=CARTESIAN_POINT ( 'NONE',  ( 2.569241531917466848, 12.06096004062977123, 3.858983728647578104 ) ) ;
#19867=CARTESIAN_POINT ( 'NONE',  ( 3.967314636381039428, 12.87327716067178152, 0.9669488592612511813 ) ) ;
#19871=CARTESIAN_POINT ( 'NONE',  ( 1.676631372968138578, 14.47082764806958544, -0.3334079287914699097 ) ) ;
#19881=CARTESIAN_POINT ( 'NONE',  ( 7.828648054350496821, 20.67359808219790196, 4.861297291341504234 ) ) ;
#19889=CARTESIAN_POINT ( 'NONE',  ( 9.260438503031343416, 14.54440023414849570, 6.890419401724486193 ) ) ;
#19890=CARTESIAN_POINT ( 'NONE',  ( 3.359084728520796759, 16.63200163831436384, 8.437760029842829468 ) ) ;
#19894=CARTESIAN_POINT ( 'NONE',  ( 4.046220154711220651, 21.31561936814513913, 5.264967463508157586 ) ) ;
#19895=CARTESIAN_POINT ( 'NONE',  ( 1.435637233034790183, 12.53020615724244102, 7.860097166555220838 ) ) ;
#19898=CARTESIAN_POINT ( 'NONE',  ( 6.990983794162659137, 12.34350287060300211, 5.597185000230755492 ) ) ;
#19906=CARTESIAN_POINT ( 'NONE',  ( 9.041911633562941475, 13.32230603934784163, -2.889390931865063461 ) ) ;
#19910=CARTESIAN_POINT ( 'NONE',  ( 9.131607688676272261, 16.83393002257671611, -3.607777635551496775 ) ) ;
#19913=CARTESIAN_POINT ( 'NONE',  ( 8.061252166635112459, 21.38919659779727311, 4.640970875387647965 ) ) ;
#19915=CARTESIAN_POINT ( 'NONE',  ( 7.259159645424166918, 14.95027458788505648, 7.545890876313082529 ) ) ;
#19919=CARTESIAN_POINT ( 'NONE',  ( 12.72960005895841107, 11.13394627749852361, 2.488341707347630827 ) ) ;
#19923=CARTESIAN_POINT ( 'NONE',  ( 5.290774276891190731, 21.33523753305656001, 1.927088233765430036 ) ) ;
#19936=CARTESIAN_POINT ( 'NONE',  ( 13.10625849968711343, 16.65997537097360492, 6.401687974235077405 ) ) ;
#19940=CARTESIAN_POINT ( 'NONE',  ( 0.7821300450196075893, 12.31440956997844083, 6.399142672586000558 ) ) ;
#19944=CARTESIAN_POINT ( 'NONE',  ( 3.821430202768995699, 16.87782039879526508, -0.6383179096349496096 ) ) ;
#19947=CARTESIAN_POINT ( 'NONE',  ( 1.437842523326486210, 20.32886153177781807, 3.861219391056186723 ) ) ;
#19950=CARTESIAN_POINT ( 'NONE',  ( 6.378434091850946785, 20.04762713518370276, 0.2153161039344592409 ) ) ;
#19954=CARTESIAN_POINT ( 'NONE',  ( 9.128749953449215582, 17.37245550884423295, -3.652603057860464020 ) ) ;
#19958=CARTESIAN_POINT ( 'NONE',  ( 10.16438117221001214, 20.46144192302394416, 4.562511949730317262 ) ) ;
#19959=CARTESIAN_POINT ( 'NONE',  ( 7.411075239409255389, 12.62844402333576177, -1.659685333687124453 ) ) ;
#19964=CARTESIAN_POINT ( 'NONE',  ( -0.9912634196990741664, 20.56718397690614353, 3.272968853020066238 ) ) ;
#19967=CARTESIAN_POINT ( 'NONE',  ( 7.343579971993509758, 17.90724651579188276, 8.163068317436712462 ) ) ;
#19972=CARTESIAN_POINT ( 'NONE',  ( 2.701204329178783503, 12.04454888244252686, 4.459376208058960067 ) ) ;
#19974=CARTESIAN_POINT ( 'NONE',  ( 11.61875096509713678, 22.07868470824458385, 1.935183652392323594 ) ) ;
#19976=CARTESIAN_POINT ( 'NONE',  ( 13.38171535118323341, 21.77020232253088139, 1.895702690670363122 ) ) ;
#19978=CARTESIAN_POINT ( 'NONE',  ( 2.279600870619827191, 19.66662180573434426, 0.4729108911692707640 ) ) ;
#19986=CARTESIAN_POINT ( 'NONE',  ( 5.292458196680172477, 13.94198686298930134, -0.8460163710559848171 ) ) ;
#19992=CARTESIAN_POINT ( 'NONE',  ( 9.266403162818965811, 15.63651455217073760, 7.174713989175733886 ) ) ;
#19996=CARTESIAN_POINT ( 'NONE',  ( 7.546616319253421246, 14.71802924512825683, 8.274008119131478267 ) ) ;
#19997=CARTESIAN_POINT ( 'NONE',  ( 0.03891284271277922063, 12.71158167823063145, 1.613795646451485988 ) ) ;
#20001=CARTESIAN_POINT ( 'NONE',  ( 2.596685839560524123, 12.01605003366594104, 3.549272492307833371 ) ) ;
#20007=CARTESIAN_POINT ( 'NONE',  ( 11.40677969663037317, 10.98269117049956201, -1.304989702490406023 ) ) ;
#20008=CARTESIAN_POINT ( 'NONE',  ( 9.401229242103068984, 18.82062145692554722, -3.104638505349831767 ) ) ;
#20010=CARTESIAN_POINT ( 'NONE',  ( 7.615293357427485255, 21.68393751741501063, 3.420954748769350573 ) ) ;
#20012=CARTESIAN_POINT ( 'NONE',  ( 4.833000283041892331, 12.10687735873178283, 5.362284929865946737 ) ) ;
#20019=CARTESIAN_POINT ( 'NONE',  ( 9.540736633860454674, 18.39925938975357056, 7.172201154206985230 ) ) ;
#20021=CARTESIAN_POINT ( 'NONE',  ( 5.853085853755254142, 13.88483174882859217, 8.144698374851461864 ) ) ;
#20024=CARTESIAN_POINT ( 'NONE',  ( 6.760877964153869435, 11.41279743154806248, 2.716365728159965354 ) ) ;
#20032=CARTESIAN_POINT ( 'NONE',  ( 13.16751444918752689, 14.99951941989845317, 6.240119134003139223 ) ) ;
#20041=CARTESIAN_POINT ( 'NONE',  ( 6.019093303612395474, 11.41279792062686127, 2.938509629527338074 ) ) ;
#20046=CARTESIAN_POINT ( 'NONE',  ( 13.89594832754920084, 20.92845091260043944, 3.355964666133559593 ) ) ;
#20048=CARTESIAN_POINT ( 'NONE',  ( 3.709026512405631415, 20.56944361589559023, 4.257456878692176261 ) ) ;
#20050=CARTESIAN_POINT ( 'NONE',  ( 6.892679051309891669, 11.28692669747560018, 5.056475153849492976 ) ) ;
#20051=CARTESIAN_POINT ( 'NONE',  ( -0.1652886651045968047, 14.27591886420808187, 0.4930659400215714472 ) ) ;
#20054=CARTESIAN_POINT ( 'NONE',  ( 8.514924039564494507, 20.49847539968255461, 0.1707108281186896503 ) ) ;
#20055=CARTESIAN_POINT ( 'NONE',  ( 6.509677182189260058, 10.79806832651256165, 3.221000148203756464 ) ) ;
#20061=CARTESIAN_POINT ( 'NONE',  ( 4.068900827735927095, 11.26224364954182100, 2.021667420744689636 ) ) ;
#20064=CARTESIAN_POINT ( 'NONE',  ( 6.418448462341823202, 20.87337156576220210, 5.890648785273186583 ) ) ;
#20070=CARTESIAN_POINT ( 'NONE',  ( 0.2977117155517410851, 12.86857687641943748, 2.662936448039754378 ) ) ;
#20074=CARTESIAN_POINT ( 'NONE',  ( 8.304011643298727208, 21.33440546750962241, 5.035657290636697425 ) ) ;
#20078=CARTESIAN_POINT ( 'NONE',  ( 1.661827395509540395, 14.91648660468646170, -0.4852861473593332309 ) ) ;
#20088=CARTESIAN_POINT ( 'NONE',  ( 9.577851990202844945, 18.90452467200534414, -2.283339625814639895 ) ) ;
#20091=ADVANCED_BREP_SHAPE_REPRESENTATION ( '', ( #13947, #2234 ), #652 ) ;
#20096=CARTESIAN_POINT ( 'NONE',  ( 9.178319404383161739, 13.53135455853282210, 6.346539953116446142 ) ) ;
#20100=CARTESIAN_POINT ( 'NONE',  ( 0.6295142619741483925, 20.10391746901840548, 1.699101084138331830 ) ) ;
#20103=CARTESIAN_POINT ( 'NONE',  ( 5.715457615665387792, 20.82992769506763864, 3.705818051953985393 ) ) ;
#20109=CARTESIAN_POINT ( 'NONE',  ( 12.61930858051215232, 11.34183091107056107, 4.682723716983176132 ) ) ;
#20110=CARTESIAN_POINT ( 'NONE',  ( 11.33230897168458462, 22.03951179526607973, 2.056163920724246807 ) ) ;
#20114=CARTESIAN_POINT ( 'NONE',  ( 6.285968434040493769, 20.60167272699510121, -0.1906146123162393569 ) ) ;
#20120=CARTESIAN_POINT ( 'NONE',  ( 9.989334639727749376, 19.11784201969034314, -2.771333082350681210 ) ) ;
#20124=CARTESIAN_POINT ( 'NONE',  ( 7.614894075436263954, 16.64415285869171868, 8.470436859809918673 ) ) ;
#20137=CARTESIAN_POINT ( 'NONE',  ( 12.63173874750594550, 11.64128040312364298, 3.463609067284325160 ) ) ;
#20142=CARTESIAN_POINT ( 'NONE',  ( 4.285612585934864605, 11.69375961036644362, 3.894991824665326785 ) ) ;
#20148=CARTESIAN_POINT ( 'NONE',  ( 6.344067149498460623, 10.92343492048921227, 2.805454655492575444 ) ) ;
#20152=CARTESIAN_POINT ( 'NONE',  ( 12.78587835270623607, 11.94669871286416196, 4.219702435597263879 ) ) ;
#20153=CARTESIAN_POINT ( 'NONE',  ( 9.260822009384501285, 16.57983669178404895, 7.311232780123860131 ) ) ;
#20155=CARTESIAN_POINT ( 'NONE',  ( 11.44511088290697742, 15.66517251583919901, 7.665544166514130175 ) ) ;
#20160=CARTESIAN_POINT ( 'NONE',  ( 9.698164836889990426, 20.96660354162156992, 3.328179347255785903 ) ) ;
#20161=CARTESIAN_POINT ( 'NONE',  ( 5.482011443615976809, 17.41093948017483939, -2.183347155986513410 ) ) ;
#20169=CARTESIAN_POINT ( 'NONE',  ( 11.64429300236424680, 20.36482133694056529, -2.863385722148856338 ) ) ;
#20171=CARTESIAN_POINT ( 'NONE',  ( -0.4433120853942719153, 13.94977879502390294, 0.7288990453601157382 ) ) ;
#20174=CARTESIAN_POINT ( 'NONE',  ( 6.745190824350061121, 20.22278037098389802, 6.747779596029768179 ) ) ;
#20184=CARTESIAN_POINT ( 'NONE',  ( 3.760608265104776748, 14.37317007178249639, -0.2024957564424711698 ) ) ;
#20189=CARTESIAN_POINT ( 'NONE',  ( 2.723825491796734610, 20.67052922820899852, 1.612990099367228147 ) ) ;
#20202=CARTESIAN_POINT ( 'NONE',  ( 10.59520296648355497, 21.11368617580202312, 0.3248148419726618052 ) ) ;
#20209=CARTESIAN_POINT ( 'NONE',  ( 9.177196879199145840, 16.94989067509651548, 7.186116761185386892 ) ) ;
#20214=CARTESIAN_POINT ( 'NONE',  ( -0.1870826769984814675, 15.70867390004682207, 0.08389080611283412925 ) ) ;
#20218=CARTESIAN_POINT ( 'NONE',  ( 2.682654501809497827, 20.17421804741920255, 6.237504504152217244 ) ) ;
#20223=CARTESIAN_POINT ( 'NONE',  ( 11.21177383612729628, 11.06331416201678053, -1.201043617887846082 ) ) ;
#20226=CARTESIAN_POINT ( 'NONE',  ( 12.75798311189342904, 19.99333349299241291, 5.919898230773216419 ) ) ;
#20228=CARTESIAN_POINT ( 'NONE',  ( 9.346550868333654449, 12.95375062105654607, 6.879218072990156863 ) ) ;
#20229=CARTESIAN_POINT ( 'NONE',  ( 6.702786100604261499, 19.52118532600693968, 6.477837816616200506 ) ) ;
#20234=CARTESIAN_POINT ( 'NONE',  ( 12.39456830054109737, 21.31987603492770234, 3.682287093270521616 ) ) ;
#20235=CARTESIAN_POINT ( 'NONE',  ( 3.522851090697392440, 21.45407066062478307, 3.485718429601260659 ) ) ;
#20239=CARTESIAN_POINT ( 'NONE',  ( 2.890013838880071351, 20.19995037221810108, 2.193135344012238530 ) ) ;
#20246=CARTESIAN_POINT ( 'NONE',  ( 9.049997712883802947, 21.82002798184797143, 1.568539052827725655 ) ) ;
#20248=CARTESIAN_POINT ( 'NONE',  ( 13.02292903621057185, 13.07787182719316554, 5.285385277681105443 ) ) ;
#20250=CARTESIAN_POINT ( 'NONE',  ( 1.578471181848339011, 16.42212273390128985, -0.01596455333784975450 ) ) ;
#20256=CARTESIAN_POINT ( 'NONE',  ( 4.189560172702622154, 18.86334382086423389, 0.05853659215941360572 ) ) ;
#20257=CARTESIAN_POINT ( 'NONE',  ( 6.101406733746572719, 11.05292897737530211, 2.887581558249757485 ) ) ;
#20260=CARTESIAN_POINT ( 'NONE',  ( 11.28205105809946751, 12.85014763714888097, -2.380148793486948744 ) ) ;
#20261=CARTESIAN_POINT ( 'NONE',  ( 9.281794360172153091, 15.41858152414332750, -2.876659026916958961 ) ) ;
#20262=CARTESIAN_POINT ( 'NONE',  ( 1.441581025922393566, 11.71888320561318153, 6.433096701223809610 ) ) ;
#20263=CARTESIAN_POINT ( 'NONE',  ( 6.852794591177100436, 21.59098349863498001, 1.404805785893212366 ) ) ;
#20264=EDGE_CURVE ( 'NONE', #8219, #10254, #3224, .T. ) ;
#20268=CARTESIAN_POINT ( 'NONE',  ( 10.50551657660874838, 19.76665074817798740, 5.435994939576656471 ) ) ;
#20269=CARTESIAN_POINT ( 'NONE',  ( 11.57780626085113518, 20.24847620595872044, -3.132666676146435236 ) ) ;
#20274=CARTESIAN_POINT ( 'NONE',  ( 11.03093538129645879, 13.20899553483338629, -3.471696574638000410 ) ) ;
#20275=CARTESIAN_POINT ( 'NONE',  ( 3.308062403515462879, 16.51832937791753864, 9.310454716487452487 ) ) ;
#20278=CARTESIAN_POINT ( 'NONE',  ( 4.847387020393643553, 21.16549811554654070, 1.624554052234806756 ) ) ;
#20290=CARTESIAN_POINT ( 'NONE',  ( 1.772782524859966680, 13.34852099903613087, 0.2659304825361097357 ) ) ;
#20301=CARTESIAN_POINT ( 'NONE',  ( 11.83589009288015070, 20.94460807410368020, 3.678752525316609123 ) ) ;
#20302=CARTESIAN_POINT ( 'NONE',  ( -0.06419268334440733637, 17.37652828937785543, 0.02458381411575647629 ) ) ;
#20310=CARTESIAN_POINT ( 'NONE',  ( 9.235082566757867539, 16.29398304642754169, 7.224769592719947120 ) ) ;
#20315=CARTESIAN_POINT ( 'NONE',  ( 0.2982434584755015994, 11.88023445195970140, 2.816173442903336266 ) ) ;
#20318=CARTESIAN_POINT ( 'NONE',  ( -0.5157468025401186207, 19.92362218466222146, 3.447839857233216065 ) ) ;
#20323=CARTESIAN_POINT ( 'NONE',  ( 6.603665676729555400, 11.36662928180900245, 5.110622262987013720 ) ) ;
#20324=CARTESIAN_POINT ( 'NONE',  ( 12.34266837804400652, 21.04141915754960124, 4.830946881310729246 ) ) ;
#20328=CARTESIAN_POINT ( 'NONE',  ( 8.173974635451950022, 10.80123558147565177, 1.780665030357663881 ) ) ;
#20329=CARTESIAN_POINT ( 'NONE',  ( 5.220610334371508010, 12.95168332381294185, 6.657391693586387937 ) ) ;
#20333=CARTESIAN_POINT ( 'NONE',  ( 7.290686113713969796, 16.23916015988696060, 7.633697861233664561 ) ) ;
#20338=CARTESIAN_POINT ( 'NONE',  ( 12.53826982310721760, 20.96877941592346062, -1.306849070834861459 ) ) ;
#20339=CARTESIAN_POINT ( 'NONE',  ( 5.199408160299433312, 13.09519236484694282, 6.678571109076385959 ) ) ;
#20340=CARTESIAN_POINT ( 'NONE',  ( -0.2371651909027980287, 15.59640844431605267, 0.003501526209365949521 ) ) ;
#20343=CARTESIAN_POINT ( 'NONE',  ( 3.429500974719062789, 20.64447347884702211, 3.600101472896897192 ) ) ;
#20348=CARTESIAN_POINT ( 'NONE',  ( 9.799408270453200842, 21.70432287120915049, 3.636903252768435735 ) ) ;
#20351=CARTESIAN_POINT ( 'NONE',  ( 13.13205531879375521, 14.07666409302394683, 5.907529146869096692 ) ) ;
#20354=CARTESIAN_POINT ( 'NONE',  ( 5.120992095093605201, 15.72743057685165802, 8.262704913055413769 ) ) ;
#20359=CARTESIAN_POINT ( 'NONE',  ( 4.799915934078755164, 20.26255486774721248, 1.564252215958407133 ) ) ;
#20362=CARTESIAN_POINT ( 'NONE',  ( 6.166197546908935401, 11.63697354833761999, 2.910818794907168439 ) ) ;
#20364=CARTESIAN_POINT ( 'NONE',  ( 7.819555740045376346, 12.04827940076156167, 0.2608701021987142044 ) ) ;
#20365=CARTESIAN_POINT ( 'NONE',  ( 3.485963715524843742, 20.55826902126646516, 3.672317462111338138 ) ) ;
#20366=CARTESIAN_POINT ( 'NONE',  ( 9.203386509245278901, 13.35056178516542325, 6.330368121291361838 ) ) ;
#20367=CARTESIAN_POINT ( 'NONE',  ( -0.5919464516433436962, 20.48604666719226230, 3.193387457549251796 ) ) ;
#20368=CARTESIAN_POINT ( 'NONE',  ( 12.60601076739248327, 20.52367786489136137, 5.624087213552067865 ) ) ;
#20374=CARTESIAN_POINT ( 'NONE',  ( 10.03169832878702117, 20.65254351994676085, 4.214616478178461634 ) ) ;
#20375=CARTESIAN_POINT ( 'NONE',  ( 7.749636708646758798, 11.34385124051986260, -0.1345962991897982075 ) ) ;
#20378=CARTESIAN_POINT ( 'NONE',  ( 12.67276266913473748, 22.06958725633792184, -0.07262669481182190689 ) ) ;
#20379=CARTESIAN_POINT ( 'NONE',  ( 3.208307485241757906, 15.46201706931346465, -1.280579935455534279 ) ) ;
#20382=CARTESIAN_POINT ( 'NONE',  ( 6.885262695410362177, 11.24414697040129063, 4.942298119348675911 ) ) ;
#20390=CARTESIAN_POINT ( 'NONE',  ( 1.890944370799874541, 14.70949108297185148, 0.3943759294202709986 ) ) ;
#20394=CARTESIAN_POINT ( 'NONE',  ( 4.262462685244984506, 21.03436180001830280, 5.762487426441945892 ) ) ;
#20396=ORIENTED_EDGE ( 'NONE', *, *, #20441, .T. ) ;
#20404=CARTESIAN_POINT ( 'NONE',  ( 10.81178337345588325, 14.41047425500502754, -3.325797169458144076 ) ) ;
#20405=CARTESIAN_POINT ( 'NONE',  ( 6.300769185105590253, 10.85645724975988102, 2.341303324005514330 ) ) ;
#20413=CARTESIAN_POINT ( 'NONE',  ( 7.674060797080146656, 17.99804626195093604, -1.858667960427092147 ) ) ;
#20418=CARTESIAN_POINT ( 'NONE',  ( 0.03294387470584737160, 17.99883169841178798, 0.2953920376092236677 ) ) ;
#20421=CARTESIAN_POINT ( 'NONE',  ( 7.439960277765663932, 14.95027458788505648, 7.491747371440758307 ) ) ;
#20427=CARTESIAN_POINT ( 'NONE',  ( 7.105517633241734465, 12.68409469243044363, -1.498797362056894178 ) ) ;
#20430=CARTESIAN_POINT ( 'NONE',  ( 13.20209200828312213, 17.93610798938899009, 6.956049917908053715 ) ) ;
#20434=CARTESIAN_POINT ( 'NONE',  ( 8.748152297807935796, 10.99744108201296200, 4.197803002740799094 ) ) ;
#20435=CARTESIAN_POINT ( 'NONE',  ( 4.546966478565406256, 19.89702943876222108, 0.8570823776154778972 ) ) ;
#20438=CARTESIAN_POINT ( 'NONE',  ( 5.701877479152492434, 17.15261597397144300, -1.334721615692817220 ) ) ;
#20439=CARTESIAN_POINT ( 'NONE',  ( 7.249888997917891764, 16.72360887485966074, 7.615665674260959861 ) ) ;
#20441=EDGE_CURVE ( 'NONE', #8132, #14025, #8751, .T. ) ;
#20443=CARTESIAN_POINT ( 'NONE',  ( 8.923014816335598454, 10.82907781979698214, 3.585810476635211241 ) ) ;
#20444=CARTESIAN_POINT ( 'NONE',  ( 5.159236230403464241, 12.90301316724979230, 6.473078888706812251 ) ) ;
#20446=CARTESIAN_POINT ( 'NONE',  ( 1.728822989146519440, 14.62510310756713672, -0.5323761966249557220 ) ) ;
#20459=CARTESIAN_POINT ( 'NONE',  ( 11.42955962579599749, 15.93097772868936168, 7.566103074860009770 ) ) ;
#20462=CARTESIAN_POINT ( 'NONE',  ( 11.26921146954438413, 17.34425637698345923, -3.509015127993665661 ) ) ;
#20465=CARTESIAN_POINT ( 'NONE',  ( 1.887498576900284109, 12.45711053362852283, 2.199572882868206847 ) ) ;
#20472=CARTESIAN_POINT ( 'NONE',  ( 6.007916013726672055, 11.31933379639777115, 2.935026084599358764 ) ) ;
#20476=CARTESIAN_POINT ( 'NONE',  ( 11.19173535783985152, 14.04501930844190660, 6.392579086694298418 ) ) ;
#20477=CARTESIAN_POINT ( 'NONE',  ( 6.506685236307152564, 11.60683490608310109, 3.211009186061718257 ) ) ;
#20478=CARTESIAN_POINT ( 'NONE',  ( 7.122533101144574275, 11.31448603738602188, 4.043997548448434287 ) ) ;
#20479=CARTESIAN_POINT ( 'NONE',  ( 14.21445728800946284, 21.25436666907090455, 4.255708983630563047 ) ) ;
#20487=CARTESIAN_POINT ( 'NONE',  ( 11.18224210415232456, 14.09124794490483268, 6.296053100427162263 ) ) ;
#20488=CARTESIAN_POINT ( 'NONE',  ( 14.25886707861190317, 21.25379664657874201, 4.242019184281260458 ) ) ;
#20490=CARTESIAN_POINT ( 'NONE',  ( 9.560141457007446775, 12.54285006689521254, -1.123051139442911461 ) ) ;
#20493=CARTESIAN_POINT ( 'NONE',  ( 1.405129138340541095, 15.60105019847626551, 9.663121315511631337 ) ) ;
#20496=CARTESIAN_POINT ( 'NONE',  ( 7.545992013913784824, 14.98089472672740108, 8.224318917088369929 ) ) ;
#20508=CARTESIAN_POINT ( 'NONE',  ( 5.361345772312789748, 18.08181486485797151, 8.509980462542200641 ) ) ;
#20522=CARTESIAN_POINT ( 'NONE',  ( 12.56986601621718691, 21.56964499642510091, 0.5722652997315497148 ) ) ;
#20523=CARTESIAN_POINT ( 'NONE',  ( -0.8825336784069820473, 20.56338889613970267, 3.242279024569009405 ) ) ;
#20526=CARTESIAN_POINT ( 'NONE',  ( 5.554765356073480653, 16.44746175198124405, 8.797311439034340097 ) ) ;
#20530=CARTESIAN_POINT ( 'NONE',  ( 7.846877201118635625, 12.15104000883038537, 0.2813510595362812561 ) ) ;
#20539=CARTESIAN_POINT ( 'NONE',  ( 1.088522589645603000, 20.85754858585166360, 2.898279402437147212 ) ) ;
#20543=CARTESIAN_POINT ( 'NONE',  ( 6.603476639551990601, 11.57021355890683978, 2.365220911883943344 ) ) ;
#20549=CARTESIAN_POINT ( 'NONE',  ( 8.761638600038448743, 15.29706862181782512, -3.464711856886600660 ) ) ;
#20551=CARTESIAN_POINT ( 'NONE',  ( 12.57654759969153702, 20.51656419951514110, 5.451503052877947120 ) ) ;
#20556=CARTESIAN_POINT ( 'NONE',  ( 9.221243833658917310, 12.25319662620856143, 6.274096147298578785 ) ) ;
#20558=CARTESIAN_POINT ( 'NONE',  ( 5.273483451284230128, 17.31877066267591658, 8.017556808149928216 ) ) ;
#20560=CARTESIAN_POINT ( 'NONE',  ( 5.797071389579374845, 12.91321502391278742, 0.09936575144167419937 ) ) ;
#20565=CARTESIAN_POINT ( 'NONE',  ( 5.729046844393140603, 13.63276237276972047, -1.556263347886826187 ) ) ;
#20566=CARTESIAN_POINT ( 'NONE',  ( 13.36585934105912976, 21.37707621349031228, 1.842755075219712380 ) ) ;
#20568=CARTESIAN_POINT ( 'NONE',  ( 1.710065114712777667, 15.58894874012881182, 9.662144323068869056 ) ) ;
#20570=ADVANCED_FACE ( 'NONE', ( #1151 ), #19605, .F. ) ;
#20578=CARTESIAN_POINT ( 'NONE',  ( 9.791419832355172659, 21.71027370924136335, 3.614944401813668495 ) ) ;
#20581=CARTESIAN_POINT ( 'NONE',  ( 12.16437857509334819, 11.19183223096340996, 1.439027855815902202 ) ) ;
#20583=CARTESIAN_POINT ( 'NONE',  ( 0.1247290703374178134, 20.17339616899437971, 6.210515518518696432 ) ) ;
#20587=CARTESIAN_POINT ( 'NONE',  ( 5.070222232012492114, 20.55825108723754369, 2.267750972750755434 ) ) ;
#20595=CARTESIAN_POINT ( 'NONE',  ( 8.619290438615989203, 20.62750485818692070, 0.1704299149245824263 ) ) ;
#20597=CARTESIAN_POINT ( 'NONE',  ( 10.31578413853228682, 20.34374524028692122, 4.916019394167047807 ) ) ;
#20598=CARTESIAN_POINT ( 'NONE',  ( 0.3579321758081180915, 12.59227895038538136, 1.630876906149107519 ) ) ;
#20605=CARTESIAN_POINT ( 'NONE',  ( 9.388131599695491047, 12.85887757399174092, 6.947284762616122933 ) ) ;
#20608=CARTESIAN_POINT ( 'NONE',  ( 9.951587701580805856, 11.56453706330047204, 0.6480317735763235776 ) ) ;
#20610=CARTESIAN_POINT ( 'NONE',  ( 12.84835963116946722, 22.16018907189590337, 0.4163025617756601626 ) ) ;
#20611=CARTESIAN_POINT ( 'NONE',  ( 3.870182538663821337, 11.34862606615942227, 2.113216645665817239 ) ) ;
#20635=CARTESIAN_POINT ( 'NONE',  ( 11.25603071367706143, 18.10558555414991844, -3.386525855160758436 ) ) ;
#20636=CARTESIAN_POINT ( 'NONE',  ( 5.651302110662487443, 15.64116283607404689, 8.852329451391270254 ) ) ;
#20639=CARTESIAN_POINT ( 'NONE',  ( 4.987524875783154954, 11.43561499633722178, 5.539610460427389249 ) ) ;
#20643=CARTESIAN_POINT ( 'NONE',  ( 8.046159076093074347, 19.48966040285201018, -1.019939477906512737 ) ) ;
#20645=CARTESIAN_POINT ( 'NONE',  ( 1.455225922851533182, 14.34770218287011723, 8.351802277904694094 ) ) ;
#20648=CARTESIAN_POINT ( 'NONE',  ( 3.430012568879817980, 15.13584884034968780, 8.277410437623871076 ) ) ;
#20652=CARTESIAN_POINT ( 'NONE',  ( 1.250047875415068344, 21.00885809591095210, 3.329580551905352070 ) ) ;
#20655=CARTESIAN_POINT ( 'NONE',  ( 0.4435595513821114499, 17.28679025579738138, 0.2841677601690540955 ) ) ;
#20663=CARTESIAN_POINT ( 'NONE',  ( 13.71574892877014307, 21.56570388316688280, 3.741136478433525259 ) ) ;
#20665=CARTESIAN_POINT ( 'NONE',  ( 13.06958847994923012, 11.92395113995147327, 5.272319428283388731 ) ) ;
#20669=CARTESIAN_POINT ( 'NONE',  ( 8.802176959052905758, 11.07856084916381079, 4.427857316288414502 ) ) ;
#20670=CARTESIAN_POINT ( 'NONE',  ( 1.504320668523305260, 14.30666394527731633, 8.418582497567321354 ) ) ;
#20672=CARTESIAN_POINT ( 'NONE',  ( 5.995197512313855448, 18.75043017290921199, -0.7670460466430296664 ) ) ;
#20674=CARTESIAN_POINT ( 'NONE',  ( 1.716565355178531371, 20.41010863060546754, 4.584836742679530452 ) ) ;
#20677=CARTESIAN_POINT ( 'NONE',  ( 13.28865384689049911, 11.60770318476056140, 4.300680844371669309 ) ) ;
#20678=CARTESIAN_POINT ( 'NONE',  ( 4.824783279085094634, 12.04281452664502616, 4.895154947829936098 ) ) ;
#20680=CARTESIAN_POINT ( 'NONE',  ( 7.555694491798023549, 14.71783044265311702, 8.271986479273186532 ) ) ;
#20681=CARTESIAN_POINT ( 'NONE',  ( 1.526914824943621962, 17.60663541863096526, 9.449669020237495332 ) ) ;
#20684=CARTESIAN_POINT ( 'NONE',  ( 0.6811041950880551976, 19.54923001721996201, 7.409756494194279064 ) ) ;
#20690=CARTESIAN_POINT ( 'NONE',  ( 8.942822476781397967, 21.77045158648074263, 1.273023891447270017 ) ) ;
#20694=CARTESIAN_POINT ( 'NONE',  ( 12.21848165272913711, 11.19810920596540171, 1.671241500708527283 ) ) ;
#20696=CARTESIAN_POINT ( 'NONE',  ( 0.6733089074914639927, 12.13066582883064193, 4.886095876978508556 ) ) ;
#20706=CARTESIAN_POINT ( 'NONE',  ( 11.40022844353273257, 21.35256525590422072, 1.960600886665106568 ) ) ;
#20707=CARTESIAN_POINT ( 'NONE',  ( 4.540541346939511946, 19.75650230952821929, 6.404782441630064937 ) ) ;
#20708=CARTESIAN_POINT ( 'NONE',  ( 11.32641745410349188, 12.84969026437554085, -2.393983499798812531 ) ) ;
#20709=CARTESIAN_POINT ( 'NONE',  ( 5.477926520976066804, 18.98716039713233883, 7.626504097506649593 ) ) ;
#20710=CARTESIAN_POINT ( 'NONE',  ( 14.20546330549358416, 21.25379664657874201, 4.258011758049313755 ) ) ;
#20715=CARTESIAN_POINT ( 'NONE',  ( 11.22190391525087350, 15.19668154793438930, 6.694160798341728835 ) ) ;
#20716=CARTESIAN_POINT ( 'NONE',  ( 9.151190155320593433, 13.32446407270766287, -2.918248225538348173 ) ) ;
#20720=CARTESIAN_POINT ( 'NONE',  ( 9.938994540168200942, 11.58108249686686264, 0.5927703295592824384 ) ) ;
#20723=CARTESIAN_POINT ( 'NONE',  ( -0.007942533697514499169, 12.00400186595892293, 3.420830230896959812 ) ) ;
#20726=CARTESIAN_POINT ( 'NONE',  ( 6.989266892685158439, 11.43297635884717245, 5.392041351863374743 ) ) ;
#20735=CARTESIAN_POINT ( 'NONE',  ( 1.989925793838051682, 17.03278999510542846, 0.1141983552420977044 ) ) ;
#20749=CARTESIAN_POINT ( 'NONE',  ( 6.736797773167128689, 11.82549305421424179, 4.274780649399409604 ) ) ;
#20751=CARTESIAN_POINT ( 'NONE',  ( 1.503361638335910078, 12.54475284465800300, 8.020844464906803140 ) ) ;
#20754=CARTESIAN_POINT ( 'NONE',  ( 5.598399313467577798, 15.02198729771266272, 8.635687164693491624 ) ) ;
#20758=CARTESIAN_POINT ( 'NONE',  ( 7.757688011553915963, 12.41336384027103179, -0.1314292562850493673 ) ) ;
#20765=CARTESIAN_POINT ( 'NONE',  ( 3.332715841987694105, 18.44329026216701095, 8.753185752870537684 ) ) ;
#20767=CARTESIAN_POINT ( 'NONE',  ( 0.3562249685988690961, 14.10021357005799025, 0.7816037492391179065 ) ) ;
#20774=CARTESIAN_POINT ( 'NONE',  ( 10.67274365531825886, 12.31998346384714083, 5.733264041280263790 ) ) ;
#20776=CARTESIAN_POINT ( 'NONE',  ( 11.48387577411441995, 11.17105998287007118, -1.405223482900355370 ) ) ;
#20781=CARTESIAN_POINT ( 'NONE',  ( 7.363730569273300830, 17.62799059285756798, -2.758751801371228662 ) ) ;
#20782=CARTESIAN_POINT ( 'NONE',  ( 7.274658096226261250, 13.47081914689558069, 6.777003322798922369 ) ) ;
#20785=CARTESIAN_POINT ( 'NONE',  ( 5.955397547760478361, 12.33419677638291745, 0.8607368628538174526 ) ) ;
#20786=CARTESIAN_POINT ( 'NONE',  ( 7.257706657338564682, 13.79373289338204600, 6.896359763853915581 ) ) ;
#20788=CARTESIAN_POINT ( 'NONE',  ( 13.41334640871851036, 18.63767531088674190, 6.295207162212891561 ) ) ;
#20789=CARTESIAN_POINT ( 'NONE',  ( 7.505451342482677646, 16.64385683817606321, 8.498745805386123564 ) ) ;
#20792=CARTESIAN_POINT ( 'NONE',  ( 0.1787847043407926884, 13.13615472609876100, 2.181548182976034145 ) ) ;
#20799=CARTESIAN_POINT ( 'NONE',  ( 10.14679030185686592, 10.59407055638359196, 1.519975852731572541 ) ) ;
#20802=CARTESIAN_POINT ( 'NONE',  ( 11.89704164873937842, 11.32715860939759267, 0.2885734480728872620 ) ) ;
#20803=CARTESIAN_POINT ( 'NONE',  ( 6.051356052310012501, 11.21701599786416104, 1.395022787371462236 ) ) ;
#20812=CARTESIAN_POINT ( 'NONE',  ( 9.653377856726027773, 12.37763185624888074, -1.110883424812121767 ) ) ;
#20813=CARTESIAN_POINT ( 'NONE',  ( 4.101486013225753346, 20.36808788457486585, 5.283137556898260812 ) ) ;
#20815=CARTESIAN_POINT ( 'NONE',  ( 12.91387984719911586, 18.46447794879854243, 6.063291446324524436 ) ) ;
#20824=CARTESIAN_POINT ( 'NONE',  ( 13.11485487186891241, 18.81117101484460363, 6.766740726881102397 ) ) ;
#20827=CARTESIAN_POINT ( 'NONE',  ( 10.10221342230659758, 11.41795989899646280, 1.305658110966970709 ) ) ;
#20831=CARTESIAN_POINT ( 'NONE',  ( 3.174975191938078645, 15.51072843360936204, -0.9428492389082121505 ) ) ;
#20843=CARTESIAN_POINT ( 'NONE',  ( 12.72410813526706264, 20.52725722417916288, 5.592342314984960261 ) ) ;
#20858=CARTESIAN_POINT ( 'NONE',  ( 3.499273979999799611, 15.44861990895924819, -1.457855545221536042 ) ) ;
#20862=CARTESIAN_POINT ( 'NONE',  ( 5.571606759789074381, 16.20829462093140094, 8.802327946292905381 ) ) ;
#20866=CARTESIAN_POINT ( 'NONE',  ( 3.179812809151942421, 12.83994299369714653, 6.696510645369547099 ) ) ;
#20875=CARTESIAN_POINT ( 'NONE',  ( 2.268027742546366632, 20.95393721777114138, 6.068657805862470056 ) ) ;
#20878=CARTESIAN_POINT ( 'NONE',  ( 4.845298251511239940, 19.94879251081626137, 6.357549859093562183 ) ) ;
#20880=CARTESIAN_POINT ( 'NONE',  ( 13.00897473812072391, 21.65922317907614314, 1.991038036765448327 ) ) ;
#20884=CARTESIAN_POINT ( 'NONE',  ( 8.839373267820224811, 17.29611120545237313, -3.150632400723435200 ) ) ;
#20888=CARTESIAN_POINT ( 'NONE',  ( 12.97938784431679871, 11.59103285605196376, 4.871812665424503308 ) ) ;
#20895=CARTESIAN_POINT ( 'NONE',  ( 7.456794536360651371, 18.25628204104152630, -2.578069215391849411 ) ) ;
#20896=CARTESIAN_POINT ( 'NONE',  ( 3.854910616174523241, 17.18874207142246391, -0.6971550151776942927 ) ) ;
#20898=CARTESIAN_POINT ( 'NONE',  ( 5.752222213375247861, 13.13460201027072216, -0.1270116662948033992 ) ) ;
#20901=CARTESIAN_POINT ( 'NONE',  ( 2.363086814207483677, 20.01344514090250826, 6.254446941780233971 ) ) ;
#20905=CARTESIAN_POINT ( 'NONE',  ( 13.59138924169983653, 12.98021359793846230, 5.706136380332087477 ) ) ;
#20906=CARTESIAN_POINT ( 'NONE',  ( 4.597578589995645615, 11.87873374808372162, 3.870235249179852399 ) ) ;
#20911=CARTESIAN_POINT ( 'NONE',  ( 5.463696641192596459, 17.51037618698124376, 8.782383522816124000 ) ) ;
#20912=CARTESIAN_POINT ( 'NONE',  ( 1.309911988839522756, 18.71936051987669103, 9.004577120499568821 ) ) ;
#20914=CARTESIAN_POINT ( 'NONE',  ( 2.488260037450269913, 12.01182523388594170, 3.580977260526816863 ) ) ;
#20923=CARTESIAN_POINT ( 'NONE',  ( 11.14095035894017016, 12.07673251640017575, 5.753578539164537986 ) ) ;
#20926=CARTESIAN_POINT ( 'NONE',  ( 11.16894477032718669, 14.35577606251322536, -3.188208178424544403 ) ) ;
#20927=CARTESIAN_POINT ( 'NONE',  ( 5.551670149194028347, 17.88589146158793497, -1.957965570236789521 ) ) ;
#20929=CARTESIAN_POINT ( 'NONE',  ( 2.748346265335036342, 12.03771362664550182, 5.108134015972813913 ) ) ;
#20934=CARTESIAN_POINT ( 'NONE',  ( 5.079859231761485461, 20.56621614536522458, 2.293009940660624135 ) ) ;
#20939=CARTESIAN_POINT ( 'NONE',  ( 12.89342041094828950, 11.95028677413862184, 4.185046594104111506 ) ) ;
#20940=CARTESIAN_POINT ( 'NONE',  ( 13.22309003533597149, 14.87475635823169640, 6.306761496560224778 ) ) ;
#20942=CARTESIAN_POINT ( 'NONE',  ( 1.961280780403269919, 14.65425108942523558, -0.5112595838893696509 ) ) ;
#20945=CARTESIAN_POINT ( 'NONE',  ( 5.126637874363053626, 19.15177079234708657, 7.986558305953045611 ) ) ;
#20951=CARTESIAN_POINT ( 'NONE',  ( 11.88288295434202624, 10.32531656698114020, 0.6793906613759156388 ) ) ;
#20954=CARTESIAN_POINT ( 'NONE',  ( 9.294500025656509123, 15.45828556898034734, -2.774045182040303370 ) ) ;
#20956=CARTESIAN_POINT ( 'NONE',  ( 0.9543875819854121811, 18.83975182281294636, 7.997141017239727923 ) ) ;
#20957=CARTESIAN_POINT ( 'NONE',  ( 0.6905276204882465629, 12.01664638779708127, 6.542292752354295082 ) ) ;
#20969=CARTESIAN_POINT ( 'NONE',  ( 1.880748080628404706, 15.39144081427376420, 0.1755720974858563377 ) ) ;
#20979=CARTESIAN_POINT ( 'NONE',  ( 1.494606009698838944, 12.54422677008150089, 8.023943171028003363 ) ) ;
#20982=CARTESIAN_POINT ( 'NONE',  ( 4.977942198378800143, 11.41917163132907120, 5.497878961665747077 ) ) ;
#20997=CARTESIAN_POINT ( 'NONE',  ( 3.607082928935879895, 13.97555289970940073, 8.644940775583602743 ) ) ;
#20999=CARTESIAN_POINT ( 'NONE',  ( 5.924761280269495778, 20.92139076675124443, 3.649616420326865285 ) ) ;
#21005=CARTESIAN_POINT ( 'NONE',  ( 6.060151407706388937, 11.20245161629656039, 3.350174019466126474 ) ) ;
#21008=CARTESIAN_POINT ( 'NONE',  ( 13.10951894981414867, 12.11001230185141786, 5.455309207400817151 ) ) ;
#21014=CARTESIAN_POINT ( 'NONE',  ( 7.261187168899082778, 16.54920457881469886, -2.885752199914386029 ) ) ;
#21015=CARTESIAN_POINT ( 'NONE',  ( 5.078941371105551994, 20.64340025166658421, 2.206626728022376582 ) ) ;
#21017=CARTESIAN_POINT ( 'NONE',  ( 9.026273815804650269, 17.99597701874386857, 6.937175287538173585 ) ) ;
#21020=CARTESIAN_POINT ( 'NONE',  ( 9.566581944649177771, 16.63265789203856571, 8.068133590630180763 ) ) ;
#21023=CARTESIAN_POINT ( 'NONE',  ( 5.974525327850455092, 11.27374497607938331, 1.150844946209645281 ) ) ;
#21024=CARTESIAN_POINT ( 'NONE',  ( 0.5711861650135396928, 20.53971507009796582, 7.163690434893576153 ) ) ;
#21026=CARTESIAN_POINT ( 'NONE',  ( 3.438407941595215789, 20.64378046205170136, 3.597508128396356586 ) ) ;
#21032=CARTESIAN_POINT ( 'NONE',  ( 10.25539797921433305, 10.56827346328852180, 1.972515333481110966 ) ) ;
#21037=CARTESIAN_POINT ( 'NONE',  ( 12.23137370410826819, 20.73799744225223662, -1.222527140174004101 ) ) ;
#21039=CARTESIAN_POINT ( 'NONE',  ( 5.904678845644677487, 11.49597437809906175, 0.7599978852366778836 ) ) ;
#21045=CARTESIAN_POINT ( 'NONE',  ( 7.035885886489748664, 20.81034843036036008, 1.590094180731808082 ) ) ;
#21046=CARTESIAN_POINT ( 'NONE',  ( 11.04177093970491796, 12.61615142531242206, 5.335282712017707318 ) ) ;
#21051=CARTESIAN_POINT ( 'NONE',  ( 6.686115959966646649, 11.04801462030960124, 4.499309094865339809 ) ) ;
#21055=CARTESIAN_POINT ( 'NONE',  ( 11.89814607795056567, 20.86867481596476281, 3.568910319330255820 ) ) ;
#21057=CARTESIAN_POINT ( 'NONE',  ( 0.2969748822967107071, 20.02444497997899120, 6.387532496747772015 ) ) ;
#21058=CARTESIAN_POINT ( 'NONE',  ( -0.1087599157681504863, 18.79999059560985231, 1.111494402889351862 ) ) ;
#21080=CARTESIAN_POINT ( 'NONE',  ( 3.419644087157343471, 18.28285541323128172, 8.928697526465610323 ) ) ;
#21083=CARTESIAN_POINT ( 'NONE',  ( 3.536909635595521184, 14.31338586005548130, -1.014190559432231797 ) ) ;
#21088=CARTESIAN_POINT ( 'NONE',  ( 2.916021650325829828, 12.21811100267743733, 5.442930941693839841 ) ) ;
#21094=CARTESIAN_POINT ( 'NONE',  ( 2.327109608273303820, 11.46633807340895217, 2.834091541352135479 ) ) ;
#21102=CARTESIAN_POINT ( 'NONE',  ( 7.758210749474673484, 11.08822532131044092, 1.918839297919416209 ) ) ;
#21106=CARTESIAN_POINT ( 'NONE',  ( 11.37417598588403855, 11.47492681191282138, -1.878663321889223248 ) ) ;
#21110=CARTESIAN_POINT ( 'NONE',  ( 7.285362733318168971, 16.88496392601005169, -2.871492799055576306 ) ) ;
#21111=CARTESIAN_POINT ( 'NONE',  ( 4.987365615438958066, 18.75973248553390604, 7.424326911423349884 ) ) ;
#21113=CARTESIAN_POINT ( 'NONE',  ( 8.577539078451785315, 19.63064409721748760, 5.907937441234182963 ) ) ;
#21117=CARTESIAN_POINT ( 'NONE',  ( 11.56363519470911072, 15.66465130118744398, 7.635224955696247484 ) ) ;
#21121=CARTESIAN_POINT ( 'NONE',  ( 0.01692536528957819947, 12.52705325500010325, 1.673389856107192264 ) ) ;
#21122=CARTESIAN_POINT ( 'NONE',  ( 1.619022443389374066, 16.88178287650320897, 9.587058323116350422 ) ) ;
#21124=CARTESIAN_POINT ( 'NONE',  ( 6.658410181020286700, 19.52167825130506174, 6.491640720976068479 ) ) ;
#21132=CARTESIAN_POINT ( 'NONE',  ( 10.76973421761783634, 11.01165039305489124, 4.129500176367342235 ) ) ;
#21135=CARTESIAN_POINT ( 'NONE',  ( 5.587485780822771808, 18.11784435417043682, -1.888017477237385000 ) ) ;
#21144=CARTESIAN_POINT ( 'NONE',  ( 9.565946762921560875, 16.58550361725992772, 7.310886168574319832 ) ) ;
#21145=CARTESIAN_POINT ( 'NONE',  ( 5.207204373775217832, 17.45024786592896149, 7.901522660181242053 ) ) ;
#21147=CARTESIAN_POINT ( 'NONE',  ( 8.652634833497350186, 19.63015825768726330, 6.037056894049368516 ) ) ;
#21153=CARTESIAN_POINT ( 'NONE',  ( 4.961560515085757572, 19.69663529535471014, 7.584757291997314077 ) ) ;
#21159=CARTESIAN_POINT ( 'NONE',  ( 9.599060309614154463, 18.43758607429610308, -2.436434164187765816 ) ) ;
#21161=CARTESIAN_POINT ( 'NONE',  ( 0.4283631078011292947, 19.87700971128948524, 6.719787991462967014 ) ) ;
#21163=CARTESIAN_POINT ( 'NONE',  ( 3.143185894743523612, 14.84625823140281753, 8.814386136658805881 ) ) ;
#21174=CARTESIAN_POINT ( 'NONE',  ( 7.535583205468054935, 13.14768317755540039, -1.049594630872383361 ) ) ;
#21186=CARTESIAN_POINT ( 'NONE',  ( 2.899943480386378614, 11.23735775897588240, 5.220590930253522721 ) ) ;
#21189=CARTESIAN_POINT ( 'NONE',  ( 3.548261816934641377, 14.10662813518449710, -0.9291583932840015159 ) ) ;
#21193=CARTESIAN_POINT ( 'NONE',  ( 0.8456107407395869746, 12.23494454746245097, 5.237939145250719797 ) ) ;
#21202=CARTESIAN_POINT ( 'NONE',  ( 3.244888726987362304, 11.99121938177022173, 6.831822597935710562 ) ) ;
#21212=CARTESIAN_POINT ( 'NONE',  ( 8.815742426116205621, 21.23906099414256232, 1.844918515833101624 ) ) ;
#21215=CARTESIAN_POINT ( 'NONE',  ( 10.94810466157118256, 16.27247983235652384, -4.349187853150674243 ) ) ;
#21219=CARTESIAN_POINT ( 'NONE',  ( 7.224900101663735974, 14.64899027572959689, -2.626539992268202006 ) ) ;
#21221=CARTESIAN_POINT ( 'NONE',  ( 6.774608736861511993, 20.53452479865724456, 1.173560763751360980 ) ) ;
#21228=CARTESIAN_POINT ( 'NONE',  ( 12.30760114933989868, 21.61111399576532222, 3.840915675052047007 ) ) ;
#21233=CARTESIAN_POINT ( 'NONE',  ( 6.822374228803519181, 20.09399725779506340, 7.039163523395035149 ) ) ;
#21234=CARTESIAN_POINT ( 'NONE',  ( 0.7138079833445840627, 11.42373057883981247, 4.642704508746212433 ) ) ;
#21236=CARTESIAN_POINT ( 'NONE',  ( 1.161278549730571763, 12.40032227216336125, 6.252213015588909961 ) ) ;
#21245=CARTESIAN_POINT ( 'NONE',  ( 10.38674899259666162, 10.59278501052695098, 2.519868619535428955 ) ) ;
#21249=CARTESIAN_POINT ( 'NONE',  ( 12.62152852634566003, 21.21270663461748285, -0.1788462545625037481 ) ) ;
#21250=CARTESIAN_POINT ( 'NONE',  ( 5.470336632480330863, 17.23705307414203247, -2.093767104412924684 ) ) ;
#21253=CARTESIAN_POINT ( 'NONE',  ( 1.325961175420450333, 20.33382539468342287, 3.515434316510341883 ) ) ;
#21260=CARTESIAN_POINT ( 'NONE',  ( 12.34322936788867331, 20.88809130931168312, -1.203018507871442599 ) ) ;
#21273=CARTESIAN_POINT ( 'NONE',  ( 12.35123053909024904, 20.10583435259948715, 4.755396859769023266 ) ) ;
#21275=CARTESIAN_POINT ( 'NONE',  ( 0.7583887236725060932, 19.33151544516331199, 7.535919219584821249 ) ) ;
#21277=CARTESIAN_POINT ( 'NONE',  ( 1.201550318572446319, 14.26529943814340129, 8.588777914063905783 ) ) ;
#21288=CARTESIAN_POINT ( 'NONE',  ( 9.089864963733731429, 21.15296384697220233, 1.773382899297284210 ) ) ;
#21289=CARTESIAN_POINT ( 'NONE',  ( 9.352501096662308555, 12.85887757399174092, 6.957954859781140478 ) ) ;
#21299=CARTESIAN_POINT ( 'NONE',  ( 3.648839215576543893, 16.52268874363389628, 9.299509987714628778 ) ) ;
#21302=CARTESIAN_POINT ( 'NONE',  ( 3.899173628609031717, 18.90516298583656152, -0.8066410379536314013 ) ) ;
#21303=ADVANCED_FACE ( 'NONE', ( #21499 ), #4558, .T. ) ;
#21315=CARTESIAN_POINT ( 'NONE',  ( 3.461646834230382996, 12.83219514639866077, 7.850548974203960917 ) ) ;
#21324=CARTESIAN_POINT ( 'NONE',  ( 9.248416887644976825, 12.30663295771102383, -1.050148961336570652 ) ) ;
#21328=CARTESIAN_POINT ( 'NONE',  ( 12.13422153915409396, 21.45254555255133155, -1.556433456872093890 ) ) ;
#21333=CARTESIAN_POINT ( 'NONE',  ( 8.390788493197108622, 21.17394158998719433, -0.2334963480496760335 ) ) ;
#21334=CARTESIAN_POINT ( 'NONE',  ( 7.295279368536716547, 20.90511879603792167, 2.551392718645653090 ) ) ;
#21339=CARTESIAN_POINT ( 'NONE',  ( 3.604122478219174752, 16.52265399103842825, 9.312174804150144425 ) ) ;
#21340=CARTESIAN_POINT ( 'NONE',  ( 0.7629431678296610952, 11.42074363723537189, 4.856465998727349742 ) ) ;
#21342=CARTESIAN_POINT ( 'NONE',  ( 7.046384120664519024, 18.17920521194865913, 7.360324746534422147 ) ) ;
#21349=CARTESIAN_POINT ( 'NONE',  ( 9.553597871840317168, 19.49545814391576926, -2.744787722736090618 ) ) ;
#21353=CARTESIAN_POINT ( 'NONE',  ( 12.34524511935337543, 20.90878755461004346, -0.9203087109956159528 ) ) ;
#21354=CARTESIAN_POINT ( 'NONE',  ( 7.827212224107905847, 21.58676227676403059, 4.002251945881059925 ) ) ;
#21356=CARTESIAN_POINT ( 'NONE',  ( 3.621962727011649896, 15.57349433917915427, -0.6543932647608998732 ) ) ;
#21360=CARTESIAN_POINT ( 'NONE',  ( 6.632063100419781421, 19.53589599333302118, 6.336315105421093996 ) ) ;
#21364=CARTESIAN_POINT ( 'NONE',  ( 6.688107640665243103, 20.11689778289562014, 0.06817244078631719273 ) ) ;
#21365=CARTESIAN_POINT ( 'NONE',  ( 5.155436405379945519, 17.75259917515757024, 7.809584811493537337 ) ) ;
#21366=CARTESIAN_POINT ( 'NONE',  ( 4.884574842566780539, 11.05839472165502180, 3.726956720474497775 ) ) ;
#21369=CARTESIAN_POINT ( 'NONE',  ( 6.767924793147533258, 11.30044898972404965, 2.706056956047799389 ) ) ;
#21380=CARTESIAN_POINT ( 'NONE',  ( 12.46412619058443738, 19.82591093859932485, 5.041212240312027859 ) ) ;
#21382=CARTESIAN_POINT ( 'NONE',  ( 0.7218944351460162556, 19.40741025969103362, 7.447597755446342838 ) ) ;
#21391=CARTESIAN_POINT ( 'NONE',  ( 0.6626195881407476174, 19.22990431264859623, 1.911452493813652120 ) ) ;
#21394=CARTESIAN_POINT ( 'NONE',  ( 11.10629993265927951, 14.44082934938793272, -3.329231321055425852 ) ) ;
#21396=CARTESIAN_POINT ( 'NONE',  ( 7.705021094126213832, 11.34324505471928113, -0.1215938047098856639 ) ) ;
#21407=CARTESIAN_POINT ( 'NONE',  ( 0.1240714093338939339, 19.02512202735066182, 0.6848216044496894250 ) ) ;
#21410=CARTESIAN_POINT ( 'NONE',  ( 3.563401380057076739, 13.90534388967183688, -0.8314790740504168776 ) ) ;
#21415=CARTESIAN_POINT ( 'NONE',  ( 2.398074235537467125, 12.22537918657540246, 3.074432563163722154 ) ) ;
#21421=CARTESIAN_POINT ( 'NONE',  ( 2.443280369300999233, 11.34257332251352146, 3.338292367401025640 ) ) ;
#21431=CARTESIAN_POINT ( 'NONE',  ( 10.49070738783592915, 19.16255833366876260, 6.254498413846182103 ) ) ;
#21434=CARTESIAN_POINT ( 'NONE',  ( 10.95919977160705905, 14.02423986086742680, -3.881915835329841080 ) ) ;
#21438=CARTESIAN_POINT ( 'NONE',  ( 7.971212282706394703, 20.65571312975535889, 4.348524338217387708 ) ) ;
#21444=CARTESIAN_POINT ( 'NONE',  ( 1.351768079374881415, 12.22725232455871058, 7.465297556611946383 ) ) ;
#21448=CARTESIAN_POINT ( 'NONE',  ( 3.693332233841136514, 15.57283695825947412, -0.6801890634934508739 ) ) ;
#21455=CARTESIAN_POINT ( 'NONE',  ( 5.947658929124695071, 11.10665485570860156, 1.375830819723275145 ) ) ;
#21458=CARTESIAN_POINT ( 'NONE',  ( 12.87278157376591992, 21.37109313374715214, 0.5016493235560532948 ) ) ;
#21460=CARTESIAN_POINT ( 'NONE',  ( 6.957760857039438918, 21.53600301301377229, 1.616326073237095651 ) ) ;
#21462=CARTESIAN_POINT ( 'NONE',  ( 0.8306377868003163023, 19.66973114709098169, 2.255943557795851984 ) ) ;
#21467=CARTESIAN_POINT ( 'NONE',  ( 6.406648404943450004, 11.79079236785502260, 1.495512976961110185 ) ) ;
#21468=CARTESIAN_POINT ( 'NONE',  ( 5.367040623886392581, 15.74799863055303284, 8.000260316783158743 ) ) ;
#21470=CARTESIAN_POINT ( 'NONE',  ( 4.109322517731720303, 12.26666322754141980, 0.3490965934614432831 ) ) ;
#21474=CARTESIAN_POINT ( 'NONE',  ( 6.600193629736931022, 11.65214223036289276, 2.781968066501882664 ) ) ;
#21484=CARTESIAN_POINT ( 'NONE',  ( 10.67700820321931765, 20.99839770658254068, 0.2808976642710648286 ) ) ;
#21499=FACE_OUTER_BOUND ( 'NONE', #883, .T. ) ;
#21502=CARTESIAN_POINT ( 'NONE',  ( 5.641984309594026747, 12.08210925389420076, -0.3035586006813633664 ) ) ;
#21514=CARTESIAN_POINT ( 'NONE',  ( 1.795691274907587509, 18.25402966388874049, -0.4402665253856706817 ) ) ;
#21517=CARTESIAN_POINT ( 'NONE',  ( 3.582146072703705997, 13.71129357845431684, -0.7217611990671898292 ) ) ;
#21519=ORIENTED_EDGE ( 'NONE', *, *, #2449, .T. ) ;
#21522=CARTESIAN_POINT ( 'NONE',  ( 0.6793796526421052029, 12.22740754112877148, 4.469871391076155831 ) ) ;
#21531=CARTESIAN_POINT ( 'NONE',  ( 1.657803152234513355, 15.27370134203824925, -0.5790142783057288245 ) ) ;
#21540=CARTESIAN_POINT ( 'NONE',  ( 13.12251614003352707, 21.80725978669622123, 2.472223153733141832 ) ) ;
#21543=CARTESIAN_POINT ( 'NONE',  ( 11.57882746174914601, 20.16567382252436857, -3.032094887718085996 ) ) ;
#21544=EDGE_LOOP ( 'NONE', ( #21519, #10359 ) ) ;
#21549=CARTESIAN_POINT ( 'NONE',  ( 9.049540828476574816, 12.76716365958394661, 5.677328593145490210 ) ) ;
#21550=CARTESIAN_POINT ( 'NONE',  ( 7.040843878398417743, 12.58136646072892262, 5.765943884753188087 ) ) ;
#21553=CARTESIAN_POINT ( 'NONE',  ( 3.216025952483349659, 17.66257927194542887, 8.239042406146007025 ) ) ;
#21559=CARTESIAN_POINT ( 'NONE',  ( 5.125831596548154678, 19.21458830873230283, 8.081027414488584526 ) ) ;
#21560=CARTESIAN_POINT ( 'NONE',  ( 1.687027707696350021, 14.46428959965339089, 9.250708045227060694 ) ) ;
#21563=CARTESIAN_POINT ( 'NONE',  ( 4.090297026962545601, 18.69411302701743338, -0.1436813144736139303 ) ) ;
#21569=CARTESIAN_POINT ( 'NONE',  ( 8.330980629002562310, 21.35551480289056059, -0.1344304400260789845 ) ) ;
#21570=CARTESIAN_POINT ( 'NONE',  ( 9.314696995175902217, 18.34482884134195046, -3.294293335070737516 ) ) ;
#21573=CARTESIAN_POINT ( 'NONE',  ( 8.596786337317182003, 20.54162763964906446, 6.075574452332789477 ) ) ;
#21575=CARTESIAN_POINT ( 'NONE',  ( 6.917740723153603000, 12.34712571434790007, 5.616724432863675176 ) ) ;
#21583=CARTESIAN_POINT ( 'NONE',  ( 14.19715987342163466, 20.58788406416984174, 3.804178473946510763 ) ) ;
#21586=CARTESIAN_POINT ( 'NONE',  ( 7.550821753472927611, 18.47894807998623534, 7.895890258472527456 ) ) ;
#21600=CARTESIAN_POINT ( 'NONE',  ( 12.89029027226322732, 12.39999842064192670, 4.636274517891662228 ) ) ;
#21604=CARTESIAN_POINT ( 'NONE',  ( 5.501791265511759121, 11.93061510394686131, 0.9090210824104238974 ) ) ;
#21609=CARTESIAN_POINT ( 'NONE',  ( 3.798728974633189814, 16.66492728325505013, -0.6608801330569669119 ) ) ;
#21615=CARTESIAN_POINT ( 'NONE',  ( 0.3256322356561986986, 18.10962087754353789, 1.158861095437264233 ) ) ;
#21618=CARTESIAN_POINT ( 'NONE',  ( 9.877816227279955896, 11.51518149844540240, 0.4592217285865553555 ) ) ;
#21620=CARTESIAN_POINT ( 'NONE',  ( 9.037814056838087140, 11.49988781216720213, 5.512589366362954379 ) ) ;
#21624=CARTESIAN_POINT ( 'NONE',  ( 10.31240588659874291, 20.19701905685399623, 4.945787191147431372 ) ) ;
#21625=CARTESIAN_POINT ( 'NONE',  ( 11.34884033191374364, 22.16525292274814163, 2.020784021226117666 ) ) ;
#21632=CARTESIAN_POINT ( 'NONE',  ( 1.387196809356705973, 12.54098868903164110, 8.059042662999539530 ) ) ;
#21635=CARTESIAN_POINT ( 'NONE',  ( 6.267479123942431229, 21.08335768476283434, 5.486273385999922425 ) ) ;
#21636=VERTEX_POINT ( 'NONE', #3562 ) ;
#21642=CARTESIAN_POINT ( 'NONE',  ( 2.196290092118426518, 12.65458560452110248, 2.124815543687548214 ) ) ;
#21643=CARTESIAN_POINT ( 'NONE',  ( 12.45174026680245838, 21.52809012965692403, -1.595795982066800400 ) ) ;
#21648=CARTESIAN_POINT ( 'NONE',  ( 1.970306187853680280, 18.49127644496248735, -0.2525819039933897003 ) ) ;
#21652=CARTESIAN_POINT ( 'NONE',  ( 13.27863086949880156, 21.38512400881313624, 1.870058080168869763 ) ) ;
#21658=CARTESIAN_POINT ( 'NONE',  ( 11.77575330418671307, 21.24843477279145887, -1.235931630819451899 ) ) ;
#21667=CARTESIAN_POINT ( 'NONE',  ( 8.934272239977493868, 12.32793309878939247, 5.125849249461625234 ) ) ;
#21672=CARTESIAN_POINT ( 'NONE',  ( -0.06146464470125744678, 17.35439399542458716, 0.1308547258846398387 ) ) ;
#21675=CARTESIAN_POINT ( 'NONE',  ( 1.398876202885256603, 20.32969464963275996, 3.494799452748480029 ) ) ;
#21683=CARTESIAN_POINT ( 'NONE',  ( 13.27727761442571541, 16.76891278191635593, 7.308350614176763571 ) ) ;
#21685=CARTESIAN_POINT ( 'NONE',  ( 9.072002966528325274, 15.54209628577143221, -3.558562164394619476 ) ) ;
#21689=CARTESIAN_POINT ( 'NONE',  ( 6.889273768381389829, 21.47949826730284428, 1.429458743405805032 ) ) ;
#21691=CARTESIAN_POINT ( 'NONE',  ( 5.989966368381897333, 12.01572996145620209, 1.466525965593846292 ) ) ;
#21696=CARTESIAN_POINT ( 'NONE',  ( 12.00508793966407595, 19.77353779035612291, -2.692760160476166398 ) ) ;
#21697=CARTESIAN_POINT ( 'NONE',  ( 5.373035982240415898, 15.58686636370129897, 7.979283019396571142 ) ) ;
#21700=CARTESIAN_POINT ( 'NONE',  ( 2.208305404124148108, 18.21888756068997495, -0.4754449005480404500 ) ) ;
#21703=CARTESIAN_POINT ( 'NONE',  ( 6.522247128157750318, 10.95050744324944247, 2.754069170700927938 ) ) ;
#21714=CARTESIAN_POINT ( 'NONE',  ( 13.14439431963711513, 16.12856496372081239, 6.412664661205437433 ) ) ;
#21718=CARTESIAN_POINT ( 'NONE',  ( -0.2827414589499773756, 14.25064834509233158, 1.265090244379412532 ) ) ;
#21728=CARTESIAN_POINT ( 'NONE',  ( 9.649387129231474347, 18.90675885874853890, -2.308582331309884328 ) ) ;
#21730=CARTESIAN_POINT ( 'NONE',  ( 12.23173370279073957, 21.60877823626870153, -1.575334389537728308 ) ) ;
#21736=CARTESIAN_POINT ( 'NONE',  ( 10.22372860683003637, 20.36372907135105592, 4.717067546579229997 ) ) ;
#21737=CARTESIAN_POINT ( 'NONE',  ( 10.45581712281804343, 21.01184353768176294, 5.351293286372672320 ) ) ;
#21742=CARTESIAN_POINT ( 'NONE',  ( 1.201291853872432203, 18.94469375348566231, 9.016395128387324931 ) ) ;
#21744=CARTESIAN_POINT ( 'NONE',  ( 6.180567681604283159, 21.19261967444545292, 5.252651310456046829 ) ) ;
#21749=CARTESIAN_POINT ( 'NONE',  ( 2.520634914125955195, 12.09468909812262716, 3.637039390294387164 ) ) ;
#21750=CARTESIAN_POINT ( 'NONE',  ( 14.51673069786281900, 21.18286304486736427, 4.116190393922946278 ) ) ;
#21753=CARTESIAN_POINT ( 'NONE',  ( 2.410440815022877992, 20.02928331742002754, 0.8004643519925526141 ) ) ;
#21762=CARTESIAN_POINT ( 'NONE',  ( 10.21327483022897376, 11.26810435610842198, 2.205732127587809455 ) ) ;
#21769=CARTESIAN_POINT ( 'NONE',  ( 8.497508964807796161, 11.57115047926810369, 3.163812390448663248 ) ) ;
#21770=CARTESIAN_POINT ( 'NONE',  ( 6.778338134665419012, 11.93678929795636101, 4.550199992997654874 ) ) ;
#21771=CARTESIAN_POINT ( 'NONE',  ( 3.141658771633866643, 18.03423197346641160, 8.097196469975823874 ) ) ;
#21775=CARTESIAN_POINT ( 'NONE',  ( -0.1943992194620844105, 15.25965415824441074, 0.1619022894663725287 ) ) ;
#21781=CARTESIAN_POINT ( 'NONE',  ( 4.622599792338005997, 19.87391983916490190, 6.369022444568970265 ) ) ;
#21787=CARTESIAN_POINT ( 'NONE',  ( 12.31748130508202088, 20.46142704777525978, 5.647513992273966110 ) ) ;
#21788=CARTESIAN_POINT ( 'NONE',  ( 9.385176790940363389, 12.04513265762483698, -1.737864651385272907 ) ) ;
#21790=CARTESIAN_POINT ( 'NONE',  ( 9.230190439779004663, 18.33056329402273832, 7.627282159427823949 ) ) ;
#21797=CARTESIAN_POINT ( 'NONE',  ( 11.16053233441080828, 11.27323348914452161, 3.901379546146052757 ) ) ;
#21799=CARTESIAN_POINT ( 'NONE',  ( 6.299708290859729054, 11.35334887747070276, 1.087827900068284670 ) ) ;
#21803=CARTESIAN_POINT ( 'NONE',  ( 2.423484750520774167, 19.25858774544496299, 1.029796980820462116 ) ) ;
#21806=( NAMED_UNIT ( * ) PLANE_ANGLE_UNIT ( ) SI_UNIT ( $, .RADIAN. ) );
#21813=CARTESIAN_POINT ( 'NONE',  ( 12.49260597456722266, 19.74893178700066443, 5.112473264219437041 ) ) ;
#21817=CARTESIAN_POINT ( 'NONE',  ( 1.233214924422777692, 13.15932452227622207, 7.544853154380925631 ) ) ;
#21822=CARTESIAN_POINT ( 'NONE',  ( 4.135061152470012047, 18.65628895784566765, -0.06275338617684531051 ) ) ;
#21823=CARTESIAN_POINT ( 'NONE',  ( 6.380166963026771221, 10.92343582149830183, 2.794643371853744007 ) ) ;
#21830=CARTESIAN_POINT ( 'NONE',  ( 10.99711771549974060, 12.61666159072338189, 5.348159617015018519 ) ) ;
#21831=CARTESIAN_POINT ( 'NONE',  ( 8.643606387840399918, 19.62966740229102314, 6.039244586192593189 ) ) ;
#21833=CARTESIAN_POINT ( 'NONE',  ( 9.008345345023000661, 15.28249587578532065, -3.627796638107509963 ) ) ;
#21838=CARTESIAN_POINT ( 'NONE',  ( 9.957777320403202737, 20.74193055653752893, 4.019321122224012832 ) ) ;
#21839=CARTESIAN_POINT ( 'NONE',  ( 7.579231183649110193, 21.81319771123894213, 3.241726534174046659 ) ) ;
#21845=CARTESIAN_POINT ( 'NONE',  ( 3.982884606420732165, 21.32044071393296036, 5.285254693471478582 ) ) ;
#21848=CARTESIAN_POINT ( 'NONE',  ( 7.220887966238155542, 18.59188200624751985, 7.907029918178476890 ) ) ;
#21854=CARTESIAN_POINT ( 'NONE',  ( 1.988580286269568953, 13.59073803854975182, 1.058507375892315805 ) ) ;
#21855=CARTESIAN_POINT ( 'NONE',  ( 3.780609725159723045, 14.10045209010493750, -0.05903433680642554415 ) ) ;
#21859=CARTESIAN_POINT ( 'NONE',  ( 1.673089330097931704, 15.97351425540567327, -0.6816346176204383100 ) ) ;
#21861=ORIENTED_EDGE ( 'NONE', *, *, #20264, .T. ) ;
#21870=CARTESIAN_POINT ( 'NONE',  ( 8.025198030962046758, 20.59028652745482191, 4.762507451596738051 ) ) ;
#21876=CARTESIAN_POINT ( 'NONE',  ( 9.270245272572291029, 14.90869586488222076, 7.012989310538706889 ) ) ;
#21877=EDGE_CURVE ( 'NONE', #21636, #8219, #15400, .T. ) ;
ENDSEC;
END-ISO-10303-21;
